ISO-10303-21;
HEADER;
/* Generated by software containing ST-Developer
 * from STEP Tools, Inc. (www.steptools.com) 
 */

FILE_DESCRIPTION(
/* description */ (
'Independent welded steel electronics enclosure with removable sealed 
lid, internal mounting tray and two threaded cable entries. 300 x 220 
mm body. No ingress or electrical safety rating assigned.'),
/* implementation_level */ '2;1');

FILE_NAME(
/* name */ 'Socket head cap screw M4x10.step',
/* time_stamp */ '2026-11-14T09:13:27-08:00',
/* author */ (''),
/* organization */ (''),
/* preprocessor_version */ 'ST-DEVELOPER v20.2',
/* originating_system */ 'Autodesk Translation Framework v15.17.0.0',
/* authorisation */ '');

FILE_SCHEMA (('AUTOMOTIVE_DESIGN { 1 0 10303 214 3 1 1 }'));
ENDSEC;

DATA;
#10=MECHANICAL_DESIGN_GEOMETRIC_PRESENTATION_REPRESENTATION('',(#977),#94412);
#153=CONICAL_SURFACE('',#8830,1.5,0.785398163397449);
#164=B_SPLINE_SURFACE_WITH_KNOTS('',3,3,((#78223,#78224,#78225,#78226,#78227,
#78228,#78229,#78230,#78231,#78232,#78233,#78234,#78235,#78236,#78237,#78238,
#78239,#78240,#78241,#78242,#78243,#78244,#78245,#78246,#78247,#78248,#78249,
#78250,#78251,#78252,#78253,#78254,#78255,#78256,#78257,#78258,#78259,#78260,
#78261,#78262,#78263,#78264,#78265,#78266,#78267,#78268,#78269,#78270,#78271,
#78272,#78273,#78274,#78275,#78276,#78277,#78278,#78279,#78280,#78281,#78282,
#78283,#78284,#78285,#78286,#78287,#78288,#78289,#78290,#78291,#78292,#78293,
#78294,#78295,#78296,#78297,#78298,#78299,#78300,#78301,#78302,#78303,#78304,
#78305,#78306,#78307,#78308,#78309,#78310),(#78311,#78312,#78313,#78314,
#78315,#78316,#78317,#78318,#78319,#78320,#78321,#78322,#78323,#78324,#78325,
#78326,#78327,#78328,#78329,#78330,#78331,#78332,#78333,#78334,#78335,#78336,
#78337,#78338,#78339,#78340,#78341,#78342,#78343,#78344,#78345,#78346,#78347,
#78348,#78349,#78350,#78351,#78352,#78353,#78354,#78355,#78356,#78357,#78358,
#78359,#78360,#78361,#78362,#78363,#78364,#78365,#78366,#78367,#78368,#78369,
#78370,#78371,#78372,#78373,#78374,#78375,#78376,#78377,#78378,#78379,#78380,
#78381,#78382,#78383,#78384,#78385,#78386,#78387,#78388,#78389,#78390,#78391,
#78392,#78393,#78394,#78395,#78396,#78397,#78398),(#78399,#78400,#78401,
#78402,#78403,#78404,#78405,#78406,#78407,#78408,#78409,#78410,#78411,#78412,
#78413,#78414,#78415,#78416,#78417,#78418,#78419,#78420,#78421,#78422,#78423,
#78424,#78425,#78426,#78427,#78428,#78429,#78430,#78431,#78432,#78433,#78434,
#78435,#78436,#78437,#78438,#78439,#78440,#78441,#78442,#78443,#78444,#78445,
#78446,#78447,#78448,#78449,#78450,#78451,#78452,#78453,#78454,#78455,#78456,
#78457,#78458,#78459,#78460,#78461,#78462,#78463,#78464,#78465,#78466,#78467,
#78468,#78469,#78470,#78471,#78472,#78473,#78474,#78475,#78476,#78477,#78478,
#78479,#78480,#78481,#78482,#78483,#78484,#78485,#78486),(#78487,#78488,
#78489,#78490,#78491,#78492,#78493,#78494,#78495,#78496,#78497,#78498,#78499,
#78500,#78501,#78502,#78503,#78504,#78505,#78506,#78507,#78508,#78509,#78510,
#78511,#78512,#78513,#78514,#78515,#78516,#78517,#78518,#78519,#78520,#78521,
#78522,#78523,#78524,#78525,#78526,#78527,#78528,#78529,#78530,#78531,#78532,
#78533,#78534,#78535,#78536,#78537,#78538,#78539,#78540,#78541,#78542,#78543,
#78544,#78545,#78546,#78547,#78548,#78549,#78550,#78551,#78552,#78553,#78554,
#78555,#78556,#78557,#78558,#78559,#78560,#78561,#78562,#78563,#78564,#78565,
#78566,#78567,#78568,#78569,#78570,#78571,#78572,#78573,#78574)),
 .UNSPECIFIED.,.F.,.F.,.F.,(4,4),(4,1,1,1,1,1,1,1,1,1,1,1,1,1,1,1,1,1,1,
1,1,1,1,1,1,1,1,1,1,1,1,1,1,1,1,1,1,1,1,1,1,1,1,1,1,1,1,1,1,1,1,1,1,1,1,
1,1,1,1,1,1,1,1,1,1,1,1,1,1,1,1,1,1,1,1,1,1,1,1,1,1,1,1,1,1,4),(-0.000292644816034893,
0.0463354841736447),(11.6151020157967,12.6127583869031,13.6100952546957,
14.6074321224883,15.6047689902808,16.6021058580734,17.599442725866,18.5967795936585,
19.5941164614511,20.5914533292437,21.5887901970362,22.5861270648288,23.5834639326213,
24.5808008004139,25.5781376682065,26.575474535999,27.5728114037916,28.5701482715842,
29.5674851393767,30.5648220071693,31.5621588749619,32.5594957427544,33.556832610547,
34.5541694783396,35.5515063461321,36.5488432139247,37.5461800817173,38.5435169495098,
39.5408538173024,40.538190685095,41.5355275528875,42.5328644206801,43.5302012884726,
44.5275381562652,45.5248750240578,46.5222118918503,47.5195487596429,48.5168856274355,
49.514222495228,50.5115593630206,51.5088962308132,52.5062330986057,53.5035699663983,
54.5009068341909,55.4982437019834,56.495580569776,57.4929174375686,58.4902543053611,
59.4875911731537,60.4849280409463,61.4822649087388,62.4796017765314,63.4769386443239,
64.4742755121165,65.4716123799091,66.4689492477016,67.4662861154942,68.4636229832868,
69.4609598510793,70.4582967188719,71.4556335866645,72.452970454457,73.4503073222496,
74.4476441900422,75.4449810578347,76.4423179256273,77.4396547934198,78.4369916612124,
79.434328529005,80.4316653967976,81.4290022645901,82.4263391323827,83.4236760001752,
84.4210128679678,85.4183497357604,86.4156866035529,87.4130234713455,88.4103603391381,
89.4076972069306,90.4050340747232,91.4023709425158,92.3997078103083,93.3970446781009,
94.3943815458935,95.391718413686,96.3893759491978),.UNSPECIFIED.);
#165=B_SPLINE_SURFACE_WITH_KNOTS('',3,3,((#78660,#78661,#78662,#78663,#78664,
#78665,#78666,#78667,#78668,#78669,#78670,#78671,#78672,#78673,#78674,#78675,
#78676,#78677,#78678,#78679,#78680,#78681,#78682,#78683,#78684,#78685,#78686,
#78687,#78688,#78689,#78690,#78691,#78692,#78693,#78694,#78695,#78696,#78697,
#78698,#78699,#78700,#78701,#78702,#78703,#78704,#78705,#78706,#78707,#78708,
#78709,#78710,#78711,#78712,#78713,#78714,#78715,#78716,#78717,#78718,#78719,
#78720,#78721,#78722,#78723,#78724,#78725,#78726,#78727,#78728,#78729,#78730,
#78731,#78732,#78733,#78734,#78735,#78736,#78737,#78738,#78739,#78740,#78741,
#78742,#78743,#78744,#78745,#78746,#78747,#78748,#78749),(#78750,#78751,
#78752,#78753,#78754,#78755,#78756,#78757,#78758,#78759,#78760,#78761,#78762,
#78763,#78764,#78765,#78766,#78767,#78768,#78769,#78770,#78771,#78772,#78773,
#78774,#78775,#78776,#78777,#78778,#78779,#78780,#78781,#78782,#78783,#78784,
#78785,#78786,#78787,#78788,#78789,#78790,#78791,#78792,#78793,#78794,#78795,
#78796,#78797,#78798,#78799,#78800,#78801,#78802,#78803,#78804,#78805,#78806,
#78807,#78808,#78809,#78810,#78811,#78812,#78813,#78814,#78815,#78816,#78817,
#78818,#78819,#78820,#78821,#78822,#78823,#78824,#78825,#78826,#78827,#78828,
#78829,#78830,#78831,#78832,#78833,#78834,#78835,#78836,#78837,#78838,#78839),
(#78840,#78841,#78842,#78843,#78844,#78845,#78846,#78847,#78848,#78849,
#78850,#78851,#78852,#78853,#78854,#78855,#78856,#78857,#78858,#78859,#78860,
#78861,#78862,#78863,#78864,#78865,#78866,#78867,#78868,#78869,#78870,#78871,
#78872,#78873,#78874,#78875,#78876,#78877,#78878,#78879,#78880,#78881,#78882,
#78883,#78884,#78885,#78886,#78887,#78888,#78889,#78890,#78891,#78892,#78893,
#78894,#78895,#78896,#78897,#78898,#78899,#78900,#78901,#78902,#78903,#78904,
#78905,#78906,#78907,#78908,#78909,#78910,#78911,#78912,#78913,#78914,#78915,
#78916,#78917,#78918,#78919,#78920,#78921,#78922,#78923,#78924,#78925,#78926,
#78927,#78928,#78929),(#78930,#78931,#78932,#78933,#78934,#78935,#78936,
#78937,#78938,#78939,#78940,#78941,#78942,#78943,#78944,#78945,#78946,#78947,
#78948,#78949,#78950,#78951,#78952,#78953,#78954,#78955,#78956,#78957,#78958,
#78959,#78960,#78961,#78962,#78963,#78964,#78965,#78966,#78967,#78968,#78969,
#78970,#78971,#78972,#78973,#78974,#78975,#78976,#78977,#78978,#78979,#78980,
#78981,#78982,#78983,#78984,#78985,#78986,#78987,#78988,#78989,#78990,#78991,
#78992,#78993,#78994,#78995,#78996,#78997,#78998,#78999,#79000,#79001,#79002,
#79003,#79004,#79005,#79006,#79007,#79008,#79009,#79010,#79011,#79012,#79013,
#79014,#79015,#79016,#79017,#79018,#79019)),.UNSPECIFIED.,.F.,.F.,.F.,(4,
4),(4,1,1,1,1,1,1,1,1,1,1,1,1,1,1,1,1,1,1,1,1,1,1,1,1,1,1,1,1,1,1,1,1,1,
1,1,1,1,1,1,1,1,1,1,1,1,1,1,1,1,1,1,1,1,1,1,1,1,1,1,1,1,1,1,1,1,1,1,1,1,
1,1,1,1,1,1,1,1,1,1,1,1,1,1,1,1,1,4),(-0.00032060916664835,0.0463085361130159),
(8.3104412613233,9.30873374912645,10.3068805755132,11.3050274018999,12.3031742282867,
13.3013210546734,14.2994678810601,15.2976147074469,16.2957615338336,17.2939083602203,
18.2920551866071,19.2902020129938,20.2883488393806,21.2864956657673,22.284642492154,
23.2827893185408,24.2809361449275,25.2790829713142,26.277229797701,27.2753766240877,
28.2735234504744,29.2716702768612,30.2698171032479,31.2679639296347,32.2661107560214,
33.2642575824081,34.2624044087949,35.2605512351816,36.2586980615683,37.2568448879551,
38.2549917143418,39.2531385407286,40.2512853671153,41.249432193502,42.2475790198888,
43.2457258462755,44.2438726726622,45.242019499049,46.2401663254357,47.2383131518225,
48.2364599782092,49.2346068045959,50.2327536309827,51.2309004573694,52.2290472837561,
53.2271941101429,54.2253409365296,55.2234877629163,56.2216345893031,57.2197814156898,
58.2179282420766,59.2160750684633,60.21422189485,61.2123687212368,62.2105155476235,
63.2086623740102,64.206809200397,65.2049560267837,66.2031028531704,67.2012496795572,
68.1993965059439,69.1975433323307,70.1956901587174,71.1938369851041,72.1919838114909,
73.1901306378776,74.1882774642643,75.1864242906511,76.1845711170378,77.1827179434245,
78.1808647698113,79.179011596198,80.1771584225848,81.1753052489715,82.1734520753582,
83.171598901745,84.1697457281317,85.1678925545184,86.1660393809052,87.1641862072919,
88.1623330336787,89.1604798600654,90.1586266864521,91.1567735128389,92.1549203392256,
93.1530671656123,94.1512139919991,95.1496814275525),.UNSPECIFIED.);
#751=B_SPLINE_CURVE_WITH_KNOTS('',3,(#70401,#70402,#70403,#70404,#70405,
#70406,#70407,#70408,#70409,#70410,#70411,#70412,#70413,#70414,#70415,#70416,
#70417,#70418,#70419,#70420,#70421,#70422,#70423,#70424,#70425,#70426,#70427,
#70428,#70429,#70430,#70431,#70432,#70433,#70434,#70435,#70436,#70437,#70438,
#70439,#70440,#70441,#70442,#70443,#70444,#70445,#70446,#70447,#70448,#70449,
#70450,#70451,#70452,#70453,#70454,#70455,#70456,#70457,#70458,#70459,#70460,
#70461,#70462,#70463,#70464,#70465,#70466,#70467,#70468,#70469,#70470,#70471,
#70472,#70473,#70474,#70475,#70476,#70477,#70478,#70479,#70480,#70481,#70482,
#70483,#70484,#70485,#70486,#70487,#70488,#70489,#70490,#70491,#70492,#70493,
#70494,#70495,#70496,#70497,#70498,#70499,#70500,#70501,#70502,#70503,#70504,
#70505,#70506,#70507,#70508,#70509,#70510,#70511,#70512,#70513,#70514,#70515,
#70516,#70517,#70518,#70519,#70520,#70521,#70522,#70523,#70524,#70525,#70526,
#70527,#70528,#70529,#70530,#70531,#70532,#70533,#70534,#70535,#70536,#70537,
#70538,#70539,#70540,#70541,#70542,#70543,#70544,#70545,#70546,#70547,#70548,
#70549,#70550,#70551,#70552),.UNSPECIFIED.,.F.,.F.,(4,2,2,2,2,2,2,2,2,2,
2,2,2,2,2,2,2,2,2,2,2,2,2,2,2,2,2,2,2,2,2,2,2,2,2,2,2,2,2,2,2,2,2,2,2,2,
2,2,2,2,2,2,2,2,2,2,2,2,2,2,2,2,2,2,2,2,2,2,2,2,2,2,2,2,2,4),(-0.832439720450299,
-0.826869617590163,-0.808861481405132,-0.780833499987269,-0.773067704421429,
-0.770108009538214,-0.768116382574119,-0.765959909741239,-0.762312705606626,
-0.745384908804739,-0.710099303019498,-0.698437745806221,-0.693536562115759,
-0.690028044113998,-0.686321672851416,-0.680574311193837,-0.659513503810848,
-0.641702968844016,-0.619034945456304,-0.615199849331523,-0.613000754903716,
-0.610993910382176,-0.608099115151558,-0.600283250865247,-0.587338578003027,
-0.547496595729687,-0.540453152200995,-0.53643269261139,-0.532958434968226,
-0.528651633463663,-0.519936259154898,-0.496482419123063,-0.466547506714132,
-0.460791187104995,-0.458246606971097,-0.456292094196737,-0.453959155317699,
-0.449413634630061,-0.432138088304667,-0.391101350064625,-0.384215720243609,
-0.380253477545728,-0.376813274772498,-0.372529386569256,-0.363797509627219,
-0.340555173373787,-0.310851867363394,-0.304874719620947,-0.302302699397911,
-0.300345282932302,-0.298021463020673,-0.293587363299895,-0.266670733512251,
-0.235518952311434,-0.228315190518444,-0.224253817045827,-0.220772909219321,
-0.216494292647445,-0.207963661830024,-0.187274992636306,-0.162167397931397,
-0.150746811951765,-0.147346959752381,-0.145436952164745,-0.143356908199464,
-0.140258588566548,-0.131161889402246,-0.114680445555956,-0.0814104958311417,
-0.0745199702012672,-0.0704979001465721,-0.0673189880139064,-0.0630357511075485,
-0.054645733886394,-0.0361759680233267,-0.0023879060453043),
 .UNSPECIFIED.);
#752=B_SPLINE_CURVE_WITH_KNOTS('',3,(#70555,#70556,#70557,#70558,#70559,
#70560,#70561,#70562,#70563,#70564,#70565,#70566,#70567,#70568,#70569,#70570,
#70571,#70572,#70573,#70574,#70575,#70576,#70577,#70578,#70579,#70580,#70581,
#70582,#70583,#70584,#70585,#70586,#70587,#70588,#70589,#70590,#70591,#70592,
#70593,#70594,#70595,#70596,#70597,#70598,#70599,#70600,#70601,#70602,#70603,
#70604,#70605,#70606,#70607,#70608,#70609,#70610,#70611,#70612,#70613,#70614,
#70615,#70616,#70617,#70618,#70619,#70620,#70621,#70622,#70623,#70624,#70625,
#70626,#70627,#70628,#70629,#70630,#70631,#70632,#70633,#70634,#70635,#70636,
#70637,#70638,#70639,#70640,#70641,#70642,#70643,#70644,#70645,#70646,#70647,
#70648,#70649,#70650,#70651,#70652,#70653,#70654,#70655,#70656,#70657,#70658,
#70659,#70660,#70661,#70662,#70663,#70664,#70665,#70666),.UNSPECIFIED.,
 .F.,.F.,(4,3,3,3,3,3,3,3,3,3,3,3,3,3,3,3,3,3,3,3,3,3,3,3,3,3,3,3,3,3,3,
3,3,3,3,3,3,4),(11.6154215191106,11.7297367073171,11.8439967914085,11.9582288133417,
12.0724673659051,12.1867470405937,12.3011995048193,12.4157406678187,12.530525337464,
12.6127583869031,12.7233097241135,12.8341579154363,12.9443596551425,13.0544807973123,
13.1645659360347,13.2759482656999,13.3861659307822,13.4981305927389,13.6100952546957,
13.7219645675355,13.833635115484,13.9451945236061,14.0566854135963,14.1681503097769,
14.2797130483556,14.3913205741359,14.5031410552373,14.6074321224883,14.7193243877964,
14.8310242929563,14.9426169352525,15.0541448818272,15.165650607069,15.2772598312806,
15.3889170097142,15.5007919240759,15.6047689902808,15.7079632679489),
 .UNSPECIFIED.);
#753=B_SPLINE_CURVE_WITH_KNOTS('',3,(#70671,#70672,#70673,#70674,#70675,
#70676,#70677,#70678,#70679,#70680,#70681,#70682,#70683,#70684,#70685,#70686,
#70687,#70688,#70689,#70690,#70691,#70692,#70693,#70694,#70695,#70696,#70697,
#70698,#70699,#70700,#70701,#70702,#70703,#70704,#70705,#70706,#70707,#70708,
#70709,#70710,#70711,#70712,#70713,#70714,#70715,#70716,#70717,#70718,#70719,
#70720,#70721,#70722,#70723,#70724,#70725,#70726,#70727,#70728,#70729,#70730,
#70731,#70732,#70733,#70734,#70735,#70736,#70737,#70738,#70739,#70740,#70741,
#70742,#70743,#70744,#70745,#70746,#70747,#70748,#70749,#70750,#70751,#70752,
#70753,#70754,#70755,#70756,#70757,#70758,#70759,#70760,#70761,#70762,#70763,
#70764,#70765,#70766,#70767,#70768,#70769,#70770,#70771,#70772,#70773,#70774,
#70775,#70776,#70777,#70778,#70779,#70780,#70781,#70782,#70783,#70784,#70785,
#70786,#70787,#70788,#70789,#70790,#70791,#70792,#70793,#70794,#70795,#70796,
#70797,#70798,#70799,#70800,#70801,#70802,#70803,#70804,#70805,#70806,#70807,
#70808,#70809,#70810,#70811,#70812,#70813,#70814,#70815,#70816,#70817,#70818,
#70819,#70820,#70821,#70822,#70823,#70824,#70825,#70826,#70827,#70828,#70829,
#70830,#70831,#70832,#70833,#70834,#70835,#70836,#70837,#70838,#70839,#70840,
#70841,#70842,#70843,#70844,#70845,#70846,#70847,#70848,#70849,#70850,#70851,
#70852,#70853,#70854,#70855,#70856,#70857,#70858,#70859,#70860,#70861,#70862,
#70863,#70864,#70865,#70866),.UNSPECIFIED.,.F.,.F.,(4,2,2,2,2,2,2,2,2,2,
2,2,2,2,2,2,2,2,2,2,2,2,2,2,2,2,2,2,2,2,2,2,2,2,2,2,2,2,2,2,2,2,2,2,2,2,
2,2,2,2,2,2,2,2,2,2,2,2,2,2,2,2,2,2,2,2,2,2,2,2,2,2,2,2,2,2,2,2,2,2,2,2,
2,2,2,2,2,2,2,2,2,2,2,2,2,2,2,4),(-1.81266124409322,-1.79276733540908,-1.78774245874958,
-1.78413545154694,-1.78088602738699,-1.77736034007158,-1.77313278625767,
-1.7628751938338,-1.7323430897624,-1.71481907485556,-1.70722121063355,-1.70434762990126,
-1.7023504852535,-1.70015348315893,-1.69631767835098,-1.67351815566529,
-1.65541173314562,-1.64160753480484,-1.63183242889914,-1.62734498751931,
-1.62386335554168,-1.61997943666278,-1.61337001706326,-1.57553292977467,
-1.55521461552979,-1.55031952255415,-1.5479061712476,-1.54614597725326,
-1.54373626788022,-1.53886064333773,-1.51624503464281,-1.49171518082637,
-1.48221880177508,-1.47477499011064,-1.47072014374758,-1.46725832855774,
-1.46302087718533,-1.45646202949209,-1.42673369885665,-1.40664731369372,
-1.39972586861402,-1.39469439482473,-1.39225491704881,-1.39049374067723,
-1.38810922361249,-1.38350809718788,-1.35550847596574,-1.33447172786105,
-1.32160487271448,-1.31664992147481,-1.31309896675601,-1.30940398565582,
-1.30370368758022,-1.28496422757591,-1.25377074519704,-1.2452465080184,
-1.23938766061273,-1.23679901624852,-1.23483900918868,-1.23248535635403,
-1.22803136628759,-1.19791152225578,-1.17811930534118,-1.16966889416318,
-1.16285427057515,-1.1589275445767,-1.1554530653352,-1.15103746979047,-1.14167963972413,
-1.10345299130861,-1.08597266242713,-1.08230006165834,-1.08013759385632,
-1.07814544078735,-1.07519412185959,-1.0675132415997,-1.03577012209783,
-1.01674010447895,-1.00827217657733,-1.00401716030596,-1.00055292200238,
-0.996508697051606,-0.989330113494435,-0.958829720251869,-0.939285289971974,
-0.929240270944908,-0.926087449720401,-0.924036862450091,-0.921932934084776,
-0.918522952283085,-0.906720319599159,-0.879123388800726,-0.856559613760745,
-0.850608065480583,-0.846863204477219,-0.843342368646973,-0.838554784676353,
-0.832439720450299),.UNSPECIFIED.);
#754=B_SPLINE_CURVE_WITH_KNOTS('',3,(#70867,#70868,#70869,#70870,#70871,
#70872,#70873,#70874,#70875,#70876,#70877,#70878,#70879,#70880,#70881,#70882,
#70883,#70884,#70885,#70886,#70887,#70888,#70889,#70890,#70891,#70892,#70893,
#70894,#70895,#70896,#70897,#70898,#70899,#70900,#70901,#70902,#70903,#70904,
#70905,#70906,#70907,#70908,#70909,#70910,#70911,#70912,#70913,#70914,#70915,
#70916,#70917,#70918,#70919,#70920,#70921,#70922,#70923,#70924,#70925,#70926,
#70927,#70928,#70929,#70930,#70931,#70932,#70933,#70934,#70935,#70936,#70937,
#70938,#70939,#70940,#70941,#70942,#70943,#70944,#70945,#70946,#70947,#70948,
#70949,#70950,#70951,#70952,#70953,#70954,#70955,#70956,#70957,#70958,#70959,
#70960,#70961,#70962,#70963,#70964,#70965,#70966,#70967,#70968,#70969,#70970,
#70971,#70972,#70973,#70974,#70975,#70976,#70977,#70978,#70979,#70980,#70981,
#70982,#70983,#70984,#70985,#70986,#70987,#70988,#70989,#70990,#70991,#70992,
#70993,#70994,#70995,#70996,#70997,#70998,#70999,#71000,#71001,#71002,#71003,
#71004,#71005,#71006,#71007,#71008,#71009,#71010,#71011,#71012,#71013,#71014,
#71015,#71016,#71017,#71018,#71019,#71020,#71021,#71022,#71023,#71024,#71025,
#71026,#71027,#71028,#71029,#71030,#71031,#71032,#71033,#71034,#71035,#71036,
#71037,#71038,#71039,#71040,#71041,#71042,#71043,#71044,#71045,#71046,#71047,
#71048),.UNSPECIFIED.,.F.,.F.,(4,2,2,2,2,2,2,2,2,2,2,2,2,2,2,2,2,2,2,2,
2,2,2,2,2,2,2,2,2,2,2,2,2,2,2,2,2,2,2,2,2,2,2,2,2,2,2,2,2,2,2,2,2,2,2,2,
2,2,2,2,2,2,2,2,2,2,2,2,2,2,2,2,2,2,2,2,2,2,2,2,2,2,2,2,2,2,2,2,2,2,4),
(-1.96102087353794,-1.9210778220991,-1.90768908845313,-1.90261212238301,
-1.89899015149673,-1.89523318959838,-1.88945687161051,-1.87049428660702,
-1.83951008342334,-1.83097501089664,-1.82509143330846,-1.82247247770524,
-1.82048980956498,-1.81806425199519,-1.81343965417973,-1.78516880189389,
-1.76443962673408,-1.75162769858289,-1.74659723188267,-1.74295525739004,
-1.73912896791266,-1.73313981744852,-1.71180491373212,-1.68359856445809,
-1.67539295566126,-1.66966423271282,-1.66705279884891,-1.66523129778753,
-1.66284792368806,-1.65842885407551,-1.62771414722485,-1.61961046122069,
-1.60534611178343,-1.59530372652048,-1.59070105366264,-1.58712704584553,
-1.58313340890746,-1.57630917514173,-1.5346589707257,-1.51655478492516,
-1.51279866884452,-1.51058411870794,-1.50853877336182,-1.50548920668655,
-1.4973716571128,-1.46972231222516,-1.44787597417284,-1.43901825751871,
-1.43462845050102,-1.43107726977685,-1.42695364633554,-1.41968164444321,
-1.39470015102531,-1.37120756793841,-1.36008734388033,-1.35678146074471,
-1.35466499630122,-1.35251672689708,-1.34907010977359,-1.33745151397172,
-1.29225652359672,-1.28337842663391,-1.27898131374437,-1.27542515951872,
-1.27129654480343,-1.26401681150532,-1.23627793034829,-1.21497380005684,
-1.20779765089936,-1.20260594018093,-1.20009827410376,-1.19828959709471,
-1.19583459759449,-1.19091409455555,-1.16913219523892,-1.14959138748375,
-1.1371471825431,-1.12802558112617,-1.12358507365322,-1.12002743601037,
-1.11593420152398,-1.10881552061661,-1.07570747800498,-1.05034180750753,
-1.04630214323217,-1.0440267864096,-1.04198301226627,-1.0390664807431,-1.03185902089032,
-1.00344831019565,-0.980904423115737),.UNSPECIFIED.);
#755=B_SPLINE_CURVE_WITH_KNOTS('',3,(#71054,#71055,#71056,#71057,#71058,
#71059,#71060,#71061,#71062,#71063,#71064,#71065,#71066,#71067,#71068,#71069,
#71070,#71071,#71072,#71073,#71074,#71075,#71076,#71077,#71078,#71079,#71080,
#71081,#71082,#71083,#71084,#71085,#71086,#71087,#71088,#71089,#71090,#71091,
#71092,#71093,#71094,#71095,#71096,#71097,#71098,#71099,#71100,#71101,#71102,
#71103,#71104,#71105,#71106,#71107,#71108,#71109,#71110,#71111,#71112,#71113,
#71114,#71115,#71116,#71117,#71118,#71119,#71120,#71121,#71122,#71123,#71124,
#71125,#71126,#71127,#71128,#71129,#71130,#71131,#71132,#71133,#71134,#71135,
#71136,#71137,#71138,#71139,#71140,#71141,#71142,#71143,#71144,#71145,#71146,
#71147,#71148,#71149,#71150,#71151,#71152,#71153,#71154,#71155,#71156,#71157,
#71158,#71159,#71160,#71161,#71162,#71163,#71164,#71165,#71166,#71167,#71168,
#71169,#71170,#71171,#71172,#71173,#71174,#71175,#71176,#71177,#71178,#71179,
#71180,#71181,#71182,#71183,#71184,#71185,#71186,#71187,#71188,#71189,#71190,
#71191,#71192,#71193,#71194,#71195,#71196,#71197,#71198,#71199,#71200,#71201,
#71202,#71203,#71204,#71205,#71206,#71207,#71208,#71209,#71210,#71211,#71212,
#71213,#71214,#71215,#71216,#71217,#71218,#71219,#71220,#71221,#71222,#71223,
#71224,#71225,#71226,#71227,#71228,#71229,#71230,#71231,#71232,#71233,#71234,
#71235,#71236,#71237,#71238,#71239,#71240,#71241,#71242,#71243,#71244,#71245,
#71246,#71247,#71248,#71249,#71250,#71251,#71252,#71253,#71254,#71255),
 .UNSPECIFIED.,.F.,.F.,(4,2,2,2,2,2,2,2,2,2,2,2,2,2,2,2,2,2,2,2,2,2,2,2,
2,2,2,2,2,2,2,2,2,2,2,2,2,2,2,2,2,2,2,2,2,2,2,2,2,2,2,2,2,2,2,2,2,2,2,2,
2,2,2,2,2,2,2,2,2,2,2,2,2,2,2,2,2,2,2,2,2,2,2,2,2,2,2,2,2,2,2,2,2,2,2,2,
2,2,2,2,4),(-0.980716191876809,-0.978672414235096,-0.975552940822149,-0.9658198544226,
-0.947332372975558,-0.915346301054667,-0.908220296565291,-0.904188294608421,
-0.900724825447165,-0.896458506346105,-0.887925166365051,-0.867229831789358,
-0.851433104800938,-0.831211436196844,-0.827406101660201,-0.825215264582828,
-0.823214725473008,-0.820323686055612,-0.812482189011151,-0.799467606998332,
-0.759486841028773,-0.752420392631451,-0.748401240518977,-0.744937024328307,
-0.740654684353247,-0.732034741535917,-0.709515640088466,-0.681414125596727,
-0.673741943135579,-0.670792836053422,-0.668801940592265,-0.666639961731244,
-0.662968627902431,-0.645501182592887,-0.607320550303155,-0.597940841755656,
-0.593521418931444,-0.590046548917378,-0.586122134330912,-0.579318836840885,
-0.570885681008858,-0.551164226425078,-0.520884723318463,-0.516443766903541,
-0.514092675065296,-0.512131947584437,-0.50953863252289,-0.50365430091602,
-0.495080015106225,-0.46340479176953,-0.445223537395943,-0.439544557874311,
-0.435853383142865,-0.432298818044017,-0.427326658916701,-0.414336065217353,
-0.392957897996095,-0.365563030778318,-0.360817628661323,-0.358433238305253,
-0.356671732192621,-0.354231240731384,-0.349195017611983,-0.342265819072556,
-0.322135019265096,-0.292499944231819,-0.285940715682199,-0.281703032443595,
-0.278241069661093,-0.274186109587776,-0.266742437072289,-0.25724536044257,
-0.232720451109095,-0.210047820755655,-0.205170490036375,-0.202760397462087,
-0.201000066178924,-0.198586752943693,-0.19369283147691,-0.173388659758249,
-0.135538027557963,-0.128941334878982,-0.125059671368355,-0.121576885851969,
-0.121418326610126,-0.121105132131795,-0.120818138703037,-0.120549361318739,
-0.120292763115349,-0.12004352354332,-0.114702401092651,-0.10833759547208,
-0.095859929684811,-0.0672894665218258,-0.0521997457773358,-0.048558064801975,
-0.0464025343649477,-0.0443849164773167,-0.0413984264305185,-0.0379008712970157,
-0.000461226072117141),.UNSPECIFIED.);
#756=B_SPLINE_CURVE_WITH_KNOTS('',3,(#71256,#71257,#71258,#71259),
 .UNSPECIFIED.,.F.,.F.,(4,4),(-1.81279307941281,-1.81266124409322),
 .UNSPECIFIED.);
#757=B_SPLINE_CURVE_WITH_KNOTS('',3,(#71260,#71261,#71262,#71263,#71264,
#71265,#71266,#71267,#71268,#71269,#71270,#71271,#71272,#71273,#71274,#71275,
#71276,#71277,#71278,#71279,#71280,#71281,#71282,#71283,#71284,#71285,#71286,
#71287,#71288,#71289,#71290,#71291,#71292,#71293,#71294,#71295,#71296,#71297,
#71298,#71299,#71300,#71301,#71302,#71303,#71304,#71305,#71306,#71307,#71308,
#71309,#71310,#71311,#71312,#71313,#71314,#71315,#71316,#71317,#71318,#71319,
#71320,#71321,#71322,#71323,#71324,#71325,#71326,#71327,#71328,#71329,#71330,
#71331,#71332,#71333,#71334,#71335,#71336,#71337,#71338,#71339,#71340,#71341,
#71342,#71343,#71344,#71345,#71346,#71347,#71348,#71349,#71350,#71351,#71352,
#71353,#71354,#71355,#71356,#71357,#71358,#71359,#71360,#71361,#71362,#71363,
#71364,#71365,#71366,#71367,#71368,#71369,#71370,#71371,#71372,#71373,#71374,
#71375,#71376,#71377,#71378,#71379,#71380,#71381,#71382,#71383,#71384,#71385,
#71386,#71387,#71388,#71389,#71390,#71391,#71392,#71393,#71394,#71395,#71396,
#71397,#71398,#71399,#71400,#71401,#71402,#71403,#71404,#71405,#71406,#71407,
#71408,#71409,#71410,#71411,#71412,#71413,#71414,#71415,#71416,#71417,#71418,
#71419,#71420,#71421,#71422,#71423,#71424,#71425,#71426,#71427,#71428,#71429,
#71430,#71431,#71432,#71433,#71434,#71435,#71436,#71437,#71438,#71439,#71440,
#71441,#71442,#71443,#71444,#71445,#71446,#71447,#71448,#71449,#71450,#71451),
 .UNSPECIFIED.,.F.,.F.,(4,2,2,2,2,2,2,2,2,2,2,2,2,2,2,2,2,2,2,2,2,2,2,2,
2,2,2,2,2,2,2,2,2,2,2,2,2,2,2,2,2,2,2,2,2,2,2,2,2,2,2,2,2,2,2,2,2,2,2,2,
2,2,2,2,2,2,2,2,2,2,2,2,2,2,2,2,2,2,2,2,2,2,2,2,2,2,2,2,2,2,2,2,2,2,2,4),
(-0.980904423115737,-0.972309092665265,-0.967911239980157,-0.964356670061167,
-0.96023244197007,-0.952761930816234,-0.943276463222857,-0.90475584504256,
-0.893569305804469,-0.890160546322017,-0.888020726753385,-0.885894250088703,
-0.882548861917824,-0.871021927181748,-0.845746410962784,-0.820760652838631,
-0.814660219619431,-0.810817202357983,-0.807197220895649,-0.802258543788371,
-0.790053692382802,-0.770883527908946,-0.739872021250145,-0.735481255138904,
-0.733105515086185,-0.731289433760281,-0.728684994697651,-0.722959927762331,
-0.714757572972524,-0.686593909683455,-0.664982129833851,-0.658982708344533,
-0.655160576120025,-0.651530644986104,-0.646530683504691,-0.633888634654308,
-0.613587865561554,-0.584603538494515,-0.580024773159365,-0.577609051934373,
-0.575595831675303,-0.572925510782955,-0.566819246973655,-0.557846581828862,
-0.522421297807217,-0.508032661170162,-0.502665909260056,-0.499339314808945,
-0.495678356795963,-0.490499572828544,-0.476486923011896,-0.439072799233891,
-0.42696797794444,-0.423469899586423,-0.421310447275918,-0.419200546260371,
-0.41593476390406,-0.405257096551555,-0.383548484379536,-0.35632540096174,
-0.349042137014981,-0.344912979061732,-0.341357276543842,-0.336961999290346,
-0.328092887858217,-0.30640436039894,-0.279004868602742,-0.270548502866671,
-0.267450027899942,-0.265394080363657,-0.263193208916502,-0.259503681376291,
-0.242900379794272,-0.20897487711414,-0.196292724032656,-0.191152695594487,
-0.18753475804462,-0.183762378235801,-0.178007648640162,-0.15806775532313,
-0.139471274744065,-0.116531584014577,-0.112631590709609,-0.110385528703995,
-0.108328879096892,-0.105338770352972,-0.0971946734452351,-0.0803228132367113,
-0.0490461816621293,-0.0392202172345926,-0.0346546877443938,-0.0310851311254527,
-0.0277462493411522,-0.0237922304117463,-0.0153089648461796,-0.000597831378872224),
 .UNSPECIFIED.);
#758=B_SPLINE_CURVE_WITH_KNOTS('',3,(#71456,#71457,#71458,#71459,#71460,
#71461,#71462,#71463,#71464,#71465,#71466,#71467,#71468,#71469,#71470,#71471,
#71472,#71473,#71474,#71475,#71476,#71477,#71478,#71479,#71480,#71481,#71482,
#71483,#71484,#71485,#71486,#71487,#71488,#71489,#71490,#71491,#71492,#71493,
#71494,#71495,#71496,#71497,#71498,#71499,#71500,#71501,#71502,#71503,#71504,
#71505,#71506,#71507,#71508,#71509,#71510,#71511,#71512,#71513,#71514,#71515,
#71516,#71517,#71518,#71519,#71520,#71521,#71522,#71523,#71524,#71525,#71526,
#71527,#71528,#71529,#71530,#71531,#71532,#71533,#71534,#71535,#71536,#71537,
#71538,#71539,#71540,#71541,#71542,#71543,#71544,#71545,#71546,#71547,#71548,
#71549,#71550,#71551,#71552,#71553,#71554,#71555,#71556,#71557,#71558,#71559,
#71560,#71561,#71562,#71563,#71564,#71565,#71566,#71567,#71568,#71569,#71570,
#71571,#71572,#71573,#71574,#71575,#71576,#71577,#71578,#71579,#71580,#71581,
#71582,#71583,#71584,#71585,#71586,#71587,#71588,#71589,#71590,#71591,#71592,
#71593,#71594,#71595,#71596,#71597,#71598,#71599,#71600,#71601,#71602,#71603,
#71604,#71605,#71606,#71607,#71608,#71609,#71610,#71611,#71612,#71613,#71614,
#71615,#71616,#71617,#71618,#71619,#71620,#71621,#71622,#71623,#71624,#71625,
#71626,#71627,#71628,#71629,#71630,#71631,#71632,#71633,#71634,#71635,#71636,
#71637,#71638,#71639,#71640,#71641,#71642,#71643,#71644,#71645,#71646,#71647,
#71648,#71649),.UNSPECIFIED.,.F.,.F.,(4,2,2,2,2,2,2,2,2,2,2,2,2,2,2,2,2,
2,2,2,2,2,2,2,2,2,2,2,2,2,2,2,2,2,2,2,2,2,2,2,2,2,2,2,2,2,2,2,2,2,2,2,2,
2,2,2,2,2,2,2,2,2,2,2,2,2,2,2,2,2,2,2,2,2,2,2,2,2,2,2,2,2,2,2,2,2,2,2,2,
2,2,2,2,2,2,2,4),(-1.96077830518356,-1.92303894553549,-1.9195585575685,
-1.91658380744085,-1.9145687419356,-1.91240997604103,-1.90875175203967,
-1.89321851940835,-1.86415749453336,-1.8522439460463,-1.84606658036546,
-1.84085238143544,-1.84059957515371,-1.8403367951535,-1.836767361395,-1.83353101195692,
-1.82916628937187,-1.81800094255874,-1.78514103559423,-1.76697589556691,
-1.76231414430016,-1.75994658742278,-1.75798800408095,-1.75546118351887,
-1.74980269346822,-1.71982555162952,-1.69641729695568,-1.68769612473125,
-1.683395728164,-1.6799311672285,-1.67592743936131,-1.66893016253422,-1.63503008075999,
-1.61774316276034,-1.60838458051561,-1.60530687648307,-1.60327189209518,
-1.6014080574858,-1.5981679426452,-1.58817764278762,-1.56193844426803,-1.54462594126031,
-1.53323266176232,-1.52848627646465,-1.52496963953694,-1.52120487833068,
-1.51516720654675,-1.48955336042955,-1.46455211737487,-1.45681757544216,
-1.4513574615147,-1.44883891487086,-1.44688311432965,-1.4444736878445,-1.4395981081522,
-1.41745863509723,-1.39735585152558,-1.3852885529307,-1.37640520956997,
-1.37207497037054,-1.36860820717853,-1.36462587699,-1.3577284847528,-1.31693071867146,
-1.30423768142103,-1.29652465936375,-1.29365133925854,-1.2916540969872,
-1.28945666156045,-1.28561942663399,-1.2627869355318,-1.24465266536888,
-1.23088331404665,-1.22112532142519,-1.21664059111359,-1.21315904218343,
-1.20927314628933,-1.20265510938848,-1.16487163089148,-1.14451539340036,
-1.13961622560703,-1.13720201432049,-1.13544178047744,-1.13303291572945,
-1.1281614471451,-1.1065266821292,-1.08766959324548,-1.06813449892399,-1.06249601517894,
-1.05881313566057,-1.05529383379258,-1.05032143653054,-1.03824005750755,
-0.999864443733036,-0.986286956218584,-0.982831507346819,-0.980716191876809),
 .UNSPECIFIED.);
#759=B_SPLINE_CURVE_WITH_KNOTS('',3,(#71651,#71652,#71653,#71654),
 .UNSPECIFIED.,.F.,.F.,(4,4),(-0.000597831378872224,-0.000459283554306568),
 .UNSPECIFIED.);
#760=B_SPLINE_CURVE_WITH_KNOTS('',3,(#71655,#71656,#71657,#71658,#71659,
#71660,#71661,#71662,#71663,#71664,#71665,#71666,#71667,#71668,#71669,#71670,
#71671,#71672,#71673,#71674,#71675,#71676,#71677,#71678,#71679,#71680,#71681,
#71682,#71683,#71684,#71685,#71686,#71687,#71688,#71689,#71690,#71691,#71692,
#71693,#71694,#71695,#71696,#71697,#71698,#71699,#71700,#71701,#71702,#71703,
#71704,#71705,#71706,#71707,#71708,#71709,#71710,#71711,#71712,#71713,#71714,
#71715,#71716,#71717,#71718,#71719,#71720,#71721,#71722,#71723,#71724,#71725,
#71726,#71727,#71728,#71729,#71730,#71731,#71732,#71733,#71734,#71735,#71736,
#71737,#71738,#71739,#71740,#71741,#71742,#71743,#71744,#71745,#71746,#71747,
#71748,#71749,#71750,#71751,#71752,#71753,#71754,#71755,#71756,#71757,#71758,
#71759,#71760,#71761,#71762,#71763,#71764,#71765,#71766,#71767,#71768,#71769,
#71770,#71771,#71772,#71773,#71774,#71775,#71776,#71777,#71778,#71779,#71780,
#71781,#71782,#71783,#71784,#71785,#71786,#71787,#71788,#71789,#71790,#71791,
#71792,#71793,#71794,#71795,#71796,#71797,#71798,#71799,#71800,#71801,#71802,
#71803,#71804,#71805,#71806,#71807,#71808,#71809,#71810,#71811,#71812,#71813,
#71814,#71815,#71816,#71817,#71818,#71819,#71820,#71821,#71822,#71823,#71824,
#71825,#71826,#71827,#71828,#71829,#71830,#71831,#71832,#71833,#71834,#71835,
#71836,#71837,#71838,#71839,#71840,#71841,#71842),.UNSPECIFIED.,.F.,.F.,
(4,2,2,2,2,2,2,2,2,2,2,2,2,2,2,2,2,2,2,2,2,2,2,2,2,2,2,2,2,2,2,2,2,2,2,
2,2,2,2,2,2,2,2,2,2,2,2,2,2,2,2,2,2,2,2,2,2,2,2,2,2,2,2,2,2,2,2,2,2,2,2,
2,2,2,2,2,2,2,2,2,2,2,2,2,2,2,2,2,2,2,2,2,2,4),(-1.96074712009502,-1.92330424369733,
-1.91964900608186,-1.9165439369243,-1.91446667464182,-1.91226232233701,
-1.90855451791569,-1.89319835882291,-1.86270909330847,-1.85157888718564,
-1.84325044659449,-1.83909365930445,-1.83553748075556,-1.83143088685372,
-1.82424920041514,-1.79201810489301,-1.7660358722662,-1.76192199699911,
-1.75963086648069,-1.75759221883059,-1.75470944996851,-1.74774631995332,
-1.71913240192821,-1.70099305695676,-1.692916777697,-1.68630278654894,-1.68235370328846,
-1.67877137455857,-1.67416767598951,-1.66381511017221,-1.62321974667725,
-1.61385009927947,-1.60755407687908,-1.60485220579725,-1.60283635909023,
-1.60044296819685,-1.59596875323513,-1.56575238006591,-1.54618049028869,
-1.53381754508987,-1.52885686033675,-1.52523362303198,-1.5213988312098,
-1.51533697940125,-1.49203488962347,-1.45787684641395,-1.45184851036184,
-1.44919146734801,-1.44717937984815,-1.44475410711998,-1.44012978729441,
-1.40504022982573,-1.38246919686681,-1.37544078819509,-1.37140591104813,
-1.36784042477756,-1.36331120523256,-1.35369281373714,-1.31590449233759,
-1.30413128628005,-1.29905106068833,-1.29504853712373,-1.29278070371425,
-1.2907332666829,-1.28779703409595,-1.28047076918301,-1.2521577912366,-1.23412924260284,
-1.22238684520311,-1.2175154038011,-1.21390593321297,-1.21003814889031,
-1.20381827504736,-1.17635519627127,-1.1531758249164,-1.14568426713791,
-1.14032563253653,-1.13778740111077,-1.13578019987408,-1.13325293777625,
-1.12795342809861,-1.09766149812672,-1.07893185758297,-1.07070186369002,
-1.06399169130368,-1.06002215112043,-1.05644384244576,-1.05187637399718,
-1.04174797824096,-1.00458373023303,-0.992891559070608,-0.985555656151887,
-0.982692227419022,-0.98065608999199),.UNSPECIFIED.);
#761=B_SPLINE_CURVE_WITH_KNOTS('',3,(#71847,#71848,#71849,#71850,#71851,
#71852,#71853,#71854,#71855,#71856,#71857,#71858,#71859,#71860,#71861,#71862,
#71863,#71864,#71865,#71866,#71867,#71868,#71869,#71870,#71871,#71872,#71873,
#71874,#71875,#71876,#71877,#71878,#71879,#71880,#71881,#71882,#71883,#71884,
#71885,#71886,#71887,#71888,#71889,#71890,#71891,#71892,#71893,#71894,#71895,
#71896,#71897,#71898,#71899,#71900,#71901,#71902,#71903,#71904,#71905,#71906,
#71907,#71908,#71909,#71910,#71911,#71912,#71913,#71914,#71915,#71916,#71917,
#71918,#71919,#71920,#71921,#71922,#71923,#71924,#71925,#71926,#71927,#71928,
#71929,#71930,#71931,#71932,#71933,#71934,#71935,#71936,#71937,#71938,#71939,
#71940,#71941,#71942,#71943,#71944,#71945,#71946,#71947,#71948,#71949,#71950,
#71951,#71952,#71953,#71954,#71955,#71956,#71957,#71958,#71959,#71960,#71961,
#71962,#71963,#71964,#71965,#71966,#71967,#71968,#71969,#71970,#71971,#71972,
#71973,#71974,#71975,#71976,#71977,#71978,#71979,#71980,#71981,#71982,#71983,
#71984,#71985,#71986,#71987,#71988,#71989,#71990,#71991,#71992,#71993,#71994,
#71995,#71996,#71997,#71998,#71999,#72000,#72001,#72002,#72003,#72004,#72005,
#72006,#72007,#72008,#72009,#72010,#72011,#72012,#72013,#72014,#72015,#72016,
#72017,#72018,#72019,#72020,#72021),.UNSPECIFIED.,.F.,.F.,(4,3,3,3,3,3,
3,3,3,3,3,3,3,3,3,3,3,3,3,3,3,3,3,3,3,3,3,3,3,3,3,3,3,3,3,3,3,3,3,3,3,3,
3,3,3,3,3,3,3,3,3,3,3,3,3,3,3,3,4),(34.5575191894876,34.6681294449895,34.7786939471955,
34.8892566164147,34.9999369681898,35.1106862346866,35.2216338987612,35.2605512351816,
35.37223736211,35.4837245346131,35.59510057765,35.7064084453262,35.8176909943029,
35.9290742355253,36.0405033729067,36.1521504834875,36.2586980615683,36.370384188506,
36.4818713610179,36.5932474040636,36.7045552717483,36.8158378207331,36.9272210619631,
37.0386501993518,37.1502973099394,37.2568448879551,37.3685310149238,37.4800181874678,
37.591394230546,37.7027020982637,37.8139846472819,37.9253678885457,38.0367970259687,
38.1484441365904,38.2549917143418,38.3666778412903,38.4781650138137,38.5895410568709,
38.7008489245676,38.8121314735645,38.923514714807,39.0349438522084,39.1465909628088,
39.2531385407286,39.3648246676801,39.4763118402064,39.5876878832665,39.6989957509661,
39.810278299966,39.9216615412113,40.0330906786155,40.1447377892186,40.2512853671153,
40.3649135742225,40.4838613048337,40.5970963231696,40.7102234970804,40.8232764462415,
40.8407044966673),.UNSPECIFIED.);
#762=B_SPLINE_CURVE_WITH_KNOTS('',3,(#72023,#72024,#72025,#72026,#72027,
#72028,#72029,#72030,#72031,#72032,#72033,#72034,#72035,#72036,#72037,#72038,
#72039,#72040,#72041,#72042,#72043,#72044,#72045,#72046,#72047,#72048,#72049,
#72050,#72051,#72052,#72053,#72054,#72055,#72056,#72057,#72058,#72059,#72060,
#72061,#72062,#72063,#72064,#72065,#72066,#72067,#72068,#72069,#72070,#72071,
#72072,#72073,#72074,#72075,#72076,#72077,#72078,#72079,#72080,#72081,#72082,
#72083,#72084,#72085,#72086,#72087,#72088,#72089,#72090,#72091,#72092,#72093,
#72094,#72095,#72096,#72097,#72098,#72099,#72100,#72101,#72102,#72103,#72104,
#72105,#72106,#72107,#72108,#72109,#72110,#72111,#72112,#72113,#72114,#72115,
#72116,#72117,#72118,#72119,#72120,#72121,#72122,#72123,#72124,#72125,#72126,
#72127,#72128,#72129,#72130,#72131,#72132,#72133,#72134,#72135,#72136,#72137,
#72138,#72139,#72140,#72141,#72142,#72143,#72144,#72145,#72146,#72147,#72148,
#72149,#72150,#72151,#72152,#72153,#72154,#72155,#72156,#72157,#72158,#72159,
#72160,#72161,#72162,#72163,#72164,#72165,#72166,#72167,#72168,#72169,#72170,
#72171,#72172,#72173,#72174,#72175,#72176,#72177,#72178,#72179,#72180,#72181,
#72182,#72183,#72184,#72185,#72186,#72187,#72188,#72189,#72190,#72191,#72192,
#72193,#72194,#72195,#72196,#72197,#72198,#72199,#72200,#72201,#72202,#72203,
#72204,#72205,#72206,#72207,#72208,#72209,#72210),.UNSPECIFIED.,.F.,.F.,
(4,2,2,2,2,2,2,2,2,2,2,2,2,2,2,2,2,2,2,2,2,2,2,2,2,2,2,2,2,2,2,2,2,2,2,
2,2,2,2,2,2,2,2,2,2,2,2,2,2,2,2,2,2,2,2,2,2,2,2,2,2,2,2,2,2,2,2,2,2,2,2,
2,2,2,2,2,2,2,2,2,2,2,2,2,2,2,2,2,2,2,2,2,2,4),(-0.98065608999199,-0.978354702906265,
-0.974193919631416,-0.949387547585181,-0.915908231415091,-0.908821162648226,
-0.904734130968147,-0.901174921302342,-0.896723296316679,-0.887544075129815,
-0.874989860281017,-0.855663936812527,-0.833802167380706,-0.828878787362181,
-0.826423081130071,-0.82461481632714,-0.822109099220653,-0.816924570097771,
-0.809762571184661,-0.788538410753232,-0.76067583807875,-0.75339538298205,
-0.74926700149047,-0.745711510526034,-0.741315910330264,-0.732444019185328,
-0.710902281581362,-0.683737513180867,-0.674991815107569,-0.671854897333428,
-0.669977362296841,-0.667842635552226,-0.664459261541117,-0.652499968117858,
-0.625142869306548,-0.602615314358564,-0.596577586739665,-0.592747420525063,
-0.589121192518809,-0.584144603645494,-0.571672275053566,-0.551817993592194,
-0.522063864325581,-0.517540737473104,-0.51513669383677,-0.513121874948797,
-0.510434546710223,-0.504227734429962,-0.49504679898894,-0.457076872418203,
-0.444858001434442,-0.439797534295136,-0.436193291229638,-0.432398455631287,
-0.426533013505774,-0.40497061089671,-0.396478025091819,-0.366393612079883,
-0.361901695905956,-0.359504295286125,-0.357488593866831,-0.354791605270093,
-0.348526688220211,-0.339224200642259,-0.299582270111105,-0.28869705123921,
-0.284334487053402,-0.2807101963141,-0.276947551747818,-0.271240817672782,
-0.251930638356581,-0.222204132934795,-0.209058317342049,-0.20547891517917,
-0.20330189090496,-0.201205602423778,-0.198006186347572,-0.187976053693093,
-0.168623959617772,-0.138280502160977,-0.130982680625002,-0.126850506466004,
-0.123295148575431,-0.119161910226838,-0.110979038605763,-0.100108977707732,
-0.0691474134185848,-0.0537121579076861,-0.0499997589962834,-0.0477939540241356,
-0.0457163929279189,-0.0426124913361034,-0.0389597549555495,-0.000459537643221521),
 .UNSPECIFIED.);
#763=B_SPLINE_CURVE_WITH_KNOTS('',3,(#72211,#72212,#72213,#72214),
 .UNSPECIFIED.,.F.,.F.,(4,4),(-1.96107617980448,-1.96094824870565),
 .UNSPECIFIED.);
#764=B_SPLINE_CURVE_WITH_KNOTS('',3,(#72219,#72220,#72221,#72222,#72223,
#72224,#72225,#72226,#72227,#72228,#72229,#72230,#72231,#72232,#72233,#72234,
#72235,#72236,#72237,#72238,#72239,#72240,#72241,#72242,#72243,#72244,#72245,
#72246,#72247,#72248,#72249,#72250,#72251,#72252,#72253,#72254,#72255,#72256,
#72257,#72258,#72259,#72260,#72261,#72262,#72263,#72264,#72265,#72266,#72267,
#72268,#72269,#72270,#72271,#72272,#72273,#72274,#72275,#72276,#72277,#72278,
#72279,#72280,#72281,#72282,#72283,#72284,#72285,#72286,#72287,#72288,#72289,
#72290,#72291,#72292,#72293,#72294,#72295,#72296,#72297,#72298,#72299,#72300,
#72301,#72302,#72303,#72304,#72305,#72306,#72307,#72308,#72309,#72310,#72311,
#72312,#72313,#72314,#72315,#72316,#72317,#72318,#72319,#72320,#72321,#72322,
#72323,#72324,#72325,#72326,#72327,#72328,#72329,#72330,#72331,#72332,#72333,
#72334,#72335,#72336,#72337,#72338,#72339,#72340,#72341,#72342,#72343,#72344,
#72345,#72346,#72347,#72348,#72349,#72350,#72351,#72352,#72353,#72354,#72355,
#72356,#72357,#72358,#72359,#72360,#72361,#72362,#72363,#72364,#72365,#72366,
#72367,#72368,#72369,#72370,#72371,#72372,#72373,#72374,#72375,#72376,#72377,
#72378,#72379,#72380,#72381,#72382,#72383,#72384,#72385,#72386,#72387,#72388,
#72389,#72390,#72391,#72392,#72393,#72394,#72395,#72396,#72397,#72398,#72399,
#72400),.UNSPECIFIED.,.F.,.F.,(4,2,2,2,2,2,2,2,2,2,2,2,2,2,2,2,2,2,2,2,
2,2,2,2,2,2,2,2,2,2,2,2,2,2,2,2,2,2,2,2,2,2,2,2,2,2,2,2,2,2,2,2,2,2,2,2,
2,2,2,2,2,2,2,2,2,2,2,2,2,2,2,2,2,2,2,2,2,2,2,2,2,2,2,2,2,2,2,2,2,2,4),
(-0.980843112000428,-0.951920574072764,-0.93097803249815,-0.925099911148539,
-0.921367497327225,-0.91783491128297,-0.912993712403994,-0.900959549939245,
-0.882102504874166,-0.851692751608264,-0.846500859890778,-0.843996323995269,
-0.842040399321844,-0.839617112311938,-0.834672024400599,-0.82791130780217,
-0.808676648352998,-0.777776377591259,-0.770611187344655,-0.766570667561399,
-0.763107510018653,-0.758851260513236,-0.750372561968623,-0.7311477990017,
-0.698670106784975,-0.691619400082618,-0.688768213516583,-0.686774255122743,
-0.684566624811173,-0.680683350602813,-0.654745732793106,-0.621847824984893,
-0.614772571925623,-0.610751308994798,-0.607286912467112,-0.603006452561707,
-0.594397921901346,-0.572089128443636,-0.544372433545687,-0.536220949894704,
-0.533208722537171,-0.531206090741462,-0.529065140719352,-0.525491672187407,
-0.510019644546239,-0.490440197595961,-0.464169367786274,-0.458064434101782,
-0.454284899439612,-0.450772458330907,-0.446059429260661,-0.434893145343032,
-0.418105823058623,-0.40231999448564,-0.382063445330295,-0.378257749039759,
-0.376066771552237,-0.374066157652966,-0.371175085181421,-0.363333968365896,
-0.350320666080443,-0.31033364904223,-0.303267813120982,-0.299248678097146,
-0.295784288883258,-0.29150149383613,-0.282879758802574,-0.26033630380799,
-0.232190580316864,-0.224570131660876,-0.221628142527779,-0.219638453710298,
-0.2174737853687,-0.213790256587188,-0.196037542778051,-0.15627237749183,
-0.148909068258633,-0.144442515297959,-0.140962687612453,-0.137065955198825,
-0.130396844528511,-0.122181170805865,-0.1033298746528,-0.0729347737568217,
-0.0677325559330417,-0.0652261680387528,-0.0632703974100668,-0.060849291775129,
-0.0559147129440345,-0.0352129286778182,-0.000461241006961862),
 .UNSPECIFIED.);
#765=B_SPLINE_CURVE_WITH_KNOTS('',3,(#72401,#72402,#72403,#72404,#72405,
#72406,#72407,#72408,#72409,#72410,#72411,#72412,#72413,#72414,#72415,#72416,
#72417,#72418,#72419,#72420,#72421,#72422,#72423,#72424,#72425,#72426,#72427,
#72428,#72429,#72430,#72431,#72432,#72433,#72434,#72435,#72436,#72437,#72438,
#72439,#72440,#72441,#72442,#72443,#72444,#72445,#72446,#72447,#72448,#72449,
#72450,#72451,#72452,#72453,#72454,#72455,#72456,#72457,#72458,#72459,#72460,
#72461,#72462,#72463,#72464,#72465,#72466,#72467,#72468,#72469,#72470,#72471,
#72472,#72473,#72474,#72475,#72476,#72477,#72478,#72479,#72480,#72481,#72482,
#72483,#72484,#72485,#72486,#72487,#72488,#72489,#72490,#72491,#72492,#72493,
#72494,#72495,#72496,#72497,#72498,#72499,#72500,#72501,#72502,#72503,#72504,
#72505,#72506,#72507,#72508,#72509,#72510,#72511,#72512,#72513,#72514,#72515,
#72516,#72517,#72518,#72519,#72520,#72521,#72522,#72523,#72524,#72525,#72526,
#72527,#72528,#72529,#72530,#72531,#72532,#72533,#72534,#72535,#72536,#72537,
#72538,#72539,#72540,#72541,#72542,#72543,#72544,#72545,#72546,#72547,#72548,
#72549,#72550,#72551,#72552,#72553,#72554,#72555,#72556,#72557,#72558,#72559,
#72560,#72561,#72562,#72563,#72564,#72565,#72566,#72567,#72568,#72569,#72570,
#72571,#72572,#72573,#72574,#72575,#72576,#72577,#72578,#72579,#72580,#72581,
#72582,#72583,#72584,#72585,#72586,#72587,#72588,#72589,#72590,#72591,#72592,
#72593,#72594,#72595,#72596),.UNSPECIFIED.,.F.,.F.,(4,2,2,2,2,2,2,2,2,2,
2,2,2,2,2,2,2,2,2,2,2,2,2,2,2,2,2,2,2,2,2,2,2,2,2,2,2,2,2,2,2,2,2,2,2,2,
2,2,2,2,2,2,2,2,2,2,2,2,2,2,2,2,2,2,2,2,2,2,2,2,2,2,2,2,2,2,2,2,2,2,2,2,
2,2,2,2,2,2,2,2,2,2,2,2,2,2,2,4),(-1.96094824870565,-1.94267634822966,-1.93757453855741,
-1.93389463107528,-1.93055551091535,-1.9269214938182,-1.92251663056985,
-1.91154006639502,-1.87350459780632,-1.85864331623043,-1.85496703801708,
-1.85276935269738,-1.85071229151882,-1.84760615733215,-1.83908925293603,
-1.81176687156231,-1.79012862831546,-1.78126315531497,-1.77686916771891,
-1.77331423489394,-1.76918566440406,-1.76190268610234,-1.7343598368956,
-1.71287409363393,-1.70566593266085,-1.70045741216294,-1.69794737952514,
-1.69613912756977,-1.69368799836249,-1.6887871031636,-1.66477914100608,
-1.64186978462822,-1.62779393690583,-1.62260782452132,-1.61894576998243,
-1.61562084588853,-1.6111258986462,-1.59938454147771,-1.56082000852686,
-1.55159161358485,-1.54536280668352,-1.54267198467194,-1.54065707216635,
-1.53825592832371,-1.53374570314146,-1.50389074900865,-1.48411910081444,
-1.47167854009571,-1.46670677666156,-1.46308157573251,-1.45925023965997,
-1.45320583801524,-1.43049911488401,-1.40327188396087,-1.39133703508837,
-1.38795574999922,-1.38582158762654,-1.38394390962964,-1.38080570146556,
-1.37204859339793,-1.34491635319189,-1.32339648253723,-1.31452753071019,
-1.31013264948267,-1.30657736343626,-1.3024487962458,-1.29516694059518,
-1.26727687454462,-1.2460478462039,-1.23888422228237,-1.23369935126642,
-1.23119363198083,-1.22938545045483,-1.22692995124973,-1.22200731257903,
-1.20005947164307,-1.18040185363748,-1.16810231749209,-1.15905619361396,
-1.15462879402588,-1.15107139437516,-1.14696713959246,-1.13979947207659,
-1.10741709051519,-1.08935693558775,-1.07971427928637,-1.07655697035418,
-1.07446917337377,-1.07255135964997,-1.06919749202155,-1.05860448862994,
-1.03288755325588,-1.00939408982909,-1.00224172321199,-0.998181261802422,
-0.994619040136678,-0.990128788067818,-0.980733160320695),.UNSPECIFIED.);
#766=B_SPLINE_CURVE_WITH_KNOTS('',3,(#72602,#72603,#72604,#72605),
 .UNSPECIFIED.,.F.,.F.,(4,4),(-0.00059011187237714,-0.000461155693138806),
 .UNSPECIFIED.);
#767=B_SPLINE_CURVE_WITH_KNOTS('',3,(#72606,#72607,#72608,#72609,#72610,
#72611,#72612,#72613,#72614,#72615,#72616,#72617,#72618,#72619,#72620,#72621,
#72622,#72623,#72624,#72625,#72626,#72627,#72628,#72629,#72630,#72631,#72632,
#72633,#72634,#72635,#72636,#72637,#72638,#72639,#72640,#72641,#72642,#72643,
#72644,#72645,#72646,#72647,#72648,#72649,#72650,#72651,#72652,#72653,#72654,
#72655,#72656,#72657,#72658,#72659,#72660,#72661,#72662,#72663,#72664,#72665,
#72666,#72667,#72668,#72669,#72670,#72671,#72672,#72673,#72674,#72675,#72676,
#72677,#72678,#72679,#72680,#72681,#72682,#72683,#72684,#72685,#72686,#72687,
#72688,#72689,#72690,#72691,#72692,#72693,#72694,#72695,#72696,#72697,#72698,
#72699,#72700,#72701,#72702,#72703,#72704,#72705,#72706,#72707,#72708,#72709,
#72710,#72711,#72712,#72713,#72714,#72715,#72716,#72717,#72718,#72719,#72720,
#72721,#72722,#72723,#72724,#72725,#72726,#72727,#72728,#72729,#72730,#72731,
#72732,#72733,#72734,#72735,#72736,#72737,#72738,#72739,#72740,#72741,#72742,
#72743,#72744,#72745,#72746,#72747,#72748,#72749,#72750,#72751,#72752,#72753,
#72754,#72755,#72756,#72757,#72758,#72759,#72760,#72761,#72762,#72763,#72764,
#72765,#72766,#72767,#72768,#72769,#72770,#72771,#72772,#72773,#72774,#72775,
#72776,#72777,#72778,#72779,#72780,#72781,#72782,#72783,#72784,#72785,#72786,
#72787,#72788,#72789,#72790,#72791,#72792,#72793,#72794,#72795,#72796,#72797,
#72798,#72799,#72800,#72801),.UNSPECIFIED.,.F.,.F.,(4,2,2,2,2,2,2,2,2,2,
2,2,2,2,2,2,2,2,2,2,2,2,2,2,2,2,2,2,2,2,2,2,2,2,2,2,2,2,2,2,2,2,2,2,2,2,
2,2,2,2,2,2,2,2,2,2,2,2,2,2,2,2,2,2,2,2,2,2,2,2,2,2,2,2,2,2,2,2,2,2,2,2,
2,2,2,2,2,2,2,2,2,2,2,2,2,2,2,4),(-1.96127857229901,-1.93985522552035,-1.93700892692586,
-1.93497772268674,-1.93297545631679,-1.9307879581078,-1.92699884857685,
-1.90790234968511,-1.87940921983079,-1.87195841343185,-1.86239540273868,
-1.85790757498593,-1.85442493793339,-1.85053917484657,-1.84392478290888,
-1.80609446922914,-1.78575694549569,-1.78085901044206,-1.77844467143018,
-1.77668401697316,-1.77427409324974,-1.76939903078909,-1.74652197923517,
-1.72215977722551,-1.71269518625917,-1.70526957307602,-1.70121772876528,
-1.69775484887694,-1.69351154078721,-1.68693455370028,-1.65825100925579,
-1.63739223770426,-1.62698053371964,-1.6237901417199,-1.62173153125583,
-1.61963407206586,-1.61626223470719,-1.60492755997675,-1.57965943749913,
-1.55876354021825,-1.55022265238004,-1.54595450920383,-1.54249039986191,
-1.53845859622391,-1.5313355561556,-1.49920527951765,-1.48078140345377,
-1.47106678260229,-1.46794885087909,-1.46590515583363,-1.46404846154953,
-1.46084862882604,-1.45121968388429,-1.42140637127894,-1.40285859854245,
-1.39440415322682,-1.39015220588884,-1.38668890395976,-1.38264408512937,
-1.37546006126579,-1.34522146269267,-1.32548750285831,-1.31863081097612,
-1.31363393132335,-1.31120058178205,-1.30943908130048,-1.30704709829179,
-1.30226459374186,-1.26775643081585,-1.24719481008332,-1.23866762891304,
-1.23440207498481,-1.23093813475068,-1.22690435255795,-1.21977193102939,
-1.18784730529338,-1.16928634353494,-1.15953032900894,-1.15640795109055,
-1.15436336841416,-1.15224834363795,-1.14879534229973,-1.1366500323816,
-1.09134295434657,-1.08283722572539,-1.07857598041775,-1.07511261894959,
-1.07107621795231,-1.06393023611763,-1.03236525183324,-1.01356487762936,
-1.00373761011916,-1.00060782109162,-0.998561885635286,-0.996449192684477,
-0.993006259241398,-0.980949239411572,-0.980843112000428),.UNSPECIFIED.);
#768=B_SPLINE_CURVE_WITH_KNOTS('',3,(#72802,#72803,#72804,#72805,#72806,
#72807,#72808,#72809,#72810,#72811,#72812,#72813,#72814,#72815,#72816,#72817,
#72818,#72819,#72820,#72821,#72822,#72823,#72824,#72825,#72826,#72827,#72828,
#72829,#72830,#72831,#72832,#72833,#72834,#72835,#72836,#72837,#72838,#72839,
#72840,#72841,#72842,#72843,#72844,#72845,#72846,#72847,#72848,#72849,#72850,
#72851,#72852,#72853,#72854,#72855,#72856,#72857,#72858,#72859,#72860,#72861,
#72862,#72863,#72864,#72865,#72866,#72867,#72868,#72869,#72870,#72871,#72872,
#72873,#72874,#72875,#72876,#72877,#72878,#72879,#72880,#72881,#72882,#72883,
#72884,#72885,#72886,#72887,#72888,#72889,#72890,#72891,#72892,#72893,#72894,
#72895,#72896,#72897,#72898,#72899,#72900,#72901,#72902,#72903,#72904,#72905,
#72906,#72907,#72908,#72909,#72910,#72911,#72912,#72913,#72914,#72915,#72916,
#72917,#72918,#72919,#72920,#72921,#72922,#72923,#72924,#72925,#72926,#72927,
#72928,#72929,#72930,#72931,#72932,#72933,#72934,#72935,#72936,#72937,#72938,
#72939,#72940,#72941,#72942,#72943,#72944,#72945,#72946,#72947,#72948,#72949,
#72950,#72951,#72952,#72953,#72954,#72955,#72956,#72957,#72958,#72959,#72960,
#72961,#72962,#72963,#72964,#72965,#72966,#72967,#72968,#72969,#72970,#72971,
#72972,#72973,#72974,#72975,#72976,#72977,#72978,#72979,#72980,#72981,#72982,
#72983,#72984,#72985,#72986,#72987),.UNSPECIFIED.,.F.,.F.,(4,2,2,2,2,2,
2,2,2,2,2,2,2,2,2,2,2,2,2,2,2,2,2,2,2,2,2,2,2,2,2,2,2,2,2,2,2,2,2,2,2,2,
2,2,2,2,2,2,2,2,2,2,2,2,2,2,2,2,2,2,2,2,2,2,2,2,2,2,2,2,2,2,2,2,2,2,2,2,
2,2,2,2,2,2,2,2,2,2,2,2,2,2,4),(-0.980733160320695,-0.967761504262221,-0.948816939040578,
-0.925615934930639,-0.921704656449749,-0.919456247566718,-0.917400783658444,
-0.914417073381265,-0.906210218868975,-0.892340202238349,-0.857447780109865,
-0.84805983114872,-0.84357098931083,-0.84000888947004,-0.83594749315517,
-0.828790636149438,-0.805263320242643,-0.779487937654314,-0.768944693925615,
-0.765595495593097,-0.763678570539921,-0.761589899403417,-0.758428350507042,
-0.748746862897344,-0.730560785329596,-0.69840951887371,-0.691231455176459,
-0.68712493722333,-0.683567663126316,-0.679143139684937,-0.670113361242895,
-0.657843241635455,-0.638007028562777,-0.616141147498622,-0.611217759662292,
-0.608762059977652,-0.606953805240607,-0.604448108809262,-0.599263646035777,
-0.592101757689801,-0.570878122232942,-0.543015147146856,-0.535734734621049,
-0.531606375940406,-0.528050903872007,-0.523655326072108,-0.514783476570161,
-0.493242124790231,-0.466077933963418,-0.457331743442727,-0.454194771661292,
-0.452317234082736,-0.450182537319255,-0.446799267891242,-0.434841052809533,
-0.407489250081597,-0.384955897295301,-0.378917993806803,-0.375087805123129,
-0.371461617414524,-0.366485182889639,-0.354013835852142,-0.334162041423826,
-0.304403816341197,-0.299881093357489,-0.297477143201675,-0.295462324625449,
-0.292774894446566,-0.286567418615831,-0.277385079455814,-0.239396270312896,
-0.227191933947655,-0.222134383304945,-0.218530646968789,-0.214734972591239,
-0.208865350260263,-0.187235817964272,-0.178898893781169,-0.148678529994814,
-0.144220005801542,-0.141829740753544,-0.139813034845904,-0.137105467137435,
-0.130776404475948,-0.121338809078955,-0.079629984705879,-0.070119736786701,
-0.0656092752384031,-0.0620452669038608,-0.0579979519653199,-0.050910013176525,
-0.0279014211884546,-0.000459681452164959),.UNSPECIFIED.);
#769=B_SPLINE_CURVE_WITH_KNOTS('',3,(#72992,#72993,#72994,#72995,#72996,
#72997,#72998,#72999,#73000,#73001,#73002,#73003,#73004,#73005,#73006,#73007,
#73008,#73009,#73010,#73011,#73012,#73013,#73014,#73015,#73016,#73017,#73018,
#73019,#73020,#73021,#73022,#73023,#73024,#73025,#73026,#73027,#73028,#73029,
#73030,#73031,#73032,#73033,#73034,#73035,#73036,#73037,#73038,#73039,#73040,
#73041,#73042,#73043,#73044,#73045,#73046,#73047,#73048,#73049,#73050,#73051,
#73052,#73053,#73054,#73055,#73056,#73057,#73058,#73059,#73060,#73061,#73062,
#73063,#73064,#73065,#73066,#73067,#73068,#73069,#73070,#73071,#73072,#73073,
#73074,#73075,#73076,#73077,#73078,#73079,#73080,#73081,#73082,#73083,#73084,
#73085,#73086,#73087,#73088,#73089,#73090,#73091,#73092,#73093,#73094,#73095,
#73096,#73097,#73098,#73099,#73100,#73101,#73102,#73103,#73104,#73105,#73106,
#73107,#73108,#73109,#73110,#73111,#73112,#73113,#73114,#73115,#73116,#73117,
#73118,#73119,#73120,#73121,#73122,#73123,#73124,#73125,#73126,#73127,#73128,
#73129,#73130,#73131,#73132,#73133,#73134,#73135,#73136,#73137,#73138,#73139,
#73140,#73141,#73142,#73143,#73144,#73145,#73146,#73147,#73148,#73149,#73150,
#73151,#73152,#73153,#73154,#73155,#73156,#73157,#73158,#73159,#73160,#73161,
#73162,#73163,#73164,#73165,#73166,#73167,#73168,#73169,#73170,#73171,#73172,
#73173,#73174,#73175,#73176,#73177,#73178,#73179,#73180,#73181,#73182,#73183,
#73184,#73185,#73186,#73187,#73188,#73189,#73190,#73191,#73192,#73193),
 .UNSPECIFIED.,.F.,.F.,(4,2,2,2,2,2,2,2,2,2,2,2,2,2,2,2,2,2,2,2,2,2,2,2,
2,2,2,2,2,2,2,2,2,2,2,2,2,2,2,2,2,2,2,2,2,2,2,2,2,2,2,2,2,2,2,2,2,2,2,2,
2,2,2,2,2,2,2,2,2,2,2,2,2,2,2,2,2,2,2,2,2,2,2,2,2,2,2,2,2,2,2,2,2,2,2,2,
2,2,2,2,4),(-0.980958235625572,-0.975406899605016,-0.956980154301351,-0.937231546846887,
-0.915150637366387,-0.910272526204308,-0.907862091967822,-0.906101545886403,
-0.903687986300938,-0.898793683562232,-0.878489188932872,-0.840649420634971,
-0.834041349898184,-0.830157017775664,-0.82667426539394,-0.822184329765441,
-0.812399541060252,-0.79857560561528,-0.780471253032548,-0.757646123466051,
-0.753808693670861,-0.751610917625146,-0.749613154731316,-0.746738837912992,
-0.739021188337069,-0.726319242544386,-0.685568997510446,-0.678664072793847,
-0.67467954056057,-0.67121208938256,-0.666882607455337,-0.658007148872636,
-0.645954181051805,-0.625705485140268,-0.603629163034814,-0.598751555046212,
-0.596341365080416,-0.594580995264852,-0.592167674597972,-0.587273847306234,
-0.566971242905889,-0.529135492171083,-0.52252805126537,-0.518644101583167,
-0.515161699457701,-0.510672225720102,-0.500888488324427,-0.487066081313597,
-0.468963384765506,-0.446140456083161,-0.442303407652579,-0.440105851115569,
-0.438108288613477,-0.435234261312038,-0.427517396431934,-0.414816752040312,
-0.374070516828562,-0.367166299282084,-0.363182169535609,-0.359715065365717,
-0.355386012453588,-0.346511417249682,-0.334459608486693,-0.314212928270044,
-0.292138917556691,-0.287261798795247,-0.284851850388718,-0.283091656914107,
-0.280678577880857,-0.275785240201533,-0.255484663542433,-0.217652712589653,
-0.211045932227278,-0.207162371337938,-0.203680318120044,-0.199191294627028,
-0.189408540320903,-0.175587524035446,-0.157482387143983,-0.134673379179808,
-0.130832621134821,-0.128634409119919,-0.126637404924991,-0.126596649745598,
-0.126556227922343,-0.126516094302381,-0.126476205440239,-0.12643651938905,
-0.126396995504326,-0.126357594267301,-0.12367729715794,-0.115989709383476,
-0.10318508505241,-0.0716022958255544,-0.0588240534330478,-0.0537446451827897,
-0.0502066078269937,-0.0465521100214381,-0.0410533708285637,-0.0321694988875906,
-0.00059011187237714),.UNSPECIFIED.);
#770=B_SPLINE_CURVE_WITH_KNOTS('',3,(#73194,#73195,#73196,#73197,#73198,
#73199,#73200,#73201,#73202,#73203,#73204),.UNSPECIFIED.,.F.,.F.,(4,1,1,
1,1,1,1,1,4),(53.4070751110265,53.5035699663983,54.5009068341909,55.4982437019834,
56.495580569776,57.4929174375686,58.4902543053611,59.4875911731537,59.690260418206),
 .UNSPECIFIED.);
#771=B_SPLINE_CURVE_WITH_KNOTS('',3,(#73209,#73210,#73211,#73212,#73213,
#73214,#73215,#73216,#73217,#73218,#73219,#73220,#73221,#73222,#73223,#73224,
#73225,#73226,#73227,#73228,#73229,#73230,#73231,#73232,#73233,#73234,#73235,
#73236,#73237,#73238,#73239,#73240,#73241,#73242,#73243,#73244,#73245,#73246,
#73247,#73248,#73249,#73250,#73251,#73252,#73253,#73254,#73255,#73256,#73257,
#73258,#73259,#73260,#73261,#73262,#73263,#73264,#73265,#73266,#73267,#73268,
#73269,#73270,#73271,#73272,#73273,#73274,#73275,#73276,#73277,#73278,#73279,
#73280,#73281,#73282,#73283,#73284,#73285,#73286,#73287,#73288,#73289,#73290,
#73291,#73292,#73293,#73294,#73295,#73296,#73297,#73298,#73299,#73300,#73301,
#73302,#73303,#73304,#73305,#73306,#73307,#73308,#73309,#73310,#73311,#73312,
#73313,#73314,#73315,#73316,#73317,#73318,#73319,#73320,#73321,#73322,#73323,
#73324,#73325,#73326,#73327,#73328,#73329,#73330,#73331,#73332,#73333,#73334,
#73335,#73336,#73337,#73338,#73339,#73340,#73341,#73342,#73343,#73344,#73345,
#73346,#73347,#73348,#73349,#73350,#73351,#73352,#73353,#73354,#73355,#73356,
#73357,#73358,#73359,#73360,#73361,#73362,#73363,#73364,#73365,#73366,#73367,
#73368,#73369,#73370,#73371,#73372,#73373,#73374,#73375,#73376,#73377,#73378,
#73379,#73380,#73381,#73382,#73383,#73384,#73385,#73386,#73387,#73388,#73389,
#73390,#73391,#73392,#73393,#73394,#73395,#73396,#73397,#73398,#73399,#73400,
#73401,#73402,#73403,#73404,#73405,#73406,#73407,#73408,#73409,#73410,#73411,
#73412,#73413,#73414),.UNSPECIFIED.,.F.,.F.,(4,2,2,2,2,2,2,2,2,2,2,2,2,
2,2,2,2,2,2,2,2,2,2,2,2,2,2,2,2,2,2,2,2,2,2,2,2,2,2,2,2,2,2,2,2,2,2,2,2,
2,2,2,2,2,2,2,2,2,2,2,2,2,2,2,2,2,2,2,2,2,2,2,2,2,2,2,2,2,2,2,2,2,2,2,2,
2,2,2,2,2,2,2,2,2,2,2,2,2,2,2,2,2,4),(-1.96126727528156,-1.93105273007122,
-1.92614954479132,-1.9225878868318,-1.9190141682557,-1.91578186639374,-1.91060622751215,
-1.8971310223569,-1.86633677311141,-1.85360048447955,-1.84595726088857,
-1.84327343451982,-1.84323393550042,-1.84319431115929,-1.84315452198443,
-1.84311452734102,-1.84307428529263,-1.84303375240652,-1.84299288354599,
-1.84099577856314,-1.83879891828285,-1.83496354364745,-1.81217175410611,
-1.7940741447777,-1.78026355404499,-1.77048549291687,-1.76599770443607,
-1.76251619351848,-1.75863280749374,-1.75202530252767,-1.714178197679,-1.69386802818047,
-1.68897397016179,-1.68656093249807,-1.6848009550598,-1.68239155645483,
-1.67751634973343,-1.65547438286872,-1.6352431033575,-1.62319130938956,
-1.61431613734523,-1.60998730604795,-1.60652055169849,-1.60253700940801,
-1.59563434610147,-1.55485900302106,-1.5421561108588,-1.53443907116245,
-1.53156514719995,-1.52956775785536,-1.52737046975683,-1.52353411615729,
-1.50072836385892,-1.48264311429537,-1.46882789384559,-1.45904707339614,
-1.45455836707444,-1.45107628042242,-1.44719239157592,-1.44058438424282,
-1.40272741777444,-1.38241646894521,-1.37752188648585,-1.37510851450253,
-1.37334825943277,-1.37093843086255,-1.36606220420035,-1.34397497225194,
-1.32386963099932,-1.31176816100545,-1.30286619566858,-1.2985320530226,
-1.29506440608076,-1.29108350664864,-1.28419492750851,-1.24334228229088,
-1.23066571853421,-1.22295878625003,-1.22008595558023,-1.21808850931274,
-1.21589023180595,-1.2120502790455,-1.18916021826107,-1.17093210297243,
-1.15724498181596,-1.14752731350888,-1.14304894156047,-1.13956753873734,
-1.13567689041728,-1.12903824464905,-1.09138538062198,-1.07093762712603,
-1.06602852102047,-1.06361211869405,-1.06185149136653,-1.05944386438801,
-1.05458021903962,-1.03062461239784,-1.00701771470968,-0.993266430473634,
-0.988196433148869,-0.984623917390367,-0.980958235625572),.UNSPECIFIED.);
#772=B_SPLINE_CURVE_WITH_KNOTS('',3,(#73415,#73416,#73417,#73418,#73419,
#73420,#73421,#73422,#73423,#73424,#73425,#73426,#73427,#73428,#73429,#73430,
#73431,#73432,#73433,#73434,#73435,#73436,#73437,#73438,#73439,#73440,#73441,
#73442,#73443,#73444,#73445,#73446,#73447,#73448,#73449,#73450,#73451,#73452,
#73453,#73454,#73455,#73456,#73457,#73458,#73459,#73460,#73461,#73462,#73463,
#73464,#73465,#73466,#73467,#73468,#73469,#73470,#73471,#73472,#73473,#73474,
#73475,#73476,#73477,#73478,#73479,#73480,#73481,#73482,#73483,#73484,#73485,
#73486,#73487,#73488,#73489,#73490,#73491,#73492,#73493,#73494,#73495,#73496,
#73497,#73498,#73499,#73500,#73501,#73502,#73503,#73504,#73505,#73506,#73507,
#73508,#73509,#73510,#73511,#73512,#73513,#73514,#73515,#73516,#73517,#73518,
#73519,#73520,#73521,#73522,#73523,#73524,#73525,#73526,#73527,#73528,#73529,
#73530,#73531,#73532,#73533,#73534,#73535,#73536,#73537,#73538,#73539,#73540,
#73541,#73542,#73543,#73544,#73545,#73546,#73547,#73548,#73549,#73550,#73551,
#73552,#73553,#73554,#73555,#73556,#73557,#73558,#73559,#73560,#73561,#73562,
#73563,#73564,#73565,#73566,#73567,#73568,#73569,#73570,#73571,#73572,#73573,
#73574,#73575,#73576,#73577,#73578,#73579,#73580,#73581,#73582,#73583,#73584,
#73585,#73586,#73587,#73588,#73589,#73590,#73591,#73592,#73593,#73594,#73595,
#73596,#73597,#73598,#73599,#73600,#73601,#73602,#73603,#73604,#73605,#73606,
#73607,#73608,#73609,#73610,#73611,#73612,#73613,#73614,#73615,#73616,#73617,
#73618,#73619,#73620,#73621,#73622,#73623,#73624,#73625,#73626,#73627,#73628,
#73629,#73630,#73631,#73632,#73633,#73634,#73635,#73636,#73637,#73638,#73639,
#73640,#73641,#73642),.UNSPECIFIED.,.F.,.F.,(4,2,2,2,2,2,2,2,2,2,2,2,2,
2,2,2,2,2,2,2,2,2,2,2,2,2,2,2,2,2,2,2,2,2,2,2,2,2,2,2,2,2,2,2,2,2,2,2,2,
2,2,2,2,2,2,2,2,2,2,2,2,2,2,2,2,2,2,2,2,2,2,2,2,2,2,2,2,2,2,2,2,2,2,2,2,
2,2,2,2,2,2,2,2,2,2,2,2,2,2,2,2,2,2,2,2,2,2,2,2,2,2,2,2,4),(-1.96131520446786,
-1.92943788095853,-1.92355672830733,-1.91837460556017,-1.91471296339964,
-1.91138682424772,-1.90688779805298,-1.89510294268181,-1.86372161370852,
-1.84999153718589,-1.84190809620745,-1.83915186119982,-1.83910758411492,
-1.83906325091772,-1.83901881608251,-1.83897423305584,-1.83892945405349,
-1.83888442984455,-1.83883910951657,-1.83879344021992,-1.83874736689821,
-1.83870083198413,-1.83865377506573,-1.83860613252695,-1.83855783714504,
-1.83853547678861,-1.8385110017733,-1.83848414646628,-1.83845459947384,
-1.83842199313684,-1.83838588992743,-1.83834576463254,-1.83635435198796,
-1.83391150945114,-1.82905403662827,-1.80453896845411,-1.78146948874141,
-1.76784738566127,-1.76271755252238,-1.75906519874492,-1.75528189243785,
-1.74947292118165,-1.73076361478782,-1.69983068591383,-1.69129819113837,
-1.68540827473551,-1.68277488549388,-1.68078271735008,-1.67834796852817,
-1.6735319106261,-1.64664242592921,-1.62516055964462,-1.61208483775083,
-1.60702606446256,-1.6033860227435,-1.59958199752634,-1.59367168168661,
-1.5735367041001,-1.54396919897841,-1.53559271686923,-1.52978051426087,
-1.52716063798383,-1.525342894526,-1.52297802099035,-1.51863753168265,-1.48721048630946,
-1.46827175016755,-1.4561578629458,-1.45123214649465,-1.44761411998053,
-1.44376628162906,-1.43764310130131,-1.41208793139349,-1.38726369023038,
-1.37583450283323,-1.3724975502077,-1.37037274843329,-1.36848817139706,
-1.36531206127979,-1.3562621341192,-1.32936021908511,-1.30803579769229,
-1.29912998301075,-1.29472808674067,-1.29117211718057,-1.28704832559484,
-1.27978989045142,-1.25015983649447,-1.23019949219605,-1.22326526031531,
-1.21820366844893,-1.21572123541111,-1.21371292489881,-1.21112617790703,
-1.20550117193668,-1.15935381865111,-1.14548612303428,-1.14032552970299,
-1.13666786901576,-1.13333789054813,-1.12795141043088,-1.11338299794338,
-1.0781257168,-1.06916468951207,-1.06306458668341,-1.06039527187634,-1.05838212573782,
-1.05596560285485,-1.05138316117734,-1.02250725217986,-1.00216615844222,
-0.989508566415736,-0.984506513065352,-0.980876168428268),.UNSPECIFIED.);
#773=B_SPLINE_CURVE_WITH_KNOTS('',3,(#73648,#73649,#73650,#73651,#73652,
#73653,#73654,#73655,#73656,#73657,#73658,#73659,#73660,#73661,#73662,#73663,
#73664,#73665,#73666,#73667,#73668,#73669,#73670,#73671,#73672,#73673,#73674,
#73675,#73676,#73677,#73678,#73679,#73680,#73681,#73682,#73683,#73684,#73685,
#73686,#73687,#73688,#73689,#73690,#73691,#73692,#73693,#73694,#73695,#73696,
#73697,#73698,#73699,#73700,#73701,#73702,#73703,#73704,#73705,#73706,#73707,
#73708,#73709,#73710,#73711,#73712,#73713,#73714,#73715,#73716,#73717,#73718,
#73719,#73720,#73721,#73722,#73723,#73724,#73725,#73726,#73727,#73728,#73729,
#73730,#73731,#73732,#73733,#73734,#73735,#73736,#73737,#73738,#73739,#73740,
#73741,#73742,#73743,#73744,#73745,#73746,#73747,#73748,#73749,#73750,#73751,
#73752,#73753,#73754,#73755,#73756,#73757,#73758,#73759,#73760,#73761,#73762,
#73763,#73764,#73765,#73766,#73767,#73768,#73769,#73770,#73771,#73772,#73773,
#73774,#73775,#73776,#73777,#73778,#73779,#73780,#73781,#73782,#73783,#73784,
#73785,#73786,#73787,#73788,#73789,#73790,#73791,#73792,#73793,#73794,#73795,
#73796,#73797,#73798,#73799,#73800,#73801,#73802,#73803,#73804,#73805,#73806,
#73807,#73808,#73809,#73810,#73811,#73812,#73813,#73814,#73815,#73816,#73817,
#73818,#73819,#73820,#73821,#73822,#73823,#73824,#73825,#73826,#73827,#73828,
#73829,#73830,#73831,#73832,#73833,#73834,#73835,#73836,#73837,#73838,#73839,
#73840,#73841,#73842,#73843),.UNSPECIFIED.,.F.,.F.,(4,2,2,2,2,2,2,2,2,2,
2,2,2,2,2,2,2,2,2,2,2,2,2,2,2,2,2,2,2,2,2,2,2,2,2,2,2,2,2,2,2,2,2,2,2,2,
2,2,2,2,2,2,2,2,2,2,2,2,2,2,2,2,2,2,2,2,2,2,2,2,2,2,2,2,2,2,2,2,2,2,2,2,
2,2,2,2,2,2,2,2,2,2,2,2,2,2,2,4),(-0.980645665338926,-0.974666323535037,
-0.97223769601446,-0.970257683639558,-0.968071541575421,-0.964288528935635,
-0.943592129360979,-0.908089213287009,-0.899205389329285,-0.894874388002916,
-0.891406785570255,-0.887423241042882,-0.880333304964163,-0.85676840480011,
-0.831089529238214,-0.820300547249837,-0.816977775915276,-0.814891115931844,
-0.812823437358398,-0.809589205111678,-0.798722729599752,-0.776101980797758,
-0.74984617806715,-0.743234039859205,-0.738980812807193,-0.735517896332518,
-0.73147514494383,-0.724093278070161,-0.714701125806817,-0.690700662497402,
-0.66726349693708,-0.662401068154134,-0.659993746122316,-0.658233185691063,
-0.655816696659856,-0.650906776451215,-0.630449032200712,-0.592853965402241,
-0.586212115740881,-0.58232090418751,-0.578839760015425,-0.574362793964848,
-0.564653076170167,-0.550979972651322,-0.532716106511657,-0.509798427376246,
-0.505957740907556,-0.50375933952987,-0.501761982408931,-0.498889608050369,
-0.491185464030826,-0.478516946050841,-0.437686937697177,-0.430799919361101,
-0.42681938163587,-0.423351716855175,-0.419017117386274,-0.410112784871566,
-0.39800523574692,-0.377884853016302,-0.35578324384419,-0.350905737624942,
-0.348495644493398,-0.34673536829787,-0.3443222050675,-0.339428793451435,
-0.319128790248061,-0.281292609047425,-0.274685858405628,-0.270802184187558,
-0.267319950605578,-0.262830583825892,-0.253046602453103,-0.239223390495474,
-0.221123327188658,-0.19830251176959,-0.194465697669086,-0.192268263689428,
-0.190270803426278,-0.187396910440489,-0.17968032809377,-0.166980042977409,
-0.126237977392895,-0.119333261613625,-0.115349155606177,-0.111882252861876,
-0.107553688668094,-0.0989119825103673,-0.0871418306658754,-0.0577696942921653,
-0.0422319173104418,-0.0385724939397159,-0.0364132232087641,-0.0343978211934399,
-0.0323424207994555,-0.0294317383989918,-0.0243303419455859,-0.000460869334322469),
 .UNSPECIFIED.);
#774=B_SPLINE_CURVE_WITH_KNOTS('',3,(#73844,#73845,#73846,#73847),
 .UNSPECIFIED.,.F.,.F.,(4,4),(-1.96141007892017,-1.96126727528156),
 .UNSPECIFIED.);
#775=B_SPLINE_CURVE_WITH_KNOTS('',3,(#73848,#73849,#73850,#73851,#73852,
#73853,#73854,#73855,#73856,#73857,#73858,#73859,#73860,#73861,#73862,#73863,
#73864,#73865,#73866,#73867,#73868,#73869,#73870,#73871,#73872,#73873,#73874,
#73875,#73876,#73877,#73878,#73879,#73880,#73881,#73882,#73883,#73884,#73885,
#73886,#73887,#73888,#73889,#73890,#73891,#73892,#73893,#73894,#73895,#73896,
#73897,#73898,#73899,#73900,#73901,#73902,#73903,#73904,#73905,#73906,#73907,
#73908,#73909,#73910,#73911,#73912,#73913,#73914,#73915,#73916,#73917,#73918,
#73919,#73920,#73921,#73922,#73923,#73924,#73925,#73926,#73927,#73928,#73929,
#73930,#73931,#73932,#73933,#73934,#73935,#73936,#73937,#73938,#73939,#73940,
#73941,#73942,#73943,#73944,#73945,#73946,#73947,#73948,#73949,#73950,#73951,
#73952,#73953,#73954,#73955,#73956,#73957,#73958,#73959,#73960,#73961,#73962,
#73963,#73964,#73965,#73966,#73967,#73968,#73969,#73970,#73971,#73972,#73973,
#73974,#73975,#73976,#73977,#73978,#73979,#73980,#73981,#73982,#73983,#73984,
#73985,#73986,#73987,#73988,#73989,#73990,#73991,#73992,#73993,#73994,#73995,
#73996,#73997,#73998,#73999,#74000,#74001,#74002,#74003,#74004,#74005,#74006,
#74007,#74008,#74009,#74010,#74011,#74012,#74013,#74014,#74015,#74016,#74017,
#74018,#74019,#74020,#74021,#74022,#74023,#74024,#74025,#74026,#74027,#74028,
#74029,#74030,#74031,#74032,#74033,#74034,#74035),.UNSPECIFIED.,.F.,.F.,
(4,2,2,2,2,2,2,2,2,2,2,2,2,2,2,2,2,2,2,2,2,2,2,2,2,2,2,2,2,2,2,2,2,2,2,
2,2,2,2,2,2,2,2,2,2,2,2,2,2,2,2,2,2,2,2,2,2,2,2,2,2,2,2,2,2,2,2,2,2,2,2,
2,2,2,2,2,2,2,2,2,2,2,2,2,2,2,2,2,2,2,2,2,2,4),(-0.980876168428268,-0.977054577333388,
-0.971058136352527,-0.947128510180332,-0.913627961840072,-0.907482535791466,
-0.904833905222632,-0.902818455338693,-0.900419719119447,-0.895784983276597,
-0.878273227041829,-0.83826909371721,-0.831190969785972,-0.827105983365669,
-0.823580675930354,-0.819143780139889,-0.81004528608956,-0.797644721499304,
-0.778040914206429,-0.756182211256192,-0.751259083678782,-0.748803498409371,
-0.746995320137182,-0.744489719700661,-0.739305420901276,-0.732143731276741,
-0.710920394724917,-0.683059416039829,-0.675779308071825,-0.671651124032574,
-0.668095803463219,-0.663700414361992,-0.654828950867061,-0.633288137205705,
-0.606124496814735,-0.597379435812432,-0.594242696942268,-0.592365256933383,
-0.59023062496181,-0.586847378039513,-0.574888246676247,-0.547530371600936,
-0.525006295033887,-0.51896894127087,-0.515138976049794,-0.511512913338456,
-0.506536511101398,-0.494064408776799,-0.474210112073718,-0.44445913581959,
-0.439936071794941,-0.43753211068626,-0.435517392602543,-0.432830240312782,
-0.426624007951772,-0.417444101433213,-0.379483725265717,-0.367259580537071,
-0.362198184110808,-0.358593915911576,-0.354799609725716,-0.348936152852545,
-0.327401860553773,-0.318880499806321,-0.288795859276366,-0.284304324023758,
-0.281907073605292,-0.279891463930923,-0.277194552678228,-0.270929622593811,
-0.261626923386461,-0.221977407363355,-0.211100078830289,-0.206738840858881,
-0.20311499433603,-0.199352136194739,-0.193643715993576,-0.174309406808942,
-0.144190326869769,-0.131417655661919,-0.127864249414894,-0.125692908616759,
-0.123592591542536,-0.120838162179996,-0.112761670237951,-0.0990543182056354,
-0.0674553159482955,-0.0558526492312413,-0.0513687559118857,-0.0480461738853702,
-0.044381004067567,-0.0391794224292523,-0.0332689907290768,-0.000593869235482755),
 .UNSPECIFIED.);
#776=B_SPLINE_CURVE_WITH_KNOTS('',3,(#74041,#74042,#74043,#74044),
 .UNSPECIFIED.,.F.,.F.,(4,4),(-0.000575552145866446,-0.000460828836829869),
 .UNSPECIFIED.);
#777=B_SPLINE_CURVE_WITH_KNOTS('',3,(#74045,#74046,#74047,#74048,#74049,
#74050,#74051,#74052,#74053,#74054,#74055,#74056,#74057,#74058,#74059,#74060,
#74061,#74062,#74063,#74064,#74065,#74066,#74067,#74068,#74069,#74070,#74071,
#74072,#74073,#74074,#74075,#74076,#74077,#74078,#74079,#74080,#74081,#74082,
#74083,#74084,#74085,#74086,#74087,#74088,#74089,#74090,#74091,#74092,#74093,
#74094,#74095,#74096,#74097,#74098,#74099,#74100,#74101,#74102,#74103,#74104,
#74105,#74106,#74107,#74108,#74109,#74110,#74111,#74112,#74113,#74114,#74115,
#74116,#74117,#74118,#74119,#74120,#74121,#74122,#74123,#74124,#74125,#74126,
#74127,#74128,#74129,#74130,#74131,#74132,#74133,#74134,#74135,#74136,#74137,
#74138,#74139,#74140,#74141,#74142,#74143,#74144,#74145,#74146,#74147,#74148,
#74149,#74150,#74151,#74152,#74153,#74154,#74155,#74156,#74157,#74158,#74159,
#74160,#74161,#74162,#74163,#74164,#74165,#74166,#74167,#74168,#74169,#74170,
#74171,#74172,#74173,#74174,#74175,#74176,#74177,#74178,#74179,#74180,#74181,
#74182,#74183,#74184,#74185,#74186,#74187,#74188,#74189,#74190,#74191,#74192,
#74193,#74194,#74195,#74196,#74197,#74198,#74199,#74200,#74201,#74202,#74203,
#74204,#74205,#74206,#74207,#74208,#74209,#74210,#74211,#74212,#74213,#74214,
#74215,#74216,#74217,#74218,#74219,#74220,#74221,#74222,#74223,#74224,#74225,
#74226,#74227,#74228,#74229,#74230,#74231,#74232,#74233,#74234,#74235,#74236,
#74237,#74238,#74239,#74240,#74241,#74242,#74243,#74244,#74245,#74246),
 .UNSPECIFIED.,.F.,.F.,(4,2,2,2,2,2,2,2,2,2,2,2,2,2,2,2,2,2,2,2,2,2,2,2,
2,2,2,2,2,2,2,2,2,2,2,2,2,2,2,2,2,2,2,2,2,2,2,2,2,2,2,2,2,2,2,2,2,2,2,2,
2,2,2,2,2,2,2,2,2,2,2,2,2,2,2,2,2,2,2,2,2,2,2,2,2,2,2,2,2,2,2,2,2,2,2,2,
2,2,2,2,4),(-1.961075810873,-1.91899853770295,-1.90998182103901,-1.90694299155077,
-1.90491534220976,-1.90304236077713,-1.8997563454517,-1.8893489139275,-1.86341553042212,
-1.84622210656141,-1.83844349395447,-1.83215983190748,-1.83188418037971,
-1.83161731506151,-1.83135527090537,-1.83109406229579,-1.8308294449826,
-1.83055660950542,-1.83026974685407,-1.82996137869829,-1.82986837677026,
-1.82968979753097,-1.82929230164806,-1.82582900399034,-1.82179662391704,
-1.81466844992312,-1.78236237688157,-1.76408344162407,-1.75441378202244,
-1.75130115434868,-1.7492588257632,-1.7471417152126,-1.74367783445721,-1.73139069868062,
-1.68623717362766,-1.67774757120391,-1.67348987226925,-1.67002732821849,
-1.6659895482079,-1.65883478865551,-1.62757226213126,-1.60857171259333,
-1.59868595244813,-1.59555035007265,-1.59350350518122,-1.59165102702241,
-1.58847137800807,-1.57900844240478,-1.55236121576361,-1.5283076110314,
-1.5211548559745,-1.51715893867982,-1.51369317433401,-1.50938093191052,
-1.50256268998503,-1.46193662360606,-1.44402953233452,-1.44033945560061,
-1.43817346777158,-1.4361845989699,-1.43324681038929,-1.42565416635324,
-1.39750794326695,-1.37496776301316,-1.36634819298059,-1.36206593053318,
-1.35860168529218,-1.35458239461893,-1.34751548241122,-1.30750617965681,
-1.29448563991458,-1.28664220003162,-1.28375081202092,-1.28175019362452,
-1.27955941510628,-1.27575453902151,-1.25548477657915,-1.23972014239311,
-1.22295403440966,-1.21179633566403,-1.20708473601124,-1.20357254405719,
-1.19979250101891,-1.1936850302796,-1.1673764481476,-1.14772300672639,-1.13232057046893,
-1.12875071981942,-1.12661057406961,-1.12460748037476,-1.12159283019553,
-1.11342327548466,-1.07482374194821,-1.05772822712093,-1.05229567064237,
-1.04865398905507,-1.04510515845138,-1.0399686208525,-1.02678462238953,
-0.989724130567848,-0.980645665338926),.UNSPECIFIED.);
#778=B_SPLINE_CURVE_WITH_KNOTS('',3,(#74248,#74249,#74250,#74251),
 .UNSPECIFIED.,.F.,.F.,(4,4),(-0.000593869235482755,-0.000459408681297817),
 .UNSPECIFIED.);
#779=B_SPLINE_CURVE_WITH_KNOTS('',3,(#74252,#74253,#74254,#74255,#74256,
#74257,#74258,#74259,#74260,#74261,#74262,#74263,#74264,#74265,#74266,#74267,
#74268,#74269,#74270,#74271,#74272,#74273,#74274,#74275,#74276,#74277,#74278,
#74279,#74280,#74281,#74282,#74283,#74284,#74285,#74286,#74287,#74288,#74289,
#74290,#74291,#74292,#74293,#74294,#74295,#74296,#74297,#74298,#74299,#74300,
#74301,#74302,#74303,#74304,#74305,#74306,#74307,#74308,#74309,#74310,#74311,
#74312,#74313,#74314,#74315,#74316,#74317,#74318,#74319,#74320,#74321,#74322,
#74323,#74324,#74325,#74326,#74327,#74328,#74329,#74330,#74331,#74332,#74333,
#74334,#74335,#74336,#74337,#74338,#74339,#74340,#74341,#74342,#74343,#74344,
#74345,#74346,#74347,#74348,#74349,#74350,#74351,#74352,#74353,#74354,#74355,
#74356,#74357,#74358,#74359,#74360,#74361,#74362,#74363,#74364,#74365,#74366,
#74367,#74368,#74369,#74370,#74371,#74372,#74373,#74374,#74375,#74376,#74377,
#74378,#74379,#74380,#74381,#74382,#74383,#74384,#74385,#74386,#74387,#74388,
#74389,#74390,#74391,#74392,#74393,#74394,#74395,#74396,#74397,#74398,#74399,
#74400,#74401,#74402,#74403,#74404,#74405,#74406,#74407,#74408,#74409,#74410,
#74411,#74412,#74413,#74414,#74415,#74416,#74417,#74418,#74419,#74420,#74421,
#74422,#74423,#74424,#74425,#74426,#74427,#74428,#74429,#74430,#74431,#74432,
#74433,#74434,#74435,#74436,#74437,#74438,#74439,#74440,#74441,#74442,#74443,
#74444,#74445,#74446,#74447),.UNSPECIFIED.,.F.,.F.,(4,2,2,2,2,2,2,2,2,2,
2,2,2,2,2,2,2,2,2,2,2,2,2,2,2,2,2,2,2,2,2,2,2,2,2,2,2,2,2,2,2,2,2,2,2,2,
2,2,2,2,2,2,2,2,2,2,2,2,2,2,2,2,2,2,2,2,2,2,2,2,2,2,2,2,2,2,2,2,2,2,2,2,
2,2,2,2,2,2,2,2,2,2,2,2,2,2,2,4),(-1.96095646099311,-1.93797621015352,-1.9347460978949,
-1.93254341532058,-1.93041904654259,-1.92827638974903,-1.92485595093305,
-1.91354033516731,-1.88921053153627,-1.86780065348812,-1.8591642713876,
-1.85476922440857,-1.85121379045361,-1.84708503604146,-1.83980280839497,
-1.81192126711676,-1.79068411128328,-1.78351891530459,-1.77833314729868,
-1.77582719487037,-1.77401893116401,-1.77156344685772,-1.76664120722514,
-1.74478166349544,-1.72518210094038,-1.71279999533315,-1.70371020745299,
-1.69927475738958,-1.69571666817842,-1.69161797086906,-1.68447675942516,
-1.65166771350105,-1.62594442589702,-1.62195617052201,-1.61969121517274,
-1.61764235909756,-1.61469844374575,-1.60732581056317,-1.57534812098983,
-1.55177478391219,-1.5457960189052,-1.54197781464795,-1.53834516078742,
-1.53333095064799,-1.52138774635452,-1.4830397119817,-1.4738260797527,-1.46760396261687,
-1.46491391257529,-1.46289870369644,-1.46049614633478,-1.45598067874288,
-1.42616602642821,-1.40636450065013,-1.39391143065581,-1.38893724766454,
-1.38531106842197,-1.38147940727529,-1.37543602554564,-1.35279227623871,
-1.325500776513,-1.3135518393757,-1.31016886069965,-1.30803404276792,-1.30615612044012,
-1.30301807546051,-1.29426535540527,-1.26712253259344,-1.24559510288315,
-1.23672438290905,-1.2323286050034,-1.22877258450223,-1.22464315431967,
-1.21735974942338,-1.18946990832735,-1.16823199635046,-1.16106610088098,
-1.15587973537714,-1.15337341850365,-1.15156485961709,-1.14910892750324,
-1.1441856525028,-1.12229264185881,-1.10245524418662,-1.09021670995437,
-1.08120233489742,-1.07678014582888,-1.07322241907951,-1.06911280232661,
-1.06192255250942,-1.02993008681522,-1.01160663459219,-1.00188219983893,
-0.998715416197789,-0.996625442669738,-0.994709137080463,-0.991364475530684,
-0.980870200702631),.UNSPECIFIED.);
#780=B_SPLINE_CURVE_WITH_KNOTS('',3,(#74452,#74453,#74454,#74455,#74456,
#74457,#74458,#74459,#74460,#74461,#74462,#74463,#74464,#74465,#74466,#74467,
#74468,#74469,#74470,#74471,#74472,#74473,#74474,#74475,#74476,#74477,#74478,
#74479,#74480,#74481,#74482,#74483,#74484,#74485,#74486,#74487,#74488,#74489,
#74490,#74491,#74492,#74493,#74494,#74495,#74496,#74497,#74498,#74499,#74500,
#74501,#74502,#74503,#74504,#74505,#74506,#74507,#74508,#74509,#74510,#74511,
#74512,#74513,#74514,#74515,#74516,#74517,#74518,#74519,#74520,#74521,#74522,
#74523,#74524,#74525,#74526,#74527,#74528,#74529,#74530,#74531,#74532,#74533,
#74534,#74535,#74536,#74537,#74538,#74539,#74540,#74541,#74542,#74543,#74544,
#74545,#74546,#74547,#74548,#74549,#74550,#74551,#74552,#74553,#74554,#74555,
#74556,#74557,#74558,#74559,#74560,#74561,#74562,#74563,#74564,#74565,#74566,
#74567,#74568,#74569,#74570,#74571,#74572,#74573,#74574,#74575,#74576,#74577,
#74578,#74579,#74580,#74581,#74582,#74583,#74584,#74585,#74586,#74587,#74588,
#74589,#74590,#74591,#74592,#74593,#74594,#74595,#74596,#74597,#74598,#74599,
#74600,#74601,#74602,#74603,#74604,#74605,#74606,#74607,#74608,#74609,#74610,
#74611,#74612,#74613,#74614,#74615,#74616,#74617,#74618,#74619,#74620,#74621,
#74622,#74623,#74624,#74625,#74626,#74627,#74628,#74629,#74630,#74631,#74632,
#74633,#74634,#74635,#74636,#74637,#74638,#74639,#74640,#74641,#74642,#74643,
#74644,#74645,#74646,#74647,#74648,#74649),.UNSPECIFIED.,.F.,.F.,(4,2,2,
2,2,2,2,2,2,2,2,2,2,2,2,2,2,2,2,2,2,2,2,2,2,2,2,2,2,2,2,2,2,2,2,2,2,2,2,
2,2,2,2,2,2,2,2,2,2,2,2,2,2,2,2,2,2,2,2,2,2,2,2,2,2,2,2,2,2,2,2,2,2,2,2,
2,2,2,2,2,2,2,2,2,2,2,2,2,2,2,2,2,2,2,2,2,2,2,4),(-0.980863317691536,-0.965867117327354,
-0.960509977420319,-0.957246005987621,-0.953700602037113,-0.948778820150156,
-0.936160706365215,-0.915796960466177,-0.886633299232025,-0.882101790965228,
-0.879731730871915,-0.877791687500907,-0.875235281143686,-0.869564325728112,
-0.861418051207541,-0.833411462878822,-0.811346039029316,-0.805410731783076,
-0.801666513767412,-0.798139560333822,-0.793332781792027,-0.781537061532407,
-0.763266075494988,-0.734529140602185,-0.727602164655597,-0.724769359783965,
-0.722778449107396,-0.720563024669574,-0.716642471906693,-0.711668238966146,
-0.700170469933032,-0.664625105612122,-0.653268497146771,-0.648885013568821,
-0.64564373405902,-0.642077590800852,-0.637040066926753,-0.623543900163697,
-0.600708867265467,-0.575511695663898,-0.570716949960351,-0.568322971638379,
-0.566562074793609,-0.564132239351519,-0.559151679267259,-0.552325315706278,
-0.53274413159117,-0.502342724765227,-0.495166210540832,-0.491123668033165,
-0.487661210975058,-0.483408908339107,-0.474949025075862,-0.456241589004391,
-0.425830697244409,-0.416794217648005,-0.413666201389874,-0.411823256843222,
-0.409765135979663,-0.406575817981292,-0.39616940360447,-0.375325037058781,
-0.346670459095679,-0.340096333282019,-0.335854279904117,-0.332392069852111,
-0.328340602631258,-0.3209145732756,-0.311447462031061,-0.287073273178223,
-0.264187156199857,-0.259311646353736,-0.256901878484548,-0.25514152450932,
-0.252727849594165,-0.247832003799856,-0.227509167754953,-0.189707310226555,
-0.183095414116581,-0.179210607710657,-0.175728497822314,-0.171240891875978,
-0.161467671206921,-0.147666351322913,-0.129541294107978,-0.106706335594181,
-0.10286893895474,-0.100671349009583,-0.0986738861195674,-0.0958001874210858,
-0.0880853442082756,-0.0557117277541239,-0.0327323384169256,-0.0267749109151,
-0.0230263763554905,-0.0197066597234133,-0.0162728494754162,-0.00976563376091629,
-0.000575552145866446),.UNSPECIFIED.);
#781=B_SPLINE_CURVE_WITH_KNOTS('',3,(#74650,#74651,#74652,#74653,#74654,
#74655,#74656,#74657,#74658,#74659,#74660,#74661,#74662,#74663,#74664,#74665,
#74666,#74667,#74668,#74669,#74670,#74671,#74672,#74673,#74674,#74675,#74676,
#74677,#74678,#74679,#74680,#74681,#74682,#74683,#74684,#74685,#74686,#74687,
#74688,#74689,#74690,#74691,#74692,#74693,#74694,#74695,#74696,#74697,#74698,
#74699,#74700,#74701,#74702,#74703,#74704,#74705,#74706,#74707,#74708,#74709,
#74710,#74711,#74712,#74713,#74714,#74715,#74716,#74717,#74718,#74719,#74720,
#74721,#74722,#74723,#74724,#74725,#74726,#74727,#74728,#74729,#74730,#74731,
#74732,#74733,#74734,#74735,#74736,#74737,#74738,#74739,#74740,#74741,#74742,
#74743,#74744,#74745,#74746,#74747,#74748,#74749,#74750,#74751,#74752,#74753,
#74754,#74755,#74756,#74757,#74758,#74759,#74760,#74761,#74762,#74763,#74764,
#74765,#74766,#74767,#74768,#74769,#74770,#74771,#74772,#74773,#74774,#74775,
#74776,#74777,#74778,#74779,#74780,#74781,#74782,#74783,#74784,#74785,#74786,
#74787,#74788,#74789,#74790,#74791,#74792,#74793,#74794,#74795,#74796,#74797,
#74798,#74799,#74800,#74801,#74802,#74803,#74804,#74805,#74806,#74807,#74808,
#74809,#74810,#74811,#74812,#74813,#74814,#74815,#74816,#74817,#74818,#74819,
#74820,#74821,#74822,#74823,#74824,#74825,#74826,#74827,#74828,#74829,#74830,
#74831,#74832,#74833),.UNSPECIFIED.,.F.,.F.,(4,2,2,2,2,2,2,2,2,2,2,2,2,
2,2,2,2,2,2,2,2,2,2,2,2,2,2,2,2,2,2,2,2,2,2,2,2,2,2,2,2,2,2,2,2,2,2,2,2,
2,2,2,2,2,2,2,2,2,2,2,2,2,2,2,2,2,2,2,2,2,2,2,2,2,2,2,2,2,2,2,2,2,2,2,2,
2,2,2,2,2,2,4),(-0.980870200702631,-0.959233141018411,-0.93190896443026,
-0.924624978851224,-0.920495370274395,-0.916939257898618,-0.91254344802788,
-0.903673180419709,-0.881982256206798,-0.854580117112285,-0.846121338780522,
-0.843022317621479,-0.840966102919178,-0.838765037533061,-0.835075393420603,
-0.818476808473076,-0.784580675202224,-0.771866281982843,-0.766721228358717,
-0.763102076304601,-0.759330410068892,-0.753580809435499,-0.733717236154346,
-0.715126304519363,-0.692092080343054,-0.688187746217947,-0.685940577943202,
-0.683884040587284,-0.680895671239572,-0.672655764602268,-0.658699668096323,
-0.623474250443168,-0.61437873329379,-0.609941876992769,-0.606383262467072,
-0.602284622260668,-0.594946843738724,-0.570014243225577,-0.54140189445304,
-0.534395639274989,-0.531506733698327,-0.529466550543011,-0.52717683878325,
-0.523072437473335,-0.517823279884699,-0.505421432498898,-0.46416692731791,
-0.457272884855933,-0.453265143176066,-0.449694296194633,-0.445117747607311,
-0.435228549961263,-0.42127824178971,-0.403401120909165,-0.380802589911048,
-0.376914723694649,-0.374671180476488,-0.372613267552639,-0.369616253580438,
-0.361308613811237,-0.347171414597535,-0.311227236971825,-0.302865741900337,
-0.298513455877025,-0.294959963192897,-0.290796418098491,-0.283134262465949,
-0.273323743896622,-0.247400704669714,-0.226926391642494,-0.222011856884129,
-0.219557785889306,-0.217749322902074,-0.215241546837998,-0.210046558937141,
-0.202865165695763,-0.181531973896022,-0.1538286593312,-0.146535290734253,
-0.142403965070233,-0.13884840128958,-0.134455871016647,-0.125601745092855,
-0.103360060575001,-0.0750737990044077,-0.0676887033980364,-0.0647427232674537,
-0.0626934621791439,-0.0604290573631328,-0.0564441447427007,-0.0309181846902309,
-0.000459946153919901),.UNSPECIFIED.);
#782=B_SPLINE_CURVE_WITH_KNOTS('',3,(#74838,#74839,#74840,#74841,#74842,
#74843,#74844,#74845,#74846,#74847,#74848,#74849,#74850,#74851,#74852,#74853,
#74854,#74855,#74856,#74857,#74858,#74859,#74860,#74861,#74862,#74863,#74864,
#74865,#74866,#74867,#74868,#74869,#74870,#74871,#74872,#74873,#74874,#74875,
#74876,#74877,#74878,#74879,#74880,#74881,#74882,#74883,#74884,#74885,#74886,
#74887,#74888,#74889,#74890,#74891,#74892,#74893,#74894,#74895,#74896,#74897,
#74898,#74899,#74900,#74901,#74902,#74903,#74904,#74905,#74906,#74907,#74908,
#74909,#74910,#74911,#74912,#74913,#74914,#74915,#74916,#74917,#74918,#74919,
#74920,#74921,#74922,#74923,#74924,#74925,#74926,#74927,#74928,#74929,#74930,
#74931,#74932,#74933,#74934,#74935,#74936,#74937,#74938,#74939,#74940,#74941,
#74942,#74943,#74944,#74945,#74946,#74947,#74948,#74949,#74950,#74951,#74952,
#74953,#74954,#74955,#74956,#74957,#74958,#74959,#74960,#74961,#74962,#74963,
#74964,#74965,#74966,#74967,#74968,#74969,#74970,#74971,#74972,#74973,#74974,
#74975,#74976,#74977,#74978,#74979,#74980,#74981,#74982,#74983,#74984,#74985,
#74986,#74987,#74988,#74989,#74990,#74991,#74992,#74993,#74994,#74995,#74996,
#74997,#74998,#74999,#75000,#75001,#75002,#75003,#75004,#75005,#75006,#75007,
#75008,#75009,#75010,#75011,#75012,#75013,#75014,#75015,#75016,#75017,#75018,
#75019,#75020,#75021,#75022,#75023),.UNSPECIFIED.,.F.,.F.,(4,2,2,2,2,2,
2,2,2,2,2,2,2,2,2,2,2,2,2,2,2,2,2,2,2,2,2,2,2,2,2,2,2,2,2,2,2,2,2,2,2,2,
2,2,2,2,2,2,2,2,2,2,2,2,2,2,2,2,2,2,2,2,2,2,2,2,2,2,2,2,2,2,2,2,2,2,2,2,
2,2,2,2,2,2,2,2,2,2,2,2,2,2,4),(-1.96110176712048,-1.93829452872204,-1.9186414530334,
-1.9006083574055,-1.89511660925849,-1.89148282314228,-1.8879775752466,-1.88296957684836,
-1.8705452485945,-1.83871994755745,-1.82085867669616,-1.81624560361653,
-1.8138996090342,-1.81194724276637,-1.80942122989633,-1.8037698646084,-1.77377296835817,
-1.75031288736422,-1.74158015519043,-1.73727086618697,-1.73379725776558,
-1.72978049298282,-1.72275139326327,-1.68282918403212,-1.66990776228069,
-1.66210217842162,-1.65920917062187,-1.65720301166931,-1.65500399323105,
-1.65116775426461,-1.62844641714766,-1.61049576819412,-1.5965862356164,
-1.5867598494002,-1.5822626255474,-1.57877859390135,-1.57489724205419,-1.5683054359448,
-1.53026405657233,-1.51002820173751,-1.50514152785202,-1.5027302127129,
-1.50097133141034,-1.49856354659451,-1.49368966976771,-1.47157101569616,
-1.45146416591831,-1.43938269548927,-1.43049338145184,-1.42616464337538,
-1.42273291481658,-1.41876854997284,-1.41194303965079,-1.37078896027392,
-1.35822156490455,-1.3505599610277,-1.3476955096223,-1.34570092152039,-1.34350102237631,
-1.33965322447287,-1.31655626217935,-1.29810095462964,-1.28467235989981,
-1.27508348352818,-1.27062655032077,-1.26714662126167,-1.26324183739805,
-1.25653819528689,-1.21940199925403,-1.19865761267728,-1.19371779055523,
-1.19129475812602,-1.18953338640535,-1.18713056761634,-1.18229177995356,
-1.15869262558282,-1.13481850835135,-1.12098292052455,-1.11590301804018,
-1.1123290773621,-1.10909528462873,-1.10474409925921,-1.09369781525337,
-1.06070327618473,-1.04725096680036,-1.03923958507351,-1.0363260922519,
-1.03432190919966,-1.03214053542194,-1.02837803395873,-1.0101859617264,
-0.980971677752746,-0.980863317691536),.UNSPECIFIED.);
#783=B_SPLINE_CURVE_WITH_KNOTS('',3,(#75024,#75025,#75026,#75027,#75028,
#75029,#75030,#75031,#75032,#75033,#75034,#75035,#75036,#75037,#75038,#75039,
#75040,#75041,#75042,#75043,#75044,#75045,#75046,#75047,#75048,#75049,#75050,
#75051,#75052,#75053,#75054,#75055,#75056,#75057,#75058,#75059,#75060,#75061,
#75062,#75063,#75064,#75065,#75066,#75067,#75068,#75069,#75070,#75071,#75072,
#75073,#75074,#75075,#75076,#75077,#75078,#75079,#75080,#75081,#75082,#75083,
#75084,#75085,#75086,#75087,#75088,#75089,#75090,#75091,#75092,#75093,#75094,
#75095,#75096,#75097,#75098,#75099,#75100,#75101,#75102,#75103,#75104,#75105,
#75106,#75107,#75108,#75109,#75110,#75111,#75112,#75113,#75114,#75115,#75116,
#75117,#75118,#75119,#75120,#75121,#75122,#75123,#75124,#75125,#75126,#75127,
#75128,#75129,#75130,#75131,#75132,#75133,#75134,#75135,#75136,#75137,#75138,
#75139,#75140,#75141,#75142,#75143,#75144,#75145,#75146,#75147,#75148,#75149,
#75150,#75151,#75152,#75153,#75154,#75155,#75156,#75157,#75158,#75159,#75160,
#75161,#75162,#75163,#75164,#75165,#75166,#75167,#75168,#75169,#75170,#75171,
#75172,#75173,#75174,#75175,#75176,#75177,#75178,#75179,#75180,#75181,#75182,
#75183,#75184,#75185,#75186,#75187,#75188,#75189,#75190,#75191,#75192,#75193,
#75194,#75195,#75196,#75197,#75198),.UNSPECIFIED.,.F.,.F.,(4,3,3,3,3,3,
3,3,3,3,3,3,3,3,3,3,3,3,3,3,3,3,3,3,3,3,3,3,3,3,3,3,3,3,3,3,3,3,3,3,3,3,
3,3,3,3,3,3,3,3,3,3,3,3,3,3,3,3,4),(84.8230016469244,84.9358865834066,85.0488192149489,
85.161925902012,85.2751347285546,85.3885713550513,85.4183497357604,85.5300439425675,
85.6415395478339,85.7529242433787,85.8642409672866,85.9755325604619,86.0869248023224,
86.198363088933,86.3100187360176,86.4156866035529,86.5273871490937,86.638889046833,
86.7502800027488,86.8616029448844,86.9729007040699,87.0842989814853,87.1957432424682,
87.307404682471,87.4130234713455,87.5247274427104,87.636232886227,87.7476274581574,
87.8589540796684,87.9702555748027,88.0816576457093,88.1931057379006,88.3047710215193,
88.4103603391381,88.5220342594052,88.6335095720259,88.7448739843744,88.856170468079,
88.9674418975776,89.0788142562456,89.1902327795706,89.3018691256319,89.4076972069306,
89.5194208240826,89.6309455635425,89.7423592069936,89.8537046463937,89.9650246763212,
90.0764446943708,90.187910442542,90.2995926613635,90.4050340747232,90.5159923259385,
90.6267854997885,90.7374578203841,90.8480714967823,90.9586521781964,91.0692819971788,
91.106186954104),.UNSPECIFIED.);
#784=B_SPLINE_CURVE_WITH_KNOTS('',3,(#75202,#75203,#75204,#75205,#75206,
#75207,#75208,#75209,#75210,#75211,#75212,#75213,#75214,#75215,#75216,#75217,
#75218,#75219,#75220,#75221,#75222,#75223,#75224,#75225,#75226,#75227,#75228,
#75229,#75230,#75231,#75232,#75233,#75234,#75235,#75236,#75237,#75238,#75239,
#75240,#75241,#75242,#75243,#75244,#75245,#75246,#75247,#75248,#75249,#75250,
#75251,#75252,#75253,#75254,#75255,#75256,#75257,#75258,#75259,#75260,#75261,
#75262),.UNSPECIFIED.,.F.,.F.,(4,3,3,3,3,3,3,3,3,3,3,3,3,3,3,3,3,3,3,3,
4),(-4.09254174883832,-3.98934747117026,-3.88363643282297,-3.77808492915444,
-3.6726592602599,-3.56730087600952,-3.46197396509548,-3.35664276205073,
-3.25120381048226,-3.14570400968359,-3.04002763980351,-2.99201060337769,
-2.88747517765022,-2.78311496418647,-2.67885241980798,-2.57465006492938,
-2.47047050196767,-2.36620671122195,-2.26190327247319,-2.15741710786687,
-2.06549325648379),.UNSPECIFIED.);
#785=B_SPLINE_CURVE_WITH_KNOTS('',3,(#75266,#75267,#75268,#75269,#75270,
#75271,#75272,#75273,#75274,#75275,#75276,#75277,#75278,#75279,#75280,#75281,
#75282,#75283,#75284,#75285,#75286,#75287,#75288,#75289,#75290,#75291,#75292,
#75293,#75294,#75295,#75296,#75297,#75298,#75299),.UNSPECIFIED.,.F.,.F.,
(4,3,3,3,3,3,3,3,3,3,3,4),(0.,0.107971890026954,0.219243757071925,0.327137813760554,
0.435034263883378,0.542962282944035,0.650951076303133,0.759107773599422,
0.867362596774567,0.975816836522539,0.998146826386724,1.11419103802952),
 .UNSPECIFIED.);
#786=B_SPLINE_CURVE_WITH_KNOTS('',3,(#75301,#75302,#75303,#75304,#75305,
#75306,#75307,#75308,#75309,#75310,#75311,#75312,#75313,#75314,#75315,#75316,
#75317,#75318,#75319,#75320,#75321,#75322,#75323,#75324,#75325,#75326,#75327,
#75328,#75329,#75330,#75331,#75332,#75333,#75334,#75335,#75336,#75337,#75338,
#75339,#75340,#75341,#75342,#75343,#75344,#75345,#75346,#75347,#75348,#75349,
#75350,#75351,#75352,#75353,#75354,#75355,#75356,#75357,#75358,#75359,#75360,
#75361,#75362,#75363,#75364,#75365,#75366,#75367,#75368,#75369,#75370,#75371,
#75372,#75373,#75374,#75375,#75376,#75377,#75378,#75379,#75380,#75381,#75382,
#75383,#75384,#75385,#75386,#75387,#75388,#75389,#75390,#75391,#75392,#75393,
#75394,#75395,#75396,#75397,#75398,#75399,#75400,#75401,#75402,#75403,#75404,
#75405,#75406,#75407,#75408,#75409,#75410,#75411,#75412,#75413,#75414,#75415,
#75416,#75417,#75418,#75419,#75420,#75421,#75422,#75423,#75424,#75425,#75426,
#75427,#75428,#75429,#75430,#75431,#75432,#75433,#75434,#75435,#75436,#75437,
#75438,#75439,#75440,#75441,#75442,#75443,#75444,#75445,#75446,#75447,#75448,
#75449,#75450,#75451,#75452,#75453,#75454,#75455,#75456,#75457,#75458,#75459,
#75460,#75461,#75462,#75463,#75464,#75465,#75466,#75467,#75468,#75469,#75470,
#75471,#75472,#75473,#75474,#75475,#75476,#75477,#75478,#75479,#75480,#75481,
#75482,#75483,#75484,#75485,#75486,#75487,#75488,#75489,#75490),
 .UNSPECIFIED.,.F.,.F.,(4,3,3,3,3,3,3,3,3,3,3,3,3,3,3,3,3,3,3,3,3,3,3,3,
3,3,3,3,3,3,3,3,3,3,3,3,3,3,3,3,3,3,3,3,3,3,3,3,3,3,3,3,3,3,3,3,3,3,3,3,
3,3,3,4),(1.11419103844362,1.21719178712621,1.32003180936696,1.42278371743724,
1.52548628532692,1.62817819909424,1.7309676550256,1.83380962645345,1.93683300941319,
1.99629365277347,2.10195062249824,2.20744865406854,2.31282196833917,2.41812869905107,
2.52340471398939,2.62868583588416,2.73407645641426,2.83952870871035,2.94515978418996,
2.9944404791602,3.10012104081475,3.20564648920596,3.31105278134987,3.41639592985287,
3.52171175683583,3.62703604294105,3.7324746359267,3.83797767810928,3.94366338405182,
3.99258730554694,4.09793916383869,4.20312978186129,4.30819381927125,4.41319030347723,
4.51815558391299,4.62312596419388,4.72820798570695,4.83335241117602,4.93868011359328,
4.99073413193368,5.09626132963981,5.20162955424616,5.30687369011875,5.4120517192167,
5.51719971962021,5.62235372499639,5.72761949265099,5.83294800853446,5.93845839412689,
5.98888095832042,6.09439886020279,6.19975815061375,6.30499393635141,6.41016398359831,
6.51530438389174,6.62045118475443,6.72571040049498,6.83103272751,6.93653755417126,
6.98702778470716,7.10330090801871,7.21921658035719,7.33454806250759,7.39737593147595),
 .UNSPECIFIED.);
#787=B_SPLINE_CURVE_WITH_KNOTS('',3,(#75492,#75493,#75494,#75495,#75496,
#75497,#75498,#75499,#75500,#75501),.UNSPECIFIED.,.F.,.F.,(4,1,1,1,1,1,
1,4),(7.39737634520911,7.9851746110939,8.98332143748063,9.98146826386737,
10.9796150902541,11.9777619166408,12.9759087430276,13.6805616523887),
 .UNSPECIFIED.);
#788=B_SPLINE_CURVE_WITH_KNOTS('',3,(#75503,#75504,#75505,#75506,#75507,
#75508,#75509,#75510,#75511,#75512,#75513,#75514,#75515,#75516,#75517,#75518,
#75519,#75520,#75521,#75522,#75523,#75524,#75525,#75526,#75527,#75528,#75529,
#75530,#75531,#75532,#75533,#75534,#75535,#75536,#75537,#75538,#75539,#75540,
#75541,#75542,#75543,#75544,#75545,#75546,#75547,#75548,#75549,#75550,#75551,
#75552,#75553,#75554,#75555,#75556,#75557,#75558,#75559,#75560,#75561,#75562,
#75563,#75564,#75565,#75566,#75567,#75568,#75569,#75570,#75571,#75572,#75573,
#75574,#75575,#75576,#75577,#75578,#75579,#75580,#75581,#75582,#75583,#75584,
#75585,#75586,#75587,#75588,#75589,#75590,#75591,#75592,#75593,#75594,#75595,
#75596,#75597,#75598,#75599,#75600,#75601,#75602,#75603,#75604,#75605,#75606,
#75607,#75608,#75609,#75610,#75611,#75612,#75613,#75614,#75615,#75616,#75617,
#75618,#75619,#75620,#75621,#75622,#75623,#75624,#75625,#75626,#75627,#75628,
#75629,#75630,#75631,#75632,#75633,#75634,#75635,#75636,#75637,#75638,#75639,
#75640,#75641,#75642,#75643,#75644,#75645,#75646,#75647,#75648,#75649,#75650,
#75651,#75652,#75653,#75654,#75655,#75656,#75657,#75658,#75659,#75660,#75661,
#75662,#75663,#75664,#75665,#75666,#75667,#75668,#75669,#75670,#75671,#75672,
#75673,#75674,#75675,#75676,#75677,#75678,#75679,#75680,#75681,#75682,#75683,
#75684,#75685,#75686,#75687,#75688,#75689,#75690,#75691,#75692),
 .UNSPECIFIED.,.F.,.F.,(4,3,3,3,3,3,3,3,3,3,3,3,3,3,3,3,3,3,3,3,3,3,3,3,
3,3,3,3,3,3,3,3,3,3,3,3,3,3,3,3,3,3,3,3,3,3,3,3,3,3,3,3,3,3,3,3,3,3,3,3,
3,3,3,4),(13.6805618202843,13.8080138554844,13.9373859483242,13.9740555694143,
14.0795516490623,14.1848886090792,14.2901014205325,14.3952481069312,14.5003647949379,
14.6054875668125,14.7107224370753,14.8160202021566,14.9215003896649,14.972202395801,
15.0776983156651,15.1830351147283,15.2882477642988,15.3933942883333,15.4985108137438,
15.6036334230391,15.7088681318705,15.8141657359377,15.9196457647817,15.9703492221878,
16.0758450672949,16.181181789708,16.2863943601952,16.3915408036808,16.4966572471969,
16.6017797733711,16.707014397786,16.8123119165726,16.9177918596926,16.9684960485745,
17.0739919802754,17.179328790682,17.2845414508035,17.38968798489,17.4948045198368,
17.5999271381349,17.7051618550945,17.8104594668023,17.915939502448,17.9666428749613,
18.0721387779979,18.1774755594657,18.2826881903856,18.3878346951245,18.4929512006224,
18.5980737894155,18.7033084769877,18.8086060593322,18.9140860659618,18.964789701348,
19.0703011871416,19.1756535393357,19.2808816837827,19.3860436404998,19.4911755122156,
19.596313357183,19.7015632702855,19.8068759332889,19.9123712558797,19.9637469595683),
 .UNSPECIFIED.);
#789=B_SPLINE_CURVE_WITH_KNOTS('',3,(#75694,#75695,#75696,#75697,#75698,
#75699,#75700,#75701,#75702,#75703,#75704,#75705,#75706,#75707,#75708,#75709,
#75710,#75711,#75712,#75713,#75714,#75715,#75716,#75717,#75718,#75719,#75720,
#75721,#75722,#75723,#75724,#75725,#75726,#75727,#75728,#75729,#75730,#75731,
#75732,#75733,#75734,#75735,#75736,#75737,#75738,#75739,#75740,#75741,#75742,
#75743,#75744,#75745,#75746,#75747,#75748,#75749,#75750,#75751,#75752,#75753,
#75754,#75755,#75756,#75757,#75758,#75759,#75760,#75761,#75762,#75763,#75764,
#75765,#75766,#75767,#75768,#75769,#75770,#75771,#75772,#75773,#75774,#75775,
#75776,#75777,#75778,#75779,#75780,#75781,#75782,#75783,#75784,#75785,#75786,
#75787,#75788,#75789,#75790,#75791,#75792,#75793,#75794,#75795,#75796,#75797,
#75798,#75799,#75800,#75801,#75802,#75803,#75804,#75805,#75806,#75807,#75808,
#75809,#75810,#75811,#75812,#75813,#75814,#75815,#75816,#75817,#75818,#75819,
#75820,#75821,#75822,#75823,#75824,#75825,#75826,#75827,#75828,#75829,#75830,
#75831,#75832,#75833,#75834,#75835,#75836,#75837,#75838,#75839,#75840,#75841,
#75842,#75843,#75844,#75845,#75846,#75847,#75848,#75849,#75850,#75851,#75852,
#75853,#75854,#75855,#75856,#75857,#75858,#75859,#75860,#75861,#75862,#75863,
#75864,#75865,#75866,#75867,#75868,#75869,#75870,#75871,#75872,#75873,#75874,
#75875,#75876,#75877,#75878,#75879,#75880,#75881,#75882,#75883),
 .UNSPECIFIED.,.F.,.F.,(4,3,3,3,3,3,3,3,3,3,3,3,3,3,3,3,3,3,3,3,3,3,3,3,
3,3,3,3,3,3,3,3,3,3,3,3,3,3,3,3,3,3,3,3,3,3,3,3,3,3,3,3,3,3,3,3,3,3,3,3,
3,3,3,4),(19.9637469598682,20.0692273547104,20.1745486411723,20.279745835274,
20.3848769652241,20.4899781819352,20.5950855919875,20.7003051304565,20.8055877081546,
20.911052473179,20.9610833541215,21.0665792569406,21.1719160381134,21.2771286686244,
21.382275172884,21.4873916778326,21.5925142660069,21.6977489528586,21.8030465344233,
21.9085265401897,21.9592301805082,22.0647260827278,22.170062863275,22.2752754931247,
22.3804219967011,22.4855385009456,22.5906610883958,22.6958957744983,22.8011933552983,
22.9066733602838,22.9573770068949,23.0628729107958,23.1682096930542,23.2734223246508,
23.3785688299953,23.4836853360264,23.5888079252789,23.6940426131956,23.7993401958192,
23.9048202026235,23.9555238332817,24.0610197363911,24.1663565178484,24.2715691486333,
24.3767156531599,24.4818321583686,24.5869547467952,24.6921894338859,24.7974870156826,
24.9029670216672,24.9536706596684,25.0591665627647,25.1645033442062,25.2697159749714,
25.374862479476,25.4799789846599,25.5851015730596,25.6903362601201,25.7956338418846,
25.9011138478342,25.9518174860552,26.0810388351796,26.2084013336569,26.2469320954389),
 .UNSPECIFIED.);
#790=B_SPLINE_CURVE_WITH_KNOTS('',3,(#75885,#75886,#75887,#75888,#75889,
#75890,#75891,#75892,#75893,#75894),.UNSPECIFIED.,.F.,.F.,(4,1,1,1,1,1,
1,4),(26.2469322667479,26.9499643124419,27.9481111388286,28.9462579652154,
29.9444047916021,30.9425516179888,31.9406984443756,32.5301175739274),
 .UNSPECIFIED.);
#791=B_SPLINE_CURVE_WITH_KNOTS('',3,(#75896,#75897,#75898,#75899,#75900,
#75901,#75902,#75903,#75904,#75905,#75906,#75907,#75908,#75909,#75910,#75911,
#75912,#75913,#75914,#75915,#75916,#75917,#75918,#75919,#75920,#75921,#75922,
#75923,#75924,#75925,#75926,#75927,#75928,#75929,#75930,#75931,#75932,#75933,
#75934,#75935,#75936,#75937,#75938,#75939,#75940,#75941,#75942,#75943,#75944,
#75945,#75946,#75947,#75948,#75949,#75950,#75951,#75952,#75953,#75954,#75955,
#75956,#75957,#75958,#75959,#75960,#75961,#75962,#75963,#75964,#75965,#75966,
#75967,#75968,#75969,#75970,#75971,#75972,#75973,#75974,#75975,#75976,#75977,
#75978,#75979,#75980,#75981,#75982,#75983,#75984,#75985,#75986,#75987,#75988,
#75989,#75990,#75991,#75992,#75993,#75994,#75995,#75996,#75997,#75998,#75999,
#76000,#76001,#76002,#76003,#76004,#76005,#76006,#76007,#76008,#76009,#76010,
#76011,#76012,#76013,#76014,#76015,#76016,#76017,#76018,#76019,#76020,#76021,
#76022,#76023,#76024,#76025,#76026,#76027,#76028,#76029,#76030,#76031,#76032,
#76033,#76034,#76035,#76036,#76037,#76038,#76039,#76040,#76041,#76042,#76043,
#76044,#76045,#76046,#76047,#76048,#76049,#76050,#76051,#76052,#76053,#76054,
#76055,#76056,#76057,#76058,#76059,#76060,#76061,#76062,#76063,#76064,#76065,
#76066,#76067,#76068,#76069,#76070,#76071,#76072,#76073,#76074,#76075,#76076,
#76077,#76078,#76079,#76080,#76081,#76082,#76083,#76084,#76085),
 .UNSPECIFIED.,.F.,.F.,(4,3,3,3,3,3,3,3,3,3,3,3,3,3,3,3,3,3,3,3,3,3,3,3,
3,3,3,3,3,3,3,3,3,3,3,3,3,3,3,3,3,3,3,3,3,3,3,3,3,3,3,3,3,3,3,3,3,3,3,3,
3,3,3,4),(32.5301179915019,32.6456707590869,32.7616131287804,32.8780966879654,
32.9388452707623,33.0443411739821,33.1496779555496,33.2548905864443,33.3600370910804,
33.4651535963978,33.5702761849327,33.6755108721297,33.7808084540318,33.8862884601192,
33.9369920971491,34.0424880003695,34.1478247819377,34.253037412833,34.3581839174697,
34.4633004227878,34.5684230113232,34.6736576985209,34.7789552804236,34.8844352865115,
34.9351389235358,35.0406348267566,35.1459716083252,35.251184239221,35.3563307438581,
35.4614472491767,35.5665698377125,35.6718045249107,35.7771021068139,35.8825821129023,
35.9332857499225,36.038781653143,36.1441184347112,36.2493310656066,36.3544775702434,
36.4595940755615,36.564716664097,36.6699513512947,36.7752489331975,36.8807289392856,
36.9314325763093,37.0369284795299,37.1422652610982,37.2474778919937,37.3526243966306,
37.4577409019488,37.5628634904844,37.6680981776822,37.7733957595852,37.8788757656733,
37.929579402696,38.0336606369063,38.1375625429156,38.2413648015755,38.3451054038156,
38.4488222501643,38.552612207333,38.6564423147378,38.7604271016251,38.813302881107),
 .UNSPECIFIED.);
#792=B_SPLINE_CURVE_WITH_KNOTS('',3,(#76087,#76088,#76089,#76090,#76091,
#76092,#76093,#76094,#76095,#76096,#76097),.UNSPECIFIED.,.F.,.F.,(4,1,1,
1,1,1,1,1,4),(38.813302881107,38.9277262290827,39.9258730554695,40.9240198818562,
41.9221667082429,42.9203135346297,43.9184603610164,44.9166071874032,45.0964881882866),
 .UNSPECIFIED.);
#793=B_SPLINE_CURVE_WITH_KNOTS('',3,(#76099,#76100,#76101,#76102,#76103,
#76104,#76105,#76106,#76107,#76108),.UNSPECIFIED.,.F.,.F.,(4,1,1,1,1,1,
1,4),(45.0964881882866,45.9147540137899,46.9129008401766,47.9110476665634,
48.9091944929501,49.9073413193368,50.9054881457236,51.3796715846493),
 .UNSPECIFIED.);
#794=B_SPLINE_CURVE_WITH_KNOTS('',3,(#76110,#76111,#76112,#76113,#76114,
#76115,#76116,#76117,#76118,#76119,#76120,#76121,#76122,#76123,#76124,#76125,
#76126,#76127,#76128,#76129,#76130,#76131,#76132,#76133,#76134,#76135,#76136,
#76137,#76138,#76139,#76140,#76141,#76142,#76143,#76144,#76145,#76146,#76147,
#76148,#76149,#76150,#76151,#76152,#76153,#76154,#76155,#76156,#76157,#76158,
#76159,#76160,#76161,#76162,#76163,#76164,#76165,#76166,#76167,#76168,#76169,
#76170,#76171,#76172,#76173,#76174,#76175,#76176,#76177,#76178,#76179,#76180,
#76181,#76182,#76183,#76184,#76185,#76186,#76187,#76188,#76189,#76190,#76191,
#76192,#76193,#76194,#76195,#76196,#76197,#76198,#76199,#76200,#76201,#76202,
#76203,#76204,#76205,#76206,#76207,#76208,#76209,#76210,#76211,#76212,#76213,
#76214,#76215,#76216,#76217,#76218,#76219,#76220,#76221,#76222,#76223,#76224,
#76225,#76226,#76227,#76228,#76229,#76230,#76231,#76232,#76233,#76234,#76235,
#76236,#76237,#76238,#76239,#76240,#76241,#76242,#76243,#76244,#76245,#76246,
#76247,#76248,#76249,#76250,#76251,#76252,#76253,#76254,#76255,#76256,#76257,
#76258,#76259,#76260,#76261,#76262,#76263,#76264,#76265,#76266,#76267,#76268,
#76269,#76270,#76271,#76272,#76273,#76274,#76275,#76276,#76277,#76278,#76279,
#76280,#76281,#76282,#76283,#76284,#76285,#76286,#76287,#76288,#76289,#76290,
#76291,#76292,#76293,#76294,#76295,#76296,#76297,#76298,#76299),
 .UNSPECIFIED.,.F.,.F.,(4,3,3,3,3,3,3,3,3,3,3,3,3,3,3,3,3,3,3,3,3,3,3,3,
3,3,3,3,3,3,3,3,3,3,3,3,3,3,3,3,3,3,3,3,3,3,3,3,3,3,3,3,3,3,3,3,3,3,3,3,
3,3,3,4),(51.3796734954662,51.4887071556465,51.5979949885878,51.7074131825927,
51.8171173718269,51.9036349721103,52.0091308753307,52.1144676568988,52.2196802877941,
52.3248267924308,52.4299432977489,52.5350658862844,52.640300573482,52.7455981553849,
52.8510781614729,52.901781798497,53.0072777017168,53.1126144832843,53.217827114179,
53.3229736188151,53.4280901241326,53.5332127126676,53.6384473998648,53.743744981767,
53.8492249878544,53.8999286248838,54.0054245281066,54.1107613096772,54.2159739405749,
54.3211204452141,54.4262369505345,54.5313595390723,54.6365942262723,54.7418918081774,
54.8473718142677,54.8980754512705,55.0035713544892,55.1089081360556,55.2141207669493,
55.3192672715845,55.4243837769011,55.529506365435,55.6347410526312,55.7400386345324,
55.8455186406191,55.8962222776573,56.0017181808736,56.1070549624377,56.2122675933288,
56.3174140979613,56.422530603275,56.5276531918063,56.6328878789998,56.7381854608983,
56.843665466982,56.894369104044,56.9984595657844,57.1024080693009,57.2062527224879,
57.3100314827545,57.413817463461,57.5176075792081,57.6214910298516,57.6628588026458),
 .UNSPECIFIED.);
#795=B_SPLINE_CURVE_WITH_KNOTS('',3,(#76301,#76302,#76303,#76304,#76305,
#76306,#76307,#76308,#76309,#76310,#76311),.UNSPECIFIED.,.F.,.F.,(4,1,1,
1,1,1,1,1,4),(57.6628588026458,57.8925159304307,58.8906627568175,59.8888095832042,
60.8869564095909,61.8851032359777,62.8832500623644,63.8813968887512,63.9460441098254),
 .UNSPECIFIED.);
#796=B_SPLINE_CURVE_WITH_KNOTS('',3,(#76313,#76314,#76315,#76316,#76317,
#76318,#76319,#76320,#76321,#76322,#76323,#76324,#76325,#76326,#76327,#76328,
#76329,#76330,#76331,#76332,#76333,#76334,#76335,#76336,#76337,#76338,#76339,
#76340,#76341,#76342,#76343,#76344,#76345,#76346,#76347,#76348,#76349,#76350,
#76351,#76352,#76353,#76354,#76355,#76356,#76357,#76358,#76359,#76360,#76361,
#76362,#76363,#76364,#76365,#76366,#76367,#76368,#76369,#76370,#76371,#76372,
#76373,#76374,#76375,#76376,#76377,#76378,#76379,#76380,#76381,#76382,#76383,
#76384,#76385,#76386,#76387,#76388,#76389,#76390,#76391,#76392,#76393,#76394,
#76395,#76396,#76397,#76398,#76399,#76400,#76401,#76402,#76403,#76404,#76405,
#76406,#76407,#76408,#76409,#76410,#76411,#76412,#76413,#76414,#76415,#76416,
#76417,#76418,#76419,#76420,#76421,#76422,#76423,#76424,#76425,#76426,#76427,
#76428,#76429,#76430,#76431,#76432,#76433,#76434,#76435,#76436,#76437,#76438,
#76439,#76440,#76441,#76442,#76443,#76444,#76445,#76446,#76447,#76448,#76449,
#76450,#76451,#76452,#76453,#76454,#76455,#76456,#76457,#76458,#76459,#76460,
#76461,#76462,#76463,#76464,#76465,#76466,#76467,#76468,#76469,#76470,#76471,
#76472,#76473,#76474,#76475,#76476,#76477,#76478,#76479,#76480,#76481,#76482,
#76483,#76484,#76485,#76486,#76487,#76488,#76489,#76490,#76491,#76492,#76493,
#76494,#76495,#76496,#76497,#76498,#76499),.UNSPECIFIED.,.F.,.F.,(4,3,3,
3,3,3,3,3,3,3,3,3,3,3,3,3,3,3,3,3,3,3,3,3,3,3,3,3,3,3,3,3,3,3,3,3,3,3,3,
3,3,3,3,3,3,3,3,3,3,3,3,3,3,3,3,3,3,3,3,3,3,3,4),(63.9460441098254,64.050525963831,
64.1548391807715,64.2590586452409,64.3632218680578,64.4673662827088,64.5716035009599,
64.6758837527691,64.7803585946505,64.8795437151379,64.9850396180399,65.0903763992768,
65.1955890298238,65.3007355341018,65.4058520390515,65.5109746272094,65.6162093140186,
65.721506895526,65.8269869012125,65.8776905415246,65.9831864493903,66.0885232356215,
66.1937358711839,66.2988823804876,66.4039988904652,66.509121483646,66.6143561754361,
66.7196537619078,66.8251337724805,66.8758373679114,66.9813332627005,67.0866700358464,
67.1918826583736,67.2970291546803,67.4021456517187,67.507268232037,67.6125029111667,
67.7178004850744,67.823280483364,67.8739841942981,67.979480098073,68.0848168801108,
68.1900295113507,68.2951760162542,68.4002925217617,68.5054151104092,68.610649797603,
68.7159473794359,68.8214273853541,68.8721310206848,68.9776269533426,69.0829637644887,
69.1881764250249,69.2933229593248,69.398439494284,69.5035621123933,69.6087968288627,
69.7140944399076,69.8195744746314,69.8702778470716,69.9912176372233,70.1111669584549,
70.2292291731328),.UNSPECIFIED.);
#797=B_SPLINE_CURVE_WITH_KNOTS('',3,(#76501,#76502,#76503,#76504,#76505,
#76506,#76507,#76508,#76509,#76510),.UNSPECIFIED.,.F.,.F.,(4,1,1,1,1,1,
1,4),(70.229229417005,70.8684246734583,71.8665714998451,72.8647183262318,
73.8628651526185,74.8610119790053,75.859158805392,76.5124147241846),
 .UNSPECIFIED.);
#798=B_SPLINE_CURVE_WITH_KNOTS('',3,(#76512,#76513,#76514,#76515,#76516,
#76517,#76518,#76519,#76520,#76521,#76522,#76523,#76524,#76525,#76526,#76527,
#76528,#76529,#76530,#76531,#76532,#76533,#76534,#76535,#76536,#76537,#76538,
#76539,#76540,#76541,#76542,#76543,#76544,#76545,#76546,#76547,#76548,#76549,
#76550,#76551,#76552,#76553,#76554,#76555,#76556,#76557,#76558,#76559,#76560,
#76561,#76562,#76563,#76564,#76565,#76566,#76567,#76568,#76569,#76570,#76571,
#76572,#76573,#76574,#76575,#76576,#76577,#76578,#76579,#76580,#76581,#76582,
#76583,#76584,#76585,#76586,#76587,#76588,#76589,#76590,#76591,#76592,#76593,
#76594,#76595,#76596,#76597,#76598,#76599,#76600,#76601,#76602,#76603,#76604,
#76605,#76606,#76607,#76608,#76609,#76610,#76611,#76612,#76613,#76614,#76615,
#76616,#76617,#76618,#76619,#76620,#76621,#76622,#76623,#76624,#76625,#76626,
#76627,#76628,#76629,#76630,#76631,#76632,#76633,#76634,#76635,#76636,#76637,
#76638,#76639,#76640,#76641,#76642,#76643,#76644,#76645,#76646,#76647,#76648,
#76649,#76650),.UNSPECIFIED.,.F.,.F.,(4,3,3,3,3,3,3,3,3,3,3,3,3,3,3,3,3,
3,3,3,3,3,3,3,3,3,3,3,3,3,3,3,3,3,3,3,3,3,3,3,3,3,3,3,3,3,4),(76.5124149635497,
76.6335427431329,76.755837417112,76.8573056317787,76.9628043403963,77.0681439068555,
77.1733592794405,77.2785084974948,77.3836276841624,77.488752918151,77.5939901791019,
77.6992902976895,77.8047727570283,77.8554524581655,77.9609542845702,78.0662970454053,
78.17151570875,78.276668275278,78.3817908625963,78.4869195439332,78.5921602982041,
78.6974639414213,78.8029499357427,78.8535992845522,78.9590728007151,79.0643871541541,
79.1695774039509,79.2747015691714,79.3797958096304,79.4848962408019,79.5901090829246,
79.6953849654392,79.8008437246019,79.8517461109389,79.9572667741261,80.0626281974763,
80.1678651799042,80.2730358426097,80.3781762780868,80.4833225342001,80.5885803347549,
80.6939007480483,80.7994029135444,80.8498929373257,80.972024192404,81.0930688950015,
81.1967061267808),.UNSPECIFIED.);
#799=B_SPLINE_CURVE_WITH_KNOTS('',3,(#76654,#76655,#76656,#76657,#76658,
#76659,#76660,#76661,#76662,#76663,#76664,#76665,#76666,#76667,#76668,#76669,
#76670,#76671,#76672,#76673,#76674,#76675,#76676,#76677,#76678,#76679,#76680,
#76681,#76682,#76683,#76684,#76685,#76686,#76687,#76688,#76689,#76690,#76691,
#76692,#76693,#76694,#76695,#76696,#76697,#76698,#76699,#76700,#76701,#76702,
#76703,#76704,#76705,#76706,#76707,#76708,#76709,#76710,#76711,#76712,#76713,
#76714,#76715,#76716,#76717,#76718,#76719,#76720,#76721,#76722,#76723,#76724,
#76725,#76726,#76727,#76728,#76729,#76730,#76731,#76732,#76733,#76734,#76735,
#76736,#76737,#76738,#76739,#76740,#76741,#76742,#76743,#76744,#76745,#76746,
#76747,#76748,#76749,#76750,#76751,#76752,#76753,#76754,#76755,#76756,#76757,
#76758,#76759,#76760,#76761,#76762,#76763,#76764,#76765,#76766,#76767,#76768),
 .UNSPECIFIED.,.F.,.F.,(4,3,3,3,3,3,3,3,3,3,3,3,3,3,3,3,3,3,3,3,3,3,3,3,
3,3,3,3,3,3,3,3,3,3,3,3,3,3,4),(-83.261823785886,-83.1517588372496,-83.0413517915619,
-82.930757367669,-82.8198433883014,-82.7789600267829,-82.6732910907865,
-82.5677808221992,-82.4623949729488,-82.3570755146399,-82.2517866003674,
-82.1464924281016,-82.0410888596141,-81.9356235523786,-81.8299800036617,
-81.7816231589903,-81.6759325426703,-81.5703968024453,-81.4649799626522,
-81.3596260975942,-81.2542994029756,-81.1489641158244,-81.0435146406177,
-80.938000619518,-80.8323045173012,-80.7842862911978,-80.6789235796683,
-80.5737218686868,-80.4686464770282,-80.3636384661016,-80.2586615036662,
-80.1536793031293,-80.0485855762287,-79.9434293428101,-79.8380904225242,
-79.7869494234052,-79.6576514134494,-79.5302108335803,-79.4907655987199),
 .UNSPECIFIED.);
#800=B_SPLINE_CURVE_WITH_KNOTS('',3,(#76770,#76771,#76772,#76773,#76774,
#76775,#76776,#76777,#76778,#76779),.UNSPECIFIED.,.F.,.F.,(4,1,1,1,1,1,
1,4),(-79.4907654349934,-78.7896125556126,-77.7922756878201,-76.7949388200275,
-75.7976019522349,-74.8002650844424,-73.8029282166498,-73.2075801278138),
 .UNSPECIFIED.);
#801=B_SPLINE_CURVE_WITH_KNOTS('',3,(#76781,#76782,#76783,#76784,#76785,
#76786,#76787,#76788,#76789,#76790,#76791,#76792,#76793,#76794,#76795,#76796,
#76797,#76798,#76799,#76800,#76801,#76802,#76803,#76804,#76805,#76806,#76807,
#76808,#76809,#76810,#76811,#76812,#76813,#76814,#76815,#76816,#76817,#76818,
#76819,#76820,#76821,#76822,#76823,#76824,#76825,#76826,#76827,#76828,#76829,
#76830,#76831,#76832,#76833,#76834,#76835,#76836,#76837,#76838,#76839,#76840,
#76841,#76842,#76843,#76844,#76845,#76846,#76847,#76848,#76849,#76850,#76851,
#76852,#76853,#76854,#76855,#76856,#76857,#76858,#76859,#76860,#76861,#76862,
#76863,#76864,#76865,#76866,#76867,#76868,#76869,#76870,#76871,#76872,#76873,
#76874,#76875,#76876,#76877,#76878,#76879,#76880,#76881,#76882,#76883,#76884,
#76885,#76886,#76887,#76888,#76889,#76890,#76891,#76892,#76893,#76894,#76895,
#76896,#76897,#76898,#76899,#76900,#76901,#76902,#76903,#76904,#76905,#76906,
#76907,#76908,#76909,#76910,#76911,#76912,#76913,#76914,#76915,#76916,#76917,
#76918,#76919,#76920,#76921,#76922,#76923,#76924,#76925,#76926,#76927,#76928,
#76929,#76930,#76931,#76932,#76933,#76934,#76935,#76936,#76937,#76938,#76939,
#76940,#76941,#76942,#76943,#76944,#76945,#76946,#76947,#76948,#76949,#76950,
#76951,#76952,#76953,#76954,#76955,#76956,#76957,#76958,#76959,#76960,#76961,
#76962,#76963,#76964,#76965,#76966,#76967,#76968,#76969,#76970),
 .UNSPECIFIED.,.F.,.F.,(4,3,3,3,3,3,3,3,3,3,3,3,3,3,3,3,3,3,3,3,3,3,3,3,
3,3,3,3,3,3,3,3,3,3,3,3,3,3,3,3,3,3,3,3,3,3,3,3,3,3,3,3,3,3,3,3,3,3,3,3,
3,3,3,4),(-73.2075796958808,-73.091556451448,-72.9751182134163,-72.8581229582674,
-72.8055913488572,-72.7000843592375,-72.594736238552,-72.4895119913637,
-72.38435368872,-72.2792252221004,-72.1740905272145,-72.0688438405957,-71.963534153129,
-71.8580426246082,-71.8082544810647,-71.7027481426044,-71.5974006878884,
-71.4921771253551,-71.3870195185762,-71.2818917579841,-71.1767577782527,
-71.071511815753,-70.9662028585869,-70.8607120622803,-70.8109176132721,
-70.7054106731065,-70.6000626073486,-70.4948384229603,-70.3896801879757,
-70.284551793783,-70.1794171760054,-70.0741705730911,-69.9688609732197,
-69.8633695374144,-69.8135807454795,-69.7080739686073,-69.602726067379,
-69.4975020485289,-69.39234397961,-69.2872157517546,-69.1820813003305,-69.076834862647,
-68.971525427607,-68.8660341542782,-68.816243877687,-68.7107371737072,-68.605389347242,
-68.5001654055624,-68.3950074152649,-68.289879267364,-68.1847448971112,
-68.079498541892,-67.9741891901756,-67.868698000628,-67.8189070098944,-67.7147383019953,
-67.6107484692928,-67.506858120488,-67.4030293549668,-67.2992243609191,
-67.1953437258928,-67.0914232330471,-66.9873412561956,-66.9243948210849),
 .UNSPECIFIED.);
#802=B_SPLINE_CURVE_WITH_KNOTS('',3,(#76972,#76973,#76974,#76975,#76976,
#76977,#76978,#76979,#76980,#76981,#76982,#76983,#76984,#76985,#76986,#76987,
#76988,#76989,#76990,#76991,#76992,#76993,#76994,#76995,#76996,#76997,#76998,
#76999,#77000,#77001,#77002,#77003,#77004,#77005,#77006,#77007,#77008,#77009,
#77010,#77011,#77012,#77013,#77014,#77015,#77016,#77017,#77018,#77019,#77020,
#77021,#77022,#77023,#77024,#77025,#77026,#77027,#77028,#77029,#77030,#77031,
#77032,#77033,#77034,#77035,#77036,#77037,#77038,#77039,#77040,#77041,#77042,
#77043,#77044,#77045,#77046,#77047,#77048,#77049,#77050,#77051,#77052,#77053,
#77054,#77055,#77056,#77057,#77058,#77059,#77060,#77061,#77062,#77063,#77064,
#77065,#77066,#77067,#77068,#77069,#77070,#77071,#77072,#77073,#77074,#77075,
#77076,#77077,#77078,#77079,#77080,#77081,#77082,#77083,#77084,#77085,#77086,
#77087,#77088,#77089,#77090,#77091,#77092,#77093,#77094,#77095,#77096,#77097,
#77098,#77099,#77100,#77101,#77102,#77103,#77104,#77105,#77106,#77107,#77108,
#77109,#77110,#77111,#77112,#77113,#77114,#77115,#77116,#77117,#77118,#77119,
#77120,#77121,#77122,#77123,#77124,#77125,#77126,#77127,#77128,#77129,#77130,
#77131,#77132,#77133,#77134,#77135,#77136,#77137,#77138,#77139,#77140,#77141,
#77142,#77143,#77144,#77145,#77146,#77147,#77148,#77149,#77150,#77151,#77152,
#77153,#77154,#77155,#77156,#77157,#77158,#77159,#77160,#77161),
 .UNSPECIFIED.,.F.,.F.,(4,3,3,3,3,3,3,3,3,3,3,3,3,3,3,3,3,3,3,3,3,3,3,3,
3,3,3,3,3,3,3,3,3,3,3,3,3,3,3,3,3,3,3,3,3,3,3,3,3,3,3,3,3,3,3,3,3,3,3,3,
3,3,3,4),(-66.9243948206342,-66.8215701421018,-66.7160633807799,-66.6107154958515,
-66.505491494335,-66.4003334433823,-66.2952052340995,-66.1900708018291,
-66.084824384052,-65.9795149693774,-65.8740237169125,-65.8242332743093,
-65.7187265202069,-65.6133786427231,-65.5081546489489,-65.4029966059188,
-65.2978684047274,-65.1927339807054,-65.0874875713589,-64.9821781652316,
-64.8766869214049,-64.8268964065167,-64.7213896402397,-64.6160417503741,
-64.5108177439724,-64.4056596881695,-64.3005314740794,-64.1953970370521,
-64.0901506146277,-63.9848411953617,-63.8793499384404,-63.8295595387242,
-63.7240527773937,-63.6187048925305,-63.5134808911892,-63.4083228404798,
-63.3031946315083,-63.1980601996171,-63.0928137823199,-62.9875043681835,
-62.8820131163417,-62.8322226709316,-62.72671591014,-62.621368025841,-62.5161440250985,
-62.4109859750092,-62.3058577666781,-62.2007233354468,-62.0954769188346,
-61.9901675053986,-61.8846762542736,-61.834885803139,-61.7293790406761,
-61.624031154676,-61.5188071521967,-61.4136491003493,-61.3085208902418,
-61.203386457218,-61.0981400388015,-60.9928306235517,-60.8873393706174,
-60.8375489353465,-60.6852937514664,-60.6412095134546),.UNSPECIFIED.);
#803=B_SPLINE_CURVE_WITH_KNOTS('',3,(#77163,#77164,#77165,#77166,#77167,
#77168,#77169,#77170,#77171,#77172),.UNSPECIFIED.,.F.,.F.,(4,1,1,1,1,1,
1,4),(-60.6412060917588,-59.8402120675539,-58.8428751997613,-57.8455383319688,
-56.8482014641762,-55.8508645963836,-54.8535277285911,-54.358024206275),
 .UNSPECIFIED.);
#804=B_SPLINE_CURVE_WITH_KNOTS('',3,(#77174,#77175,#77176,#77177,#77178,
#77179,#77180,#77181,#77182,#77183),.UNSPECIFIED.,.F.,.F.,(4,1,1,1,1,1,
1,4),(-54.358024206275,-53.8561908607985,-52.8588539930059,-51.8615171252134,
-50.8641802574208,-49.8668433896283,-48.8695065218357,-48.0748417313677),
 .UNSPECIFIED.);
#805=B_SPLINE_CURVE_WITH_KNOTS('',3,(#77185,#77186,#77187,#77188,#77189,
#77190,#77191,#77192,#77193,#77194,#77195,#77196,#77197,#77198,#77199,#77200,
#77201,#77202,#77203,#77204,#77205,#77206,#77207,#77208,#77209,#77210,#77211,
#77212,#77213,#77214,#77215,#77216,#77217,#77218,#77219,#77220,#77221,#77222,
#77223,#77224,#77225,#77226,#77227,#77228,#77229,#77230,#77231,#77232,#77233,
#77234,#77235,#77236,#77237,#77238,#77239,#77240,#77241,#77242,#77243,#77244,
#77245,#77246,#77247,#77248,#77249,#77250,#77251,#77252,#77253,#77254,#77255,
#77256,#77257,#77258,#77259,#77260,#77261,#77262,#77263,#77264,#77265,#77266,
#77267,#77268,#77269,#77270,#77271,#77272,#77273,#77274,#77275,#77276,#77277,
#77278,#77279,#77280,#77281,#77282,#77283,#77284,#77285,#77286,#77287,#77288,
#77289,#77290,#77291,#77292,#77293,#77294,#77295,#77296,#77297,#77298,#77299,
#77300,#77301,#77302,#77303,#77304,#77305,#77306,#77307,#77308,#77309,#77310,
#77311,#77312,#77313,#77314,#77315,#77316,#77317,#77318,#77319,#77320,#77321,
#77322,#77323,#77324,#77325,#77326,#77327,#77328,#77329,#77330,#77331,#77332,
#77333,#77334,#77335,#77336,#77337,#77338,#77339,#77340,#77341,#77342,#77343,
#77344,#77345,#77346,#77347,#77348,#77349,#77350,#77351,#77352,#77353,#77354,
#77355,#77356,#77357,#77358,#77359,#77360,#77361,#77362,#77363,#77364,#77365,
#77366,#77367,#77368,#77369,#77370,#77371,#77372,#77373,#77374),
 .UNSPECIFIED.,.F.,.F.,(4,3,3,3,3,3,3,3,3,3,3,3,3,3,3,3,3,3,3,3,3,3,3,3,
3,3,3,3,3,3,3,3,3,3,3,3,3,3,3,3,3,3,3,3,3,3,3,3,3,3,3,3,3,3,3,3,3,3,3,3,
3,3,3,4),(-48.0748388990954,-47.9249917028415,-47.8721696540431,-47.7666628922655,
-47.6613150069605,-47.5560910051876,-47.4509329540531,-47.3458047446638,
-47.2406703123627,-47.1354238946705,-47.0301144801472,-46.9246232279348,
-46.8748327862506,-46.7693260244729,-46.6639781391679,-46.5587541373949,
-46.4535960862603,-46.3484678768709,-46.2433334445698,-46.1380870268776,
-46.0327776123541,-45.9272863601416,-45.877495918458,-45.7719891566803,
-45.6666412713754,-45.5614172696023,-45.4562592184678,-45.3511310090785,
-45.2459965767774,-45.1407501590852,-45.0354407445618,-44.9299494923494,
-44.8801590506654,-44.7746522888878,-44.6693044035828,-44.5640804018098,
-44.4589223506753,-44.353794141286,-44.248659708985,-44.1434132912928,-44.0381038767694,
-43.932612624557,-43.8828221828729,-43.7773154210952,-43.6719675357902,
-43.5667435340172,-43.4615854828827,-43.3564572734934,-43.2513228411923,
-43.1460764235,-43.0407670089766,-42.9352757567642,-42.8854853150803,-42.7799785533026,
-42.6746306679976,-42.5694066662245,-42.46424861509,-42.3591204057007,-42.2539859733997,
-42.1487395557075,-42.043430141184,-41.9379388889716,-41.8881484472877,
-41.7916535919158),.UNSPECIFIED.);
#806=B_SPLINE_CURVE_WITH_KNOTS('',3,(#77376,#77377,#77378,#77379,#77380,
#77381,#77382,#77383,#77384,#77385),.UNSPECIFIED.,.F.,.F.,(4,1,1,1,1,1,
1,4),(-41.7916448301768,-40.8908115794952,-39.8934747117026,-38.89613784391,
-37.8988009761175,-36.9014641083249,-35.9041272405323,-35.5084682847363),
 .UNSPECIFIED.);
#807=B_SPLINE_CURVE_WITH_KNOTS('',3,(#77387,#77388,#77389,#77390,#77391,
#77392,#77393,#77394,#77395,#77396),.UNSPECIFIED.,.F.,.F.,(4,1,1,1,1,1,
1,4),(-35.5084682847363,-34.9067903727398,-33.9094535049472,-32.9121166371546,
-31.9147797693621,-30.9174429015695,-29.9201060337769,-29.2252829775567),
 .UNSPECIFIED.);
#808=B_SPLINE_CURVE_WITH_KNOTS('',3,(#77398,#77399,#77400,#77401,#77402,
#77403,#77404,#77405,#77406,#77407,#77408,#77409,#77410,#77411,#77412,#77413,
#77414,#77415,#77416,#77417,#77418,#77419,#77420,#77421,#77422,#77423,#77424,
#77425,#77426,#77427,#77428,#77429,#77430,#77431,#77432,#77433,#77434,#77435,
#77436,#77437,#77438,#77439,#77440,#77441,#77442,#77443,#77444,#77445,#77446,
#77447,#77448,#77449,#77450,#77451,#77452,#77453,#77454,#77455,#77456,#77457,
#77458,#77459,#77460,#77461,#77462,#77463,#77464,#77465,#77466,#77467,#77468,
#77469,#77470,#77471,#77472,#77473,#77474,#77475,#77476,#77477,#77478,#77479,
#77480,#77481,#77482,#77483,#77484,#77485,#77486,#77487,#77488,#77489,#77490,
#77491,#77492,#77493,#77494,#77495,#77496,#77497,#77498,#77499,#77500,#77501,
#77502,#77503,#77504,#77505,#77506,#77507,#77508,#77509,#77510,#77511,#77512,
#77513,#77514,#77515,#77516,#77517,#77518,#77519,#77520,#77521,#77522,#77523,
#77524,#77525,#77526,#77527,#77528,#77529,#77530,#77531,#77532,#77533,#77534,
#77535,#77536,#77537,#77538,#77539,#77540,#77541,#77542,#77543,#77544,#77545,
#77546,#77547,#77548,#77549,#77550,#77551,#77552,#77553,#77554,#77555,#77556,
#77557,#77558,#77559,#77560,#77561,#77562,#77563,#77564,#77565,#77566,#77567,
#77568,#77569,#77570,#77571,#77572,#77573,#77574,#77575,#77576,#77577,#77578,
#77579,#77580,#77581,#77582,#77583,#77584,#77585,#77586,#77587),
 .UNSPECIFIED.,.F.,.F.,(4,3,3,3,3,3,3,3,3,3,3,3,3,3,3,3,3,3,3,3,3,3,3,3,
3,3,3,3,3,3,3,3,3,3,3,3,3,3,3,3,3,3,3,3,3,3,3,3,3,3,3,3,3,3,3,3,3,3,3,3,
3,3,3,4),(-29.2252827922655,-29.0991589622948,-28.9713058339057,-28.9227691659844,
-28.8172624042227,-28.7119145189336,-28.6066905171762,-28.5015324660573,
-28.3964042566833,-28.2912698243975,-28.1860234067202,-28.0807139922114,
-27.9752227400132,-27.9254322981918,-27.8199255364382,-27.7145776511576,
-27.6093536494092,-27.5041955982994,-27.399067388935,-27.2939329566588,
-27.1886865389915,-27.083377124493,-26.9778858723053,-26.9280954303993,
-26.822588668514,-26.7172407831012,-26.6120167812205,-26.5068587299785,
-26.4017305204819,-26.2965960880741,-26.1913496702766,-26.0860402556486,
-25.9805490033337,-25.9307585626067,-25.8252518009642,-25.7199039157939,
-25.6146799141543,-25.5095218631522,-25.4043936538942,-25.2992592217232,
-25.1940128041582,-25.0887033897605,-24.9832121376703,-24.9334216948141,
-24.8279149331472,-24.7225670479549,-24.6173430462968,-24.5121849952785,
-24.4070567860065,-24.3019223538238,-24.1966759362505,-24.0913665218466,
-23.985875269753,-23.9360848270216,-23.8306415847865,-23.7253571698249,
-23.6201964101123,-23.5151013526131,-23.4100357905481,-23.3049635610877,
-23.1997792451331,-23.0945313462189,-22.989102608445,-22.9420976708651),
 .UNSPECIFIED.);
#809=B_SPLINE_CURVE_WITH_KNOTS('',3,(#77589,#77590,#77591,#77592,#77593,
#77594,#77595,#77596,#77597,#77598,#77599,#77600,#77601,#77602,#77603,#77604,
#77605,#77606,#77607,#77608,#77609,#77610,#77611,#77612,#77613,#77614,#77615,
#77616,#77617,#77618,#77619,#77620,#77621,#77622,#77623,#77624,#77625,#77626,
#77627,#77628,#77629,#77630,#77631,#77632,#77633,#77634,#77635,#77636,#77637,
#77638,#77639,#77640,#77641,#77642,#77643,#77644,#77645,#77646,#77647,#77648,
#77649,#77650,#77651,#77652,#77653,#77654,#77655,#77656,#77657,#77658,#77659,
#77660,#77661,#77662,#77663,#77664,#77665,#77666,#77667,#77668,#77669,#77670,
#77671,#77672,#77673,#77674,#77675,#77676,#77677,#77678,#77679,#77680,#77681,
#77682,#77683,#77684,#77685,#77686,#77687,#77688,#77689,#77690,#77691,#77692,
#77693,#77694,#77695,#77696,#77697,#77698,#77699,#77700,#77701,#77702,#77703,
#77704,#77705,#77706,#77707,#77708,#77709,#77710,#77711,#77712,#77713,#77714,
#77715,#77716,#77717,#77718,#77719,#77720,#77721,#77722,#77723,#77724,#77725,
#77726,#77727,#77728,#77729,#77730,#77731,#77732,#77733,#77734,#77735,#77736,
#77737,#77738,#77739,#77740,#77741,#77742,#77743,#77744,#77745,#77746,#77747,
#77748,#77749,#77750,#77751,#77752,#77753,#77754,#77755,#77756,#77757,#77758,
#77759,#77760,#77761,#77762,#77763,#77764,#77765,#77766,#77767,#77768,#77769,
#77770,#77771,#77772,#77773,#77774,#77775,#77776,#77777,#77778,#77779,#77780,
#77781),.UNSPECIFIED.,.F.,.F.,(4,3,3,3,3,3,3,3,3,3,3,3,3,3,3,3,3,3,3,3,
3,3,3,3,3,3,3,3,3,3,3,3,3,3,3,3,3,3,3,3,3,3,3,3,3,3,3,3,3,3,3,3,3,3,3,3,
3,3,3,3,3,3,3,3,4),(-22.9420976703771,-22.938747959229,-22.8332411985356,
-22.7278933143125,-22.6226693136126,-22.5175112635451,-22.4123830552153,
-22.3072486239646,-22.202002207302,-22.0966927937979,-21.9912015425781,
-21.9414110914364,-21.8359043300259,-21.7305564451011,-21.6253324437251,
-21.5201743929979,-21.4150461840255,-21.3099117521501,-21.2046653348939,
-21.099355920813,-20.9938646690483,-20.9440742236439,-20.8385674571758,
-20.7332195671627,-20.6279955606782,-20.5228375048328,-20.4177092907404,
-20.312574853751,-20.2073284314246,-20.1020190122912,-19.9965277555541,
-19.9467373558513,-19.8412306024336,-19.7358827254785,-19.6306587320008,
-19.5255006891231,-19.42037248794,-19.3152380637825,-19.2099916540847,-19.1046822474822,
-18.9991910029953,-18.9494004880587,-18.843893726015,-18.738545840529,-18.6333218386999,
-18.5281637875865,-18.4230355782947,-18.3179011461671,-18.2126547287602,
-18.1073453145864,-18.0018540628175,-17.9520636202662,-17.8465568287251,
-17.7412089135173,-17.6359848817813,-17.5308268006639,-17.425698561317,
-17.3205640991286,-17.2153176518591,-17.1100082078919,-17.0045169267502,
-16.9547267524736,-16.8256995639624,-16.6984996556285,-16.6589125353624),
 .UNSPECIFIED.);
#810=B_SPLINE_CURVE_WITH_KNOTS('',3,(#77783,#77784,#77785,#77786,#77787,
#77788,#77789,#77790,#77791,#77792),.UNSPECIFIED.,.F.,.F.,(4,1,1,1,1,1,
1,4),(-16.6589123631975,-15.957389884681,-14.9600530168885,-13.9627161490959,
-12.9653792813033,-11.9680424135108,-10.9707055457182,-10.3757270560179),
 .UNSPECIFIED.);
#811=B_SPLINE_CURVE_WITH_KNOTS('',3,(#77793,#77794,#77795,#77796,#77797,
#77798,#77799,#77800,#77801,#77802),.UNSPECIFIED.,.F.,.F.,(4,1,1,1,1,1,
1,4),(-10.3757270560179,-9.97336867792565,-8.97603181013308,-7.97869494234052,
-6.98135807454796,-5.98402120675539,-4.98668433896283,-4.09255056086263),
 .UNSPECIFIED.);
#812=B_SPLINE_CURVE_WITH_KNOTS('',3,(#77805,#77806,#77807,#77808,#77809,
#77810,#77811,#77812,#77813,#77814,#77815,#77816,#77817,#77818,#77819,#77820,
#77821,#77822,#77823,#77824,#77825,#77826,#77827,#77828,#77829,#77830,#77831,
#77832,#77833,#77834,#77835,#77836,#77837,#77838,#77839,#77840,#77841,#77842,
#77843,#77844,#77845,#77846,#77847,#77848,#77849,#77850,#77851,#77852,#77853,
#77854,#77855,#77856,#77857,#77858,#77859,#77860,#77861,#77862,#77863,#77864,
#77865,#77866,#77867,#77868,#77869,#77870,#77871,#77872,#77873,#77874,#77875,
#77876,#77877,#77878,#77879,#77880,#77881,#77882,#77883,#77884,#77885,#77886,
#77887,#77888,#77889,#77890,#77891,#77892,#77893,#77894,#77895,#77896,#77897,
#77898,#77899,#77900,#77901,#77902,#77903,#77904,#77905,#77906,#77907,#77908,
#77909,#77910,#77911,#77912,#77913,#77914,#77915,#77916,#77917,#77918,#77919,
#77920,#77921,#77922,#77923,#77924,#77925,#77926,#77927,#77928,#77929,#77930,
#77931,#77932,#77933,#77934,#77935,#77936,#77937,#77938,#77939,#77940,#77941,
#77942,#77943,#77944,#77945,#77946,#77947,#77948,#77949),.UNSPECIFIED.,
 .F.,.F.,(4,3,3,3,3,3,3,3,3,3,3,3,3,3,3,3,3,3,3,3,3,3,3,3,3,3,3,3,3,3,3,
3,3,3,3,3,3,3,3,3,3,3,3,3,3,3,3,3,4),(91.1061869546275,91.240949975046,
91.377756011333,91.4023709425158,91.5139078873181,91.6252460499158,91.736473290312,
91.8476328030592,91.9587676852827,92.0700052418336,92.1812896847161,92.2927949344866,
92.3997078103083,92.5116216959549,92.6233352578315,92.7349367134751,92.8464686433293,
92.9579735293104,93.0695743704088,93.1812190271,93.2930745898801,93.3970446781009,
93.508902541041,93.6205658556783,93.7321205945633,93.8436093723387,93.9550747093353,
94.0666418835812,94.1782560360033,94.2900867617897,94.3943815458935,94.5048591627506,
94.6157165691175,94.7258879039597,94.8359949135827,94.9460821633185,95.0574912259104,
95.167750747137,95.2797345804115,95.391718413686,95.5065472606386,95.6211289936563,
95.7355648062727,95.849889628328,95.9641382305635,96.0783796323015,96.1926089700896,
96.3069226046808,96.3890552814785),.UNSPECIFIED.);
#813=B_SPLINE_CURVE_WITH_KNOTS('',3,(#77952,#77953,#77954,#77955,#77956,
#77957,#77958,#77959,#77960,#77961,#77962,#77963,#77964,#77965,#77966,#77967,
#77968,#77969,#77970,#77971,#77972,#77973,#77974,#77975,#77976,#77977,#77978,
#77979,#77980,#77981,#77982,#77983,#77984,#77985,#77986,#77987,#77988,#77989,
#77990,#77991,#77992,#77993,#77994,#77995,#77996,#77997,#77998,#77999,#78000,
#78001,#78002,#78003,#78004,#78005,#78006,#78007,#78008,#78009,#78010,#78011,
#78012,#78013,#78014,#78015,#78016,#78017,#78018,#78019,#78020,#78021,#78022,
#78023,#78024,#78025,#78026,#78027,#78028,#78029,#78030,#78031,#78032,#78033,
#78034,#78035,#78036,#78037,#78038,#78039,#78040,#78041,#78042,#78043,#78044,
#78045,#78046,#78047,#78048,#78049,#78050,#78051,#78052,#78053,#78054,#78055,
#78056,#78057,#78058,#78059,#78060,#78061,#78062,#78063),.UNSPECIFIED.,
 .F.,.F.,(4,3,3,3,3,3,3,3,3,3,3,3,3,3,3,3,3,3,3,3,3,3,3,3,3,3,3,3,3,3,3,
3,3,3,3,3,3,4),(91.106186954104,91.1567735128389,91.2686768073151,91.380379426595,
91.4919697243224,91.603490302343,91.7149836637296,91.8265730643033,91.938206154167,
92.0500508175322,92.1549203392256,92.2667654043467,92.3784155768566,92.4899569626954,
92.6014322014353,92.712883838097,92.824437435839,92.9360379010216,93.0478556711412,
93.1530671656123,93.2635326749248,93.3744928395591,93.4846514236711,93.5947455296085,
93.7048197379926,93.8164183014942,93.9266649332374,94.0389394626183,94.1512139919991,
94.2660363471297,94.3806110684729,94.4950395788434,94.6093568388985,94.7235976498901,
94.8378311521221,94.9520524352461,95.066358323657,95.1493608183857),
 .UNSPECIFIED.);
#814=B_SPLINE_CURVE_WITH_KNOTS('',3,(#78066,#78067,#78068,#78069,#78070,
#78071,#78072,#78073,#78074,#78075,#78076,#78077,#78078,#78079,#78080,#78081,
#78082,#78083,#78084,#78085,#78086,#78087,#78088,#78089,#78090,#78091),
 .UNSPECIFIED.,.F.,.F.,(4,2,2,2,2,2,2,2,2,2,2,2,4),(-0.913628530073302,
-0.835954964095443,-0.751212961809997,-0.639956110136178,-0.529437845948086,
-0.428568674976155,-0.345923223199362,-0.279967532511881,-0.210201642795373,
-0.152537234598984,-0.0832286370344242,-0.0398354201531648,-4.96018234762577E-5),
 .UNSPECIFIED.);
#815=B_SPLINE_CURVE_WITH_KNOTS('',3,(#78092,#78093,#78094,#78095,#78096,
#78097,#78098,#78099,#78100,#78101,#78102,#78103,#78104,#78105,#78106,#78107,
#78108,#78109,#78110,#78111,#78112,#78113,#78114,#78115,#78116,#78117,#78118,
#78119,#78120,#78121,#78122,#78123,#78124,#78125,#78126,#78127,#78128,#78129,
#78130,#78131,#78132,#78133,#78134,#78135,#78136,#78137,#78138,#78139,#78140,
#78141,#78142,#78143,#78144,#78145,#78146,#78147,#78148,#78149,#78150,#78151,
#78152),.UNSPECIFIED.,.F.,.F.,(4,3,3,3,3,3,3,3,3,3,3,3,3,3,3,3,3,3,3,3,
4),(-0.271362855059931,-0.249815153611103,-0.228817936840513,-0.21475709335129,
-0.20269615019584,-0.199258579296682,-0.179079219908023,-0.172574562883619,
-0.151002742523167,-0.132127399707771,-0.128545224966699,-0.108660381316369,
-0.088904641890274,-0.0695673848931777,-0.0643977176859483,-0.0611873514593056,
-0.0424333152675423,-0.0240015440670001,-0.00742689876696626,-0.00610711498195276,
-1.33929388601358E-14),.UNSPECIFIED.);
#816=B_SPLINE_CURVE_WITH_KNOTS('',3,(#78153,#78154,#78155,#78156,#78157,
#78158,#78159,#78160,#78161,#78162,#78163,#78164,#78165,#78166,#78167,#78168,
#78169,#78170,#78171,#78172,#78173,#78174,#78175,#78176,#78177,#78178,#78179,
#78180,#78181,#78182,#78183,#78184,#78185,#78186,#78187,#78188,#78189,#78190,
#78191,#78192,#78193,#78194,#78195,#78196,#78197,#78198,#78199,#78200,#78201,
#78202,#78203,#78204,#78205,#78206,#78207,#78208,#78209,#78210,#78211,#78212,
#78213,#78214,#78215,#78216,#78217,#78218,#78219),.UNSPECIFIED.,.F.,.F.,
(4,3,3,3,3,3,3,3,3,3,3,3,3,3,3,3,3,3,3,3,3,3,4),(-0.304888653691309,-0.297138437894475,
-0.27579526247451,-0.25452115728438,-0.238505141940676,-0.229387728747905,
-0.225368790891129,-0.221917825979367,-0.200380627888395,-0.178797401191701,
-0.157590348312134,-0.15077543359462,-0.1472283770012,-0.12639303453475,
-0.106224887749054,-0.105100297430208,-0.083375892217648,-0.0782531846850942,
-0.0733795998480499,-0.0515968866484263,-0.0295071888683422,-0.00749310652115608,
-5.77388764150222E-6),.UNSPECIFIED.);
#817=B_SPLINE_CURVE_WITH_KNOTS('',3,(#78575,#78576,#78577,#78578,#78579,
#78580,#78581,#78582,#78583,#78584,#78585,#78586,#78587,#78588,#78589,#78590,
#78591,#78592,#78593,#78594,#78595,#78596,#78597,#78598,#78599,#78600,#78601,
#78602,#78603,#78604,#78605,#78606,#78607,#78608,#78609,#78610,#78611,#78612,
#78613,#78614,#78615,#78616,#78617,#78618,#78619,#78620,#78621,#78622,#78623,
#78624,#78625,#78626,#78627,#78628,#78629,#78630,#78631,#78632,#78633,#78634,
#78635,#78636,#78637,#78638,#78639,#78640,#78641,#78642,#78643,#78644,#78645,
#78646,#78647,#78648,#78649,#78650,#78651,#78652,#78653,#78654,#78655,#78656,
#78657,#78658,#78659),.UNSPECIFIED.,.F.,.F.,(4,3,3,3,3,3,3,3,3,3,3,3,3,
3,3,3,3,3,3,3,3,3,3,3,3,3,3,3,4),(-0.364629307890664,-0.350886157932352,
-0.32922367190401,-0.318978960138819,-0.313744359949613,-0.309365983727222,
-0.288066930719578,-0.266904292681073,-0.264007580396482,-0.260298494201204,
-0.239603026511185,-0.219189259610856,-0.199417582510638,-0.194877404256716,
-0.191399198693004,-0.171813503246808,-0.166173778995206,-0.146078326122423,
-0.126707179806039,-0.123380359543154,-0.103933540649634,-0.0846710840002831,
-0.0655680939453014,-0.062174737667072,-0.0589393440631834,-0.0403289038697169,
-0.0223014018348129,-0.00442011167346308,0.),.UNSPECIFIED.);
#818=B_SPLINE_CURVE_WITH_KNOTS('',3,(#79021,#79022,#79023,#79024,#79025,
#79026,#79027,#79028,#79029,#79030,#79031,#79032,#79033,#79034,#79035,#79036,
#79037,#79038,#79039,#79040,#79041,#79042,#79043,#79044,#79045,#79046,#79047,
#79048,#79049,#79050,#79051,#79052,#79053,#79054,#79055,#79056,#79057,#79058,
#79059,#79060,#79061,#79062,#79063,#79064,#79065,#79066,#79067,#79068,#79069,
#79070,#79071,#79072,#79073,#79074,#79075,#79076,#79077,#79078,#79079,#79080,
#79081,#79082,#79083,#79084,#79085,#79086,#79087,#79088,#79089,#79090,#79091,
#79092,#79093,#79094,#79095,#79096,#79097,#79098,#79099,#79100,#79101,#79102),
 .UNSPECIFIED.,.F.,.F.,(4,3,3,3,3,3,3,3,3,3,3,3,3,3,3,3,3,3,3,3,3,3,3,3,
3,3,3,4),(-0.366397579005846,-0.355505695503922,-0.337427534487906,-0.327287439123245,
-0.321639660907082,-0.302932980904847,-0.290487499977824,-0.283637563200549,
-0.278450433971176,-0.258630766453179,-0.238832793368305,-0.226847110991912,
-0.218285448981465,-0.214861428615519,-0.194431505887542,-0.187234374154516,
-0.16731282220457,-0.147391270254625,-0.143955108128756,-0.123548173224516,
-0.102525007863438,-0.0815018425023604,-0.0762248591763458,-0.071232862628432,
-0.0495803100067464,-0.0278917785029102,-0.0066769277724615,-3.86019020422907E-15),
 .UNSPECIFIED.);
#819=B_SPLINE_CURVE_WITH_KNOTS('',3,(#79103,#79104,#79105,#79106),
 .UNSPECIFIED.,.F.,.F.,(4,4),(-0.0125583369336329,0.),.UNSPECIFIED.);
#947=SHAPE_REPRESENTATION_RELATIONSHIP('SRR','None',#94499,#962);
#962=ADVANCED_BREP_SHAPE_REPRESENTATION('',(#992),#94408);
#977=STYLED_ITEM('',(#94578),#992);
#992=MANIFOLD_SOLID_BREP('Body1',#8262);
#1045=FACE_BOUND('',#1858,.T.);
#1046=FACE_BOUND('',#1861,.T.);
#1141=PLANE('',#8832);
#1142=PLANE('',#8833);
#1143=PLANE('',#8834);
#1144=PLANE('',#8835);
#1145=PLANE('',#8836);
#1146=PLANE('',#8837);
#1147=PLANE('',#8838);
#1148=PLANE('',#8839);
#1149=PLANE('',#8843);
#1150=PLANE('',#8844);
#1427=FACE_OUTER_BOUND('',#1832,.T.);
#1428=FACE_OUTER_BOUND('',#1833,.T.);
#1429=FACE_OUTER_BOUND('',#1834,.T.);
#1430=FACE_OUTER_BOUND('',#1835,.T.);
#1431=FACE_OUTER_BOUND('',#1836,.T.);
#1432=FACE_OUTER_BOUND('',#1837,.T.);
#1433=FACE_OUTER_BOUND('',#1838,.T.);
#1434=FACE_OUTER_BOUND('',#1839,.T.);
#1435=FACE_OUTER_BOUND('',#1840,.T.);
#1436=FACE_OUTER_BOUND('',#1841,.T.);
#1437=FACE_OUTER_BOUND('',#1842,.T.);
#1438=FACE_OUTER_BOUND('',#1843,.T.);
#1439=FACE_OUTER_BOUND('',#1844,.T.);
#1440=FACE_OUTER_BOUND('',#1845,.T.);
#1441=FACE_OUTER_BOUND('',#1846,.T.);
#1442=FACE_OUTER_BOUND('',#1847,.T.);
#1443=FACE_OUTER_BOUND('',#1848,.T.);
#1444=FACE_OUTER_BOUND('',#1849,.T.);
#1445=FACE_OUTER_BOUND('',#1850,.T.);
#1446=FACE_OUTER_BOUND('',#1851,.T.);
#1447=FACE_OUTER_BOUND('',#1852,.T.);
#1448=FACE_OUTER_BOUND('',#1853,.T.);
#1449=FACE_OUTER_BOUND('',#1854,.T.);
#1450=FACE_OUTER_BOUND('',#1855,.T.);
#1451=FACE_OUTER_BOUND('',#1856,.T.);
#1452=FACE_OUTER_BOUND('',#1857,.T.);
#1453=FACE_OUTER_BOUND('',#1859,.T.);
#1454=FACE_OUTER_BOUND('',#1860,.T.);
#1455=FACE_OUTER_BOUND('',#1862,.T.);
#1832=EDGE_LOOP('',(#7078,#7079,#7080,#7081));
#1833=EDGE_LOOP('',(#7082,#7083,#7084,#7085));
#1834=EDGE_LOOP('',(#7086,#7087,#7088,#7089,#7090));
#1835=EDGE_LOOP('',(#7091,#7092,#7093,#7094,#7095));
#1836=EDGE_LOOP('',(#7096,#7097,#7098,#7099,#7100));
#1837=EDGE_LOOP('',(#7101,#7102,#7103,#7104));
#1838=EDGE_LOOP('',(#7105,#7106,#7107,#7108,#7109));
#1839=EDGE_LOOP('',(#7110,#7111,#7112,#7113));
#1840=EDGE_LOOP('',(#7114,#7115,#7116,#7117));
#1841=EDGE_LOOP('',(#7118,#7119,#7120,#7121,#7122));
#1842=EDGE_LOOP('',(#7123,#7124,#7125,#7126,#7127,#7128));
#1843=EDGE_LOOP('',(#7129,#7130,#7131,#7132));
#1844=EDGE_LOOP('',(#7133,#7134,#7135,#7136));
#1845=EDGE_LOOP('',(#7137,#7138,#7139,#7140,#7141,#7142,#7143,#7144,#7145,
#7146,#7147,#7148,#7149,#7150,#7151,#7152,#7153,#7154,#7155,#7156,#7157,
#7158,#7159,#7160,#7161,#7162,#7163,#7164,#7165,#7166));
#1846=EDGE_LOOP('',(#7167,#7168,#7169,#7170));
#1847=EDGE_LOOP('',(#7171,#7172,#7173,#7174,#7175,#7176,#7177,#7178));
#1848=EDGE_LOOP('',(#7179,#7180,#7181,#7182,#7183,#7184,#7185,#7186,#7187,
#7188,#7189,#7190,#7191,#7192,#7193,#7194,#7195,#7196,#7197,#7198,#7199,
#7200,#7201,#7202,#7203,#7204,#7205,#7206,#7207,#7208,#7209,#7210,#7211));
#1849=EDGE_LOOP('',(#7212,#7213,#7214,#7215,#7216,#7217,#7218,#7219,#7220,
#7221,#7222,#7223,#7224,#7225,#7226,#7227,#7228,#7229,#7230,#7231,#7232,
#7233,#7234,#7235,#7236,#7237,#7238,#7239,#7240,#7241,#7242,#7243,#7244,
#7245,#7246,#7247));
#1850=EDGE_LOOP('',(#7248,#7249,#7250,#7251));
#1851=EDGE_LOOP('',(#7252,#7253,#7254,#7255));
#1852=EDGE_LOOP('',(#7256,#7257,#7258,#7259));
#1853=EDGE_LOOP('',(#7260,#7261,#7262,#7263));
#1854=EDGE_LOOP('',(#7264,#7265,#7266,#7267));
#1855=EDGE_LOOP('',(#7268,#7269,#7270,#7271));
#1856=EDGE_LOOP('',(#7272,#7273,#7274,#7275,#7276,#7277));
#1857=EDGE_LOOP('',(#7278));
#1858=EDGE_LOOP('',(#7279,#7280,#7281,#7282,#7283));
#1859=EDGE_LOOP('',(#7284,#7285,#7286,#7287));
#1860=EDGE_LOOP('',(#7288));
#1861=EDGE_LOOP('',(#7289,#7290,#7291,#7292,#7293,#7294));
#1862=EDGE_LOOP('',(#7295));
#2254=LINE('',#70399,#2652);
#2255=LINE('',#70670,#2653);
#2256=LINE('',#71052,#2654);
#2257=LINE('',#71455,#2655);
#2258=LINE('',#71846,#2656);
#2259=LINE('',#72218,#2657);
#2260=LINE('',#72600,#2658);
#2261=LINE('',#72991,#2659);
#2262=LINE('',#73208,#2660);
#2263=LINE('',#73646,#2661);
#2264=LINE('',#74039,#2662);
#2265=LINE('',#74451,#2663);
#2266=LINE('',#74837,#2664);
#2267=LINE('',#78221,#2665);
#2268=LINE('',#79110,#2666);
#2269=LINE('',#79112,#2667);
#2270=LINE('',#79114,#2668);
#2271=LINE('',#79115,#2669);
#2272=LINE('',#79118,#2670);
#2273=LINE('',#79120,#2671);
#2274=LINE('',#79121,#2672);
#2275=LINE('',#79124,#2673);
#2276=LINE('',#79126,#2674);
#2277=LINE('',#79127,#2675);
#2278=LINE('',#79130,#2676);
#2279=LINE('',#79132,#2677);
#2280=LINE('',#79133,#2678);
#2281=LINE('',#79136,#2679);
#2282=LINE('',#79138,#2680);
#2283=LINE('',#79139,#2681);
#2284=LINE('',#79141,#2682);
#2285=LINE('',#79142,#2683);
#2286=LINE('',#79149,#2684);
#2652=VECTOR('',#10024,1.5555);
#2653=VECTOR('',#10029,1.5555);
#2654=VECTOR('',#10032,1.5555);
#2655=VECTOR('',#10035,1.5555);
#2656=VECTOR('',#10038,1.5555);
#2657=VECTOR('',#10041,1.5555);
#2658=VECTOR('',#10044,1.5555);
#2659=VECTOR('',#10047,1.5555);
#2660=VECTOR('',#10050,1.5555);
#2661=VECTOR('',#10053,1.5555);
#2662=VECTOR('',#10056,1.5555);
#2663=VECTOR('',#10059,1.5555);
#2664=VECTOR('',#10062,1.5555);
#2665=VECTOR('',#10075,1.5);
#2666=VECTOR('',#10080,10.);
#2667=VECTOR('',#10081,10.);
#2668=VECTOR('',#10082,10.);
#2669=VECTOR('',#10083,10.);
#2670=VECTOR('',#10086,10.);
#2671=VECTOR('',#10087,10.);
#2672=VECTOR('',#10088,10.);
#2673=VECTOR('',#10091,10.);
#2674=VECTOR('',#10092,10.);
#2675=VECTOR('',#10093,10.);
#2676=VECTOR('',#10096,10.);
#2677=VECTOR('',#10097,10.);
#2678=VECTOR('',#10098,10.);
#2679=VECTOR('',#10101,10.);
#2680=VECTOR('',#10102,10.);
#2681=VECTOR('',#10103,10.);
#2682=VECTOR('',#10106,10.);
#2683=VECTOR('',#10107,10.);
#2684=VECTOR('',#10116,3.5);
#2817=CIRCLE('',#8812,1.5555);
#2818=CIRCLE('',#8826,1.954);
#2819=CIRCLE('',#8827,1.954);
#2820=CIRCLE('',#8829,1.5555);
#2821=CIRCLE('',#8831,1.);
#2822=CIRCLE('',#8840,3.5);
#2823=CIRCLE('',#8842,3.5);
#3598=VERTEX_POINT('',#70397);
#3599=VERTEX_POINT('',#70398);
#3600=VERTEX_POINT('',#70400);
#3601=VERTEX_POINT('',#70553);
#3602=VERTEX_POINT('',#70668);
#3603=VERTEX_POINT('',#70669);
#3604=VERTEX_POINT('',#71050);
#3605=VERTEX_POINT('',#71051);
#3606=VERTEX_POINT('',#71053);
#3607=VERTEX_POINT('',#71453);
#3608=VERTEX_POINT('',#71454);
#3609=VERTEX_POINT('',#71650);
#3610=VERTEX_POINT('',#71844);
#3611=VERTEX_POINT('',#71845);
#3612=VERTEX_POINT('',#72022);
#3613=VERTEX_POINT('',#72216);
#3614=VERTEX_POINT('',#72217);
#3615=VERTEX_POINT('',#72598);
#3616=VERTEX_POINT('',#72599);
#3617=VERTEX_POINT('',#72601);
#3618=VERTEX_POINT('',#72989);
#3619=VERTEX_POINT('',#72990);
#3620=VERTEX_POINT('',#73206);
#3621=VERTEX_POINT('',#73207);
#3622=VERTEX_POINT('',#73644);
#3623=VERTEX_POINT('',#73645);
#3624=VERTEX_POINT('',#73647);
#3625=VERTEX_POINT('',#74037);
#3626=VERTEX_POINT('',#74038);
#3627=VERTEX_POINT('',#74040);
#3628=VERTEX_POINT('',#74247);
#3629=VERTEX_POINT('',#74449);
#3630=VERTEX_POINT('',#74450);
#3631=VERTEX_POINT('',#74835);
#3632=VERTEX_POINT('',#74836);
#3633=VERTEX_POINT('',#75200);
#3634=VERTEX_POINT('',#75201);
#3635=VERTEX_POINT('',#75263);
#3636=VERTEX_POINT('',#75265);
#3637=VERTEX_POINT('',#75300);
#3638=VERTEX_POINT('',#75491);
#3639=VERTEX_POINT('',#75502);
#3640=VERTEX_POINT('',#75693);
#3641=VERTEX_POINT('',#75884);
#3642=VERTEX_POINT('',#75895);
#3643=VERTEX_POINT('',#76086);
#3644=VERTEX_POINT('',#76098);
#3645=VERTEX_POINT('',#76109);
#3646=VERTEX_POINT('',#76300);
#3647=VERTEX_POINT('',#76312);
#3648=VERTEX_POINT('',#76500);
#3649=VERTEX_POINT('',#76511);
#3650=VERTEX_POINT('',#76651);
#3651=VERTEX_POINT('',#76653);
#3652=VERTEX_POINT('',#76769);
#3653=VERTEX_POINT('',#76780);
#3654=VERTEX_POINT('',#76971);
#3655=VERTEX_POINT('',#77162);
#3656=VERTEX_POINT('',#77173);
#3657=VERTEX_POINT('',#77184);
#3658=VERTEX_POINT('',#77375);
#3659=VERTEX_POINT('',#77386);
#3660=VERTEX_POINT('',#77397);
#3661=VERTEX_POINT('',#77588);
#3662=VERTEX_POINT('',#77782);
#3663=VERTEX_POINT('',#77804);
#3664=VERTEX_POINT('',#77950);
#3665=VERTEX_POINT('',#78065);
#3666=VERTEX_POINT('',#78220);
#3667=VERTEX_POINT('',#79020);
#3668=VERTEX_POINT('',#79108);
#3669=VERTEX_POINT('',#79109);
#3670=VERTEX_POINT('',#79111);
#3671=VERTEX_POINT('',#79113);
#3672=VERTEX_POINT('',#79117);
#3673=VERTEX_POINT('',#79119);
#3674=VERTEX_POINT('',#79123);
#3675=VERTEX_POINT('',#79125);
#3676=VERTEX_POINT('',#79129);
#3677=VERTEX_POINT('',#79131);
#3678=VERTEX_POINT('',#79135);
#3679=VERTEX_POINT('',#79137);
#3680=VERTEX_POINT('',#79145);
#3681=VERTEX_POINT('',#79148);
#4804=EDGE_CURVE('',#3598,#3599,#2254,.T.);
#4805=EDGE_CURVE('',#3600,#3598,#751,.F.);
#4806=EDGE_CURVE('',#3601,#3600,#2817,.T.);
#4807=EDGE_CURVE('',#3601,#3599,#752,.T.);
#4808=EDGE_CURVE('',#3602,#3603,#2255,.T.);
#4809=EDGE_CURVE('',#3598,#3602,#753,.F.);
#4810=EDGE_CURVE('',#3599,#3603,#754,.T.);
#4811=EDGE_CURVE('',#3604,#3605,#2256,.T.);
#4812=EDGE_CURVE('',#3606,#3604,#755,.F.);
#4813=EDGE_CURVE('',#3602,#3606,#756,.F.);
#4814=EDGE_CURVE('',#3603,#3605,#757,.T.);
#4815=EDGE_CURVE('',#3607,#3608,#2257,.T.);
#4816=EDGE_CURVE('',#3604,#3607,#758,.F.);
#4817=EDGE_CURVE('',#3605,#3609,#759,.T.);
#4818=EDGE_CURVE('',#3609,#3608,#760,.T.);
#4819=EDGE_CURVE('',#3610,#3611,#2258,.T.);
#4820=EDGE_CURVE('',#3607,#3610,#761,.T.);
#4821=EDGE_CURVE('',#3608,#3612,#762,.T.);
#4822=EDGE_CURVE('',#3612,#3611,#763,.T.);
#4823=EDGE_CURVE('',#3613,#3614,#2259,.T.);
#4824=EDGE_CURVE('',#3610,#3613,#764,.F.);
#4825=EDGE_CURVE('',#3611,#3614,#765,.T.);
#4826=EDGE_CURVE('',#3615,#3616,#2260,.T.);
#4827=EDGE_CURVE('',#3617,#3615,#766,.F.);
#4828=EDGE_CURVE('',#3613,#3617,#767,.F.);
#4829=EDGE_CURVE('',#3614,#3616,#768,.T.);
#4830=EDGE_CURVE('',#3618,#3619,#2261,.T.);
#4831=EDGE_CURVE('',#3615,#3618,#769,.F.);
#4832=EDGE_CURVE('',#3616,#3619,#770,.T.);
#4833=EDGE_CURVE('',#3620,#3621,#2262,.T.);
#4834=EDGE_CURVE('',#3618,#3620,#771,.F.);
#4835=EDGE_CURVE('',#3619,#3621,#772,.T.);
#4836=EDGE_CURVE('',#3622,#3623,#2263,.T.);
#4837=EDGE_CURVE('',#3624,#3622,#773,.F.);
#4838=EDGE_CURVE('',#3620,#3624,#774,.F.);
#4839=EDGE_CURVE('',#3621,#3623,#775,.T.);
#4840=EDGE_CURVE('',#3625,#3626,#2264,.T.);
#4841=EDGE_CURVE('',#3627,#3625,#776,.F.);
#4842=EDGE_CURVE('',#3622,#3627,#777,.F.);
#4843=EDGE_CURVE('',#3623,#3628,#778,.T.);
#4844=EDGE_CURVE('',#3628,#3626,#779,.T.);
#4845=EDGE_CURVE('',#3629,#3630,#2265,.T.);
#4846=EDGE_CURVE('',#3625,#3629,#780,.F.);
#4847=EDGE_CURVE('',#3626,#3630,#781,.T.);
#4848=EDGE_CURVE('',#3631,#3632,#2266,.T.);
#4849=EDGE_CURVE('',#3629,#3631,#782,.F.);
#4850=EDGE_CURVE('',#3630,#3632,#783,.T.);
#4851=EDGE_CURVE('',#3633,#3634,#784,.T.);
#4852=EDGE_CURVE('',#3634,#3635,#2818,.F.);
#4853=EDGE_CURVE('',#3635,#3636,#785,.T.);
#4854=EDGE_CURVE('',#3636,#3637,#786,.T.);
#4855=EDGE_CURVE('',#3637,#3638,#787,.T.);
#4856=EDGE_CURVE('',#3638,#3639,#788,.T.);
#4857=EDGE_CURVE('',#3639,#3640,#789,.T.);
#4858=EDGE_CURVE('',#3640,#3641,#790,.T.);
#4859=EDGE_CURVE('',#3641,#3642,#791,.T.);
#4860=EDGE_CURVE('',#3642,#3643,#792,.T.);
#4861=EDGE_CURVE('',#3643,#3644,#793,.T.);
#4862=EDGE_CURVE('',#3644,#3645,#794,.T.);
#4863=EDGE_CURVE('',#3645,#3646,#795,.T.);
#4864=EDGE_CURVE('',#3646,#3647,#796,.T.);
#4865=EDGE_CURVE('',#3647,#3648,#797,.T.);
#4866=EDGE_CURVE('',#3648,#3649,#798,.T.);
#4867=EDGE_CURVE('',#3649,#3650,#2819,.T.);
#4868=EDGE_CURVE('',#3650,#3651,#799,.T.);
#4869=EDGE_CURVE('',#3651,#3652,#800,.T.);
#4870=EDGE_CURVE('',#3652,#3653,#801,.T.);
#4871=EDGE_CURVE('',#3653,#3654,#802,.T.);
#4872=EDGE_CURVE('',#3654,#3655,#803,.T.);
#4873=EDGE_CURVE('',#3655,#3656,#804,.T.);
#4874=EDGE_CURVE('',#3656,#3657,#805,.T.);
#4875=EDGE_CURVE('',#3657,#3658,#806,.T.);
#4876=EDGE_CURVE('',#3658,#3659,#807,.T.);
#4877=EDGE_CURVE('',#3659,#3660,#808,.T.);
#4878=EDGE_CURVE('',#3660,#3661,#809,.T.);
#4879=EDGE_CURVE('',#3661,#3662,#810,.T.);
#4880=EDGE_CURVE('',#3662,#3633,#811,.T.);
#4881=EDGE_CURVE('',#3632,#3663,#812,.T.);
#4882=EDGE_CURVE('',#3663,#3664,#2820,.T.);
#4883=EDGE_CURVE('',#3631,#3664,#813,.T.);
#4884=EDGE_CURVE('',#3664,#3665,#814,.T.);
#4885=EDGE_CURVE('',#3650,#3663,#815,.T.);
#4886=EDGE_CURVE('',#3665,#3649,#816,.T.);
#4887=EDGE_CURVE('',#3665,#3666,#2267,.T.);
#4888=EDGE_CURVE('',#3666,#3666,#2821,.T.);
#4889=EDGE_CURVE('',#3634,#3601,#817,.T.);
#4890=EDGE_CURVE('',#3667,#3635,#818,.T.);
#4891=EDGE_CURVE('',#3667,#3600,#819,.T.);
#4892=EDGE_CURVE('',#3668,#3669,#2268,.T.);
#4893=EDGE_CURVE('',#3668,#3670,#2269,.T.);
#4894=EDGE_CURVE('',#3670,#3671,#2270,.T.);
#4895=EDGE_CURVE('',#3669,#3671,#2271,.T.);
#4896=EDGE_CURVE('',#3672,#3668,#2272,.T.);
#4897=EDGE_CURVE('',#3672,#3673,#2273,.T.);
#4898=EDGE_CURVE('',#3673,#3670,#2274,.T.);
#4899=EDGE_CURVE('',#3674,#3672,#2275,.T.);
#4900=EDGE_CURVE('',#3674,#3675,#2276,.T.);
#4901=EDGE_CURVE('',#3675,#3673,#2277,.T.);
#4902=EDGE_CURVE('',#3676,#3674,#2278,.T.);
#4903=EDGE_CURVE('',#3676,#3677,#2279,.T.);
#4904=EDGE_CURVE('',#3677,#3675,#2280,.T.);
#4905=EDGE_CURVE('',#3678,#3676,#2281,.T.);
#4906=EDGE_CURVE('',#3678,#3679,#2282,.T.);
#4907=EDGE_CURVE('',#3679,#3677,#2283,.T.);
#4908=EDGE_CURVE('',#3669,#3678,#2284,.T.);
#4909=EDGE_CURVE('',#3671,#3679,#2285,.T.);
#4910=EDGE_CURVE('',#3680,#3680,#2822,.T.);
#4911=EDGE_CURVE('',#3680,#3681,#2286,.T.);
#4912=EDGE_CURVE('',#3681,#3681,#2823,.T.);
#7078=ORIENTED_EDGE('',*,*,#4804,.F.);
#7079=ORIENTED_EDGE('',*,*,#4805,.F.);
#7080=ORIENTED_EDGE('',*,*,#4806,.F.);
#7081=ORIENTED_EDGE('',*,*,#4807,.T.);
#7082=ORIENTED_EDGE('',*,*,#4808,.F.);
#7083=ORIENTED_EDGE('',*,*,#4809,.F.);
#7084=ORIENTED_EDGE('',*,*,#4804,.T.);
#7085=ORIENTED_EDGE('',*,*,#4810,.T.);
#7086=ORIENTED_EDGE('',*,*,#4811,.F.);
#7087=ORIENTED_EDGE('',*,*,#4812,.F.);
#7088=ORIENTED_EDGE('',*,*,#4813,.F.);
#7089=ORIENTED_EDGE('',*,*,#4808,.T.);
#7090=ORIENTED_EDGE('',*,*,#4814,.T.);
#7091=ORIENTED_EDGE('',*,*,#4815,.F.);
#7092=ORIENTED_EDGE('',*,*,#4816,.F.);
#7093=ORIENTED_EDGE('',*,*,#4811,.T.);
#7094=ORIENTED_EDGE('',*,*,#4817,.T.);
#7095=ORIENTED_EDGE('',*,*,#4818,.T.);
#7096=ORIENTED_EDGE('',*,*,#4819,.F.);
#7097=ORIENTED_EDGE('',*,*,#4820,.F.);
#7098=ORIENTED_EDGE('',*,*,#4815,.T.);
#7099=ORIENTED_EDGE('',*,*,#4821,.T.);
#7100=ORIENTED_EDGE('',*,*,#4822,.T.);
#7101=ORIENTED_EDGE('',*,*,#4823,.F.);
#7102=ORIENTED_EDGE('',*,*,#4824,.F.);
#7103=ORIENTED_EDGE('',*,*,#4819,.T.);
#7104=ORIENTED_EDGE('',*,*,#4825,.T.);
#7105=ORIENTED_EDGE('',*,*,#4826,.F.);
#7106=ORIENTED_EDGE('',*,*,#4827,.F.);
#7107=ORIENTED_EDGE('',*,*,#4828,.F.);
#7108=ORIENTED_EDGE('',*,*,#4823,.T.);
#7109=ORIENTED_EDGE('',*,*,#4829,.T.);
#7110=ORIENTED_EDGE('',*,*,#4830,.F.);
#7111=ORIENTED_EDGE('',*,*,#4831,.F.);
#7112=ORIENTED_EDGE('',*,*,#4826,.T.);
#7113=ORIENTED_EDGE('',*,*,#4832,.T.);
#7114=ORIENTED_EDGE('',*,*,#4833,.F.);
#7115=ORIENTED_EDGE('',*,*,#4834,.F.);
#7116=ORIENTED_EDGE('',*,*,#4830,.T.);
#7117=ORIENTED_EDGE('',*,*,#4835,.T.);
#7118=ORIENTED_EDGE('',*,*,#4836,.F.);
#7119=ORIENTED_EDGE('',*,*,#4837,.F.);
#7120=ORIENTED_EDGE('',*,*,#4838,.F.);
#7121=ORIENTED_EDGE('',*,*,#4833,.T.);
#7122=ORIENTED_EDGE('',*,*,#4839,.T.);
#7123=ORIENTED_EDGE('',*,*,#4840,.F.);
#7124=ORIENTED_EDGE('',*,*,#4841,.F.);
#7125=ORIENTED_EDGE('',*,*,#4842,.F.);
#7126=ORIENTED_EDGE('',*,*,#4836,.T.);
#7127=ORIENTED_EDGE('',*,*,#4843,.T.);
#7128=ORIENTED_EDGE('',*,*,#4844,.T.);
#7129=ORIENTED_EDGE('',*,*,#4845,.F.);
#7130=ORIENTED_EDGE('',*,*,#4846,.F.);
#7131=ORIENTED_EDGE('',*,*,#4840,.T.);
#7132=ORIENTED_EDGE('',*,*,#4847,.T.);
#7133=ORIENTED_EDGE('',*,*,#4848,.F.);
#7134=ORIENTED_EDGE('',*,*,#4849,.F.);
#7135=ORIENTED_EDGE('',*,*,#4845,.T.);
#7136=ORIENTED_EDGE('',*,*,#4850,.T.);
#7137=ORIENTED_EDGE('',*,*,#4851,.T.);
#7138=ORIENTED_EDGE('',*,*,#4852,.T.);
#7139=ORIENTED_EDGE('',*,*,#4853,.T.);
#7140=ORIENTED_EDGE('',*,*,#4854,.T.);
#7141=ORIENTED_EDGE('',*,*,#4855,.T.);
#7142=ORIENTED_EDGE('',*,*,#4856,.T.);
#7143=ORIENTED_EDGE('',*,*,#4857,.T.);
#7144=ORIENTED_EDGE('',*,*,#4858,.T.);
#7145=ORIENTED_EDGE('',*,*,#4859,.T.);
#7146=ORIENTED_EDGE('',*,*,#4860,.T.);
#7147=ORIENTED_EDGE('',*,*,#4861,.T.);
#7148=ORIENTED_EDGE('',*,*,#4862,.T.);
#7149=ORIENTED_EDGE('',*,*,#4863,.T.);
#7150=ORIENTED_EDGE('',*,*,#4864,.T.);
#7151=ORIENTED_EDGE('',*,*,#4865,.T.);
#7152=ORIENTED_EDGE('',*,*,#4866,.T.);
#7153=ORIENTED_EDGE('',*,*,#4867,.T.);
#7154=ORIENTED_EDGE('',*,*,#4868,.T.);
#7155=ORIENTED_EDGE('',*,*,#4869,.T.);
#7156=ORIENTED_EDGE('',*,*,#4870,.T.);
#7157=ORIENTED_EDGE('',*,*,#4871,.T.);
#7158=ORIENTED_EDGE('',*,*,#4872,.T.);
#7159=ORIENTED_EDGE('',*,*,#4873,.T.);
#7160=ORIENTED_EDGE('',*,*,#4874,.T.);
#7161=ORIENTED_EDGE('',*,*,#4875,.T.);
#7162=ORIENTED_EDGE('',*,*,#4876,.T.);
#7163=ORIENTED_EDGE('',*,*,#4877,.T.);
#7164=ORIENTED_EDGE('',*,*,#4878,.T.);
#7165=ORIENTED_EDGE('',*,*,#4879,.T.);
#7166=ORIENTED_EDGE('',*,*,#4880,.T.);
#7167=ORIENTED_EDGE('',*,*,#4848,.T.);
#7168=ORIENTED_EDGE('',*,*,#4881,.T.);
#7169=ORIENTED_EDGE('',*,*,#4882,.T.);
#7170=ORIENTED_EDGE('',*,*,#4883,.F.);
#7171=ORIENTED_EDGE('',*,*,#4884,.F.);
#7172=ORIENTED_EDGE('',*,*,#4882,.F.);
#7173=ORIENTED_EDGE('',*,*,#4885,.F.);
#7174=ORIENTED_EDGE('',*,*,#4867,.F.);
#7175=ORIENTED_EDGE('',*,*,#4886,.F.);
#7176=ORIENTED_EDGE('',*,*,#4887,.T.);
#7177=ORIENTED_EDGE('',*,*,#4888,.F.);
#7178=ORIENTED_EDGE('',*,*,#4887,.F.);
#7179=ORIENTED_EDGE('',*,*,#4885,.T.);
#7180=ORIENTED_EDGE('',*,*,#4881,.F.);
#7181=ORIENTED_EDGE('',*,*,#4850,.F.);
#7182=ORIENTED_EDGE('',*,*,#4847,.F.);
#7183=ORIENTED_EDGE('',*,*,#4844,.F.);
#7184=ORIENTED_EDGE('',*,*,#4843,.F.);
#7185=ORIENTED_EDGE('',*,*,#4839,.F.);
#7186=ORIENTED_EDGE('',*,*,#4835,.F.);
#7187=ORIENTED_EDGE('',*,*,#4832,.F.);
#7188=ORIENTED_EDGE('',*,*,#4829,.F.);
#7189=ORIENTED_EDGE('',*,*,#4825,.F.);
#7190=ORIENTED_EDGE('',*,*,#4822,.F.);
#7191=ORIENTED_EDGE('',*,*,#4821,.F.);
#7192=ORIENTED_EDGE('',*,*,#4818,.F.);
#7193=ORIENTED_EDGE('',*,*,#4817,.F.);
#7194=ORIENTED_EDGE('',*,*,#4814,.F.);
#7195=ORIENTED_EDGE('',*,*,#4810,.F.);
#7196=ORIENTED_EDGE('',*,*,#4807,.F.);
#7197=ORIENTED_EDGE('',*,*,#4889,.F.);
#7198=ORIENTED_EDGE('',*,*,#4851,.F.);
#7199=ORIENTED_EDGE('',*,*,#4880,.F.);
#7200=ORIENTED_EDGE('',*,*,#4879,.F.);
#7201=ORIENTED_EDGE('',*,*,#4878,.F.);
#7202=ORIENTED_EDGE('',*,*,#4877,.F.);
#7203=ORIENTED_EDGE('',*,*,#4876,.F.);
#7204=ORIENTED_EDGE('',*,*,#4875,.F.);
#7205=ORIENTED_EDGE('',*,*,#4874,.F.);
#7206=ORIENTED_EDGE('',*,*,#4873,.F.);
#7207=ORIENTED_EDGE('',*,*,#4872,.F.);
#7208=ORIENTED_EDGE('',*,*,#4871,.F.);
#7209=ORIENTED_EDGE('',*,*,#4870,.F.);
#7210=ORIENTED_EDGE('',*,*,#4869,.F.);
#7211=ORIENTED_EDGE('',*,*,#4868,.F.);
#7212=ORIENTED_EDGE('',*,*,#4886,.T.);
#7213=ORIENTED_EDGE('',*,*,#4866,.F.);
#7214=ORIENTED_EDGE('',*,*,#4865,.F.);
#7215=ORIENTED_EDGE('',*,*,#4864,.F.);
#7216=ORIENTED_EDGE('',*,*,#4863,.F.);
#7217=ORIENTED_EDGE('',*,*,#4862,.F.);
#7218=ORIENTED_EDGE('',*,*,#4861,.F.);
#7219=ORIENTED_EDGE('',*,*,#4860,.F.);
#7220=ORIENTED_EDGE('',*,*,#4859,.F.);
#7221=ORIENTED_EDGE('',*,*,#4858,.F.);
#7222=ORIENTED_EDGE('',*,*,#4857,.F.);
#7223=ORIENTED_EDGE('',*,*,#4856,.F.);
#7224=ORIENTED_EDGE('',*,*,#4855,.F.);
#7225=ORIENTED_EDGE('',*,*,#4854,.F.);
#7226=ORIENTED_EDGE('',*,*,#4853,.F.);
#7227=ORIENTED_EDGE('',*,*,#4890,.F.);
#7228=ORIENTED_EDGE('',*,*,#4891,.T.);
#7229=ORIENTED_EDGE('',*,*,#4805,.T.);
#7230=ORIENTED_EDGE('',*,*,#4809,.T.);
#7231=ORIENTED_EDGE('',*,*,#4813,.T.);
#7232=ORIENTED_EDGE('',*,*,#4812,.T.);
#7233=ORIENTED_EDGE('',*,*,#4816,.T.);
#7234=ORIENTED_EDGE('',*,*,#4820,.T.);
#7235=ORIENTED_EDGE('',*,*,#4824,.T.);
#7236=ORIENTED_EDGE('',*,*,#4828,.T.);
#7237=ORIENTED_EDGE('',*,*,#4827,.T.);
#7238=ORIENTED_EDGE('',*,*,#4831,.T.);
#7239=ORIENTED_EDGE('',*,*,#4834,.T.);
#7240=ORIENTED_EDGE('',*,*,#4838,.T.);
#7241=ORIENTED_EDGE('',*,*,#4837,.T.);
#7242=ORIENTED_EDGE('',*,*,#4842,.T.);
#7243=ORIENTED_EDGE('',*,*,#4841,.T.);
#7244=ORIENTED_EDGE('',*,*,#4846,.T.);
#7245=ORIENTED_EDGE('',*,*,#4849,.T.);
#7246=ORIENTED_EDGE('',*,*,#4883,.T.);
#7247=ORIENTED_EDGE('',*,*,#4884,.T.);
#7248=ORIENTED_EDGE('',*,*,#4892,.F.);
#7249=ORIENTED_EDGE('',*,*,#4893,.T.);
#7250=ORIENTED_EDGE('',*,*,#4894,.T.);
#7251=ORIENTED_EDGE('',*,*,#4895,.F.);
#7252=ORIENTED_EDGE('',*,*,#4896,.F.);
#7253=ORIENTED_EDGE('',*,*,#4897,.T.);
#7254=ORIENTED_EDGE('',*,*,#4898,.T.);
#7255=ORIENTED_EDGE('',*,*,#4893,.F.);
#7256=ORIENTED_EDGE('',*,*,#4899,.F.);
#7257=ORIENTED_EDGE('',*,*,#4900,.T.);
#7258=ORIENTED_EDGE('',*,*,#4901,.T.);
#7259=ORIENTED_EDGE('',*,*,#4897,.F.);
#7260=ORIENTED_EDGE('',*,*,#4902,.F.);
#7261=ORIENTED_EDGE('',*,*,#4903,.T.);
#7262=ORIENTED_EDGE('',*,*,#4904,.T.);
#7263=ORIENTED_EDGE('',*,*,#4900,.F.);
#7264=ORIENTED_EDGE('',*,*,#4905,.F.);
#7265=ORIENTED_EDGE('',*,*,#4906,.T.);
#7266=ORIENTED_EDGE('',*,*,#4907,.T.);
#7267=ORIENTED_EDGE('',*,*,#4903,.F.);
#7268=ORIENTED_EDGE('',*,*,#4908,.F.);
#7269=ORIENTED_EDGE('',*,*,#4895,.T.);
#7270=ORIENTED_EDGE('',*,*,#4909,.T.);
#7271=ORIENTED_EDGE('',*,*,#4906,.F.);
#7272=ORIENTED_EDGE('',*,*,#4909,.F.);
#7273=ORIENTED_EDGE('',*,*,#4894,.F.);
#7274=ORIENTED_EDGE('',*,*,#4898,.F.);
#7275=ORIENTED_EDGE('',*,*,#4901,.F.);
#7276=ORIENTED_EDGE('',*,*,#4904,.F.);
#7277=ORIENTED_EDGE('',*,*,#4907,.F.);
#7278=ORIENTED_EDGE('',*,*,#4910,.T.);
#7279=ORIENTED_EDGE('',*,*,#4889,.T.);
#7280=ORIENTED_EDGE('',*,*,#4806,.T.);
#7281=ORIENTED_EDGE('',*,*,#4891,.F.);
#7282=ORIENTED_EDGE('',*,*,#4890,.T.);
#7283=ORIENTED_EDGE('',*,*,#4852,.F.);
#7284=ORIENTED_EDGE('',*,*,#4910,.F.);
#7285=ORIENTED_EDGE('',*,*,#4911,.T.);
#7286=ORIENTED_EDGE('',*,*,#4912,.T.);
#7287=ORIENTED_EDGE('',*,*,#4911,.F.);
#7288=ORIENTED_EDGE('',*,*,#4912,.F.);
#7289=ORIENTED_EDGE('',*,*,#4892,.T.);
#7290=ORIENTED_EDGE('',*,*,#4908,.T.);
#7291=ORIENTED_EDGE('',*,*,#4905,.T.);
#7292=ORIENTED_EDGE('',*,*,#4902,.T.);
#7293=ORIENTED_EDGE('',*,*,#4899,.T.);
#7294=ORIENTED_EDGE('',*,*,#4896,.T.);
#7295=ORIENTED_EDGE('',*,*,#4888,.T.);
#7832=CYLINDRICAL_SURFACE('',#8811,1.5555);
#7833=CYLINDRICAL_SURFACE('',#8813,1.5555);
#7834=CYLINDRICAL_SURFACE('',#8814,1.5555);
#7835=CYLINDRICAL_SURFACE('',#8815,1.5555);
#7836=CYLINDRICAL_SURFACE('',#8816,1.5555);
#7837=CYLINDRICAL_SURFACE('',#8817,1.5555);
#7838=CYLINDRICAL_SURFACE('',#8818,1.5555);
#7839=CYLINDRICAL_SURFACE('',#8819,1.5555);
#7840=CYLINDRICAL_SURFACE('',#8820,1.5555);
#7841=CYLINDRICAL_SURFACE('',#8821,1.5555);
#7842=CYLINDRICAL_SURFACE('',#8822,1.5555);
#7843=CYLINDRICAL_SURFACE('',#8823,1.5555);
#7844=CYLINDRICAL_SURFACE('',#8824,1.5555);
#7845=CYLINDRICAL_SURFACE('',#8825,1.954);
#7846=CYLINDRICAL_SURFACE('',#8828,1.5555);
#7847=CYLINDRICAL_SURFACE('',#8841,3.5);
#8164=ADVANCED_FACE('',(#1427),#7832,.T.);
#8165=ADVANCED_FACE('',(#1428),#7833,.T.);
#8166=ADVANCED_FACE('',(#1429),#7834,.T.);
#8167=ADVANCED_FACE('',(#1430),#7835,.T.);
#8168=ADVANCED_FACE('',(#1431),#7836,.T.);
#8169=ADVANCED_FACE('',(#1432),#7837,.T.);
#8170=ADVANCED_FACE('',(#1433),#7838,.T.);
#8171=ADVANCED_FACE('',(#1434),#7839,.T.);
#8172=ADVANCED_FACE('',(#1435),#7840,.T.);
#8173=ADVANCED_FACE('',(#1436),#7841,.T.);
#8174=ADVANCED_FACE('',(#1437),#7842,.T.);
#8175=ADVANCED_FACE('',(#1438),#7843,.T.);
#8176=ADVANCED_FACE('',(#1439),#7844,.T.);
#8177=ADVANCED_FACE('',(#1440),#7845,.T.);
#8178=ADVANCED_FACE('',(#1441),#7846,.T.);
#8179=ADVANCED_FACE('',(#1442),#153,.T.);
#8180=ADVANCED_FACE('',(#1443),#164,.F.);
#8181=ADVANCED_FACE('',(#1444),#165,.F.);
#8182=ADVANCED_FACE('',(#1445),#1141,.F.);
#8183=ADVANCED_FACE('',(#1446),#1142,.F.);
#8184=ADVANCED_FACE('',(#1447),#1143,.F.);
#8185=ADVANCED_FACE('',(#1448),#1144,.F.);
#8186=ADVANCED_FACE('',(#1449),#1145,.F.);
#8187=ADVANCED_FACE('',(#1450),#1146,.F.);
#8188=ADVANCED_FACE('',(#1451),#1147,.F.);
#8189=ADVANCED_FACE('',(#1452,#1045),#1148,.T.);
#8190=ADVANCED_FACE('',(#1453),#7847,.T.);
#8191=ADVANCED_FACE('',(#1454,#1046),#1149,.F.);
#8192=ADVANCED_FACE('',(#1455),#1150,.T.);
#8262=CLOSED_SHELL('',(#8164,#8165,#8166,#8167,#8168,#8169,#8170,#8171,
#8172,#8173,#8174,#8175,#8176,#8177,#8178,#8179,#8180,#8181,#8182,#8183,
#8184,#8185,#8186,#8187,#8188,#8189,#8190,#8191,#8192));
#8810=AXIS2_PLACEMENT_3D('',#70395,#10020,#10021);
#8811=AXIS2_PLACEMENT_3D('',#70396,#10022,#10023);
#8812=AXIS2_PLACEMENT_3D('',#70554,#10025,#10026);
#8813=AXIS2_PLACEMENT_3D('',#70667,#10027,#10028);
#8814=AXIS2_PLACEMENT_3D('',#71049,#10030,#10031);
#8815=AXIS2_PLACEMENT_3D('',#71452,#10033,#10034);
#8816=AXIS2_PLACEMENT_3D('',#71843,#10036,#10037);
#8817=AXIS2_PLACEMENT_3D('',#72215,#10039,#10040);
#8818=AXIS2_PLACEMENT_3D('',#72597,#10042,#10043);
#8819=AXIS2_PLACEMENT_3D('',#72988,#10045,#10046);
#8820=AXIS2_PLACEMENT_3D('',#73205,#10048,#10049);
#8821=AXIS2_PLACEMENT_3D('',#73643,#10051,#10052);
#8822=AXIS2_PLACEMENT_3D('',#74036,#10054,#10055);
#8823=AXIS2_PLACEMENT_3D('',#74448,#10057,#10058);
#8824=AXIS2_PLACEMENT_3D('',#74834,#10060,#10061);
#8825=AXIS2_PLACEMENT_3D('',#75199,#10063,#10064);
#8826=AXIS2_PLACEMENT_3D('',#75264,#10065,#10066);
#8827=AXIS2_PLACEMENT_3D('',#76652,#10067,#10068);
#8828=AXIS2_PLACEMENT_3D('',#77803,#10069,#10070);
#8829=AXIS2_PLACEMENT_3D('',#77951,#10071,#10072);
#8830=AXIS2_PLACEMENT_3D('',#78064,#10073,#10074);
#8831=AXIS2_PLACEMENT_3D('',#78222,#10076,#10077);
#8832=AXIS2_PLACEMENT_3D('',#79107,#10078,#10079);
#8833=AXIS2_PLACEMENT_3D('',#79116,#10084,#10085);
#8834=AXIS2_PLACEMENT_3D('',#79122,#10089,#10090);
#8835=AXIS2_PLACEMENT_3D('',#79128,#10094,#10095);
#8836=AXIS2_PLACEMENT_3D('',#79134,#10099,#10100);
#8837=AXIS2_PLACEMENT_3D('',#79140,#10104,#10105);
#8838=AXIS2_PLACEMENT_3D('',#79143,#10108,#10109);
#8839=AXIS2_PLACEMENT_3D('',#79144,#10110,#10111);
#8840=AXIS2_PLACEMENT_3D('',#79146,#10112,#10113);
#8841=AXIS2_PLACEMENT_3D('',#79147,#10114,#10115);
#8842=AXIS2_PLACEMENT_3D('',#79150,#10117,#10118);
#8843=AXIS2_PLACEMENT_3D('',#79151,#10119,#10120);
#8844=AXIS2_PLACEMENT_3D('',#79152,#10121,#10122);
#10020=DIRECTION('axis',(0.,0.,1.));
#10021=DIRECTION('refdir',(1.,0.,0.));
#10022=DIRECTION('center_axis',(0.,0.,1.));
#10023=DIRECTION('ref_axis',(1.,9.40280585438808E-14,0.));
#10024=DIRECTION('',(0.,0.,-1.));
#10025=DIRECTION('center_axis',(0.,0.,-1.));
#10026=DIRECTION('ref_axis',(1.,9.40280585438808E-14,0.));
#10027=DIRECTION('center_axis',(0.,0.,1.));
#10028=DIRECTION('ref_axis',(1.,9.40280585438808E-14,0.));
#10029=DIRECTION('',(0.,0.,-1.));
#10030=DIRECTION('center_axis',(0.,0.,1.));
#10031=DIRECTION('ref_axis',(1.,9.40280585438808E-14,0.));
#10032=DIRECTION('',(0.,0.,-1.));
#10033=DIRECTION('center_axis',(0.,0.,1.));
#10034=DIRECTION('ref_axis',(1.,9.40280585438808E-14,0.));
#10035=DIRECTION('',(0.,0.,-1.));
#10036=DIRECTION('center_axis',(0.,0.,1.));
#10037=DIRECTION('ref_axis',(1.,9.40280585438808E-14,0.));
#10038=DIRECTION('',(0.,0.,-1.));
#10039=DIRECTION('center_axis',(0.,0.,1.));
#10040=DIRECTION('ref_axis',(1.,9.40280585438808E-14,0.));
#10041=DIRECTION('',(0.,0.,-1.));
#10042=DIRECTION('center_axis',(0.,0.,1.));
#10043=DIRECTION('ref_axis',(1.,9.40280585438808E-14,0.));
#10044=DIRECTION('',(0.,0.,-1.));
#10045=DIRECTION('center_axis',(0.,0.,1.));
#10046=DIRECTION('ref_axis',(1.,9.40280585438808E-14,0.));
#10047=DIRECTION('',(0.,0.,-1.));
#10048=DIRECTION('center_axis',(0.,0.,1.));
#10049=DIRECTION('ref_axis',(1.,9.40280585438808E-14,0.));
#10050=DIRECTION('',(0.,0.,-1.));
#10051=DIRECTION('center_axis',(0.,0.,1.));
#10052=DIRECTION('ref_axis',(1.,9.40280585438808E-14,0.));
#10053=DIRECTION('',(0.,0.,-1.));
#10054=DIRECTION('center_axis',(0.,0.,1.));
#10055=DIRECTION('ref_axis',(1.,9.40280585438808E-14,0.));
#10056=DIRECTION('',(0.,0.,-1.));
#10057=DIRECTION('center_axis',(0.,0.,1.));
#10058=DIRECTION('ref_axis',(1.,9.40280585438808E-14,0.));
#10059=DIRECTION('',(0.,0.,-1.));
#10060=DIRECTION('center_axis',(0.,0.,1.));
#10061=DIRECTION('ref_axis',(1.,9.40280585438808E-14,0.));
#10062=DIRECTION('',(0.,0.,-1.));
#10063=DIRECTION('center_axis',(0.,0.,1.));
#10064=DIRECTION('ref_axis',(1.,0.,0.));
#10065=DIRECTION('center_axis',(0.,0.,-1.));
#10066=DIRECTION('ref_axis',(1.,0.,0.));
#10067=DIRECTION('center_axis',(0.,0.,-1.));
#10068=DIRECTION('ref_axis',(1.,0.,0.));
#10069=DIRECTION('center_axis',(0.,0.,1.));
#10070=DIRECTION('ref_axis',(1.,9.40280585438808E-14,0.));
#10071=DIRECTION('center_axis',(0.,0.,-1.));
#10072=DIRECTION('ref_axis',(1.,9.40280585438808E-14,0.));
#10073=DIRECTION('center_axis',(0.,0.,-1.));
#10074=DIRECTION('ref_axis',(1.,0.,0.));
#10075=DIRECTION('',(0.707106781186548,-8.65956056235494E-17,0.707106781186547));
#10076=DIRECTION('center_axis',(0.,0.,1.));
#10077=DIRECTION('ref_axis',(1.,0.,0.));
#10078=DIRECTION('center_axis',(-1.60246890531964E-16,-1.,0.));
#10079=DIRECTION('ref_axis',(1.,-1.60246890531964E-16,0.));
#10080=DIRECTION('',(1.,-1.60246890531964E-16,0.));
#10081=DIRECTION('',(0.,0.,1.));
#10082=DIRECTION('',(1.,-1.60246890531964E-16,0.));
#10083=DIRECTION('',(0.,0.,1.));
#10084=DIRECTION('center_axis',(-0.866025403784439,-0.5,0.));
#10085=DIRECTION('ref_axis',(0.5,-0.866025403784439,0.));
#10086=DIRECTION('',(0.5,-0.866025403784439,0.));
#10087=DIRECTION('',(0.,0.,1.));
#10088=DIRECTION('',(0.5,-0.866025403784439,0.));
#10089=DIRECTION('center_axis',(-0.866025403784439,0.5,0.));
#10090=DIRECTION('ref_axis',(-0.5,-0.866025403784439,0.));
#10091=DIRECTION('',(-0.5,-0.866025403784439,0.));
#10092=DIRECTION('',(0.,0.,1.));
#10093=DIRECTION('',(-0.5,-0.866025403784439,0.));
#10094=DIRECTION('center_axis',(1.60246890531964E-16,1.,0.));
#10095=DIRECTION('ref_axis',(-1.,1.60246890531964E-16,0.));
#10096=DIRECTION('',(-1.,1.60246890531964E-16,0.));
#10097=DIRECTION('',(0.,0.,1.));
#10098=DIRECTION('',(-1.,1.60246890531964E-16,0.));
#10099=DIRECTION('center_axis',(0.866025403784439,0.5,0.));
#10100=DIRECTION('ref_axis',(-0.5,0.866025403784439,0.));
#10101=DIRECTION('',(-0.5,0.866025403784439,0.));
#10102=DIRECTION('',(0.,0.,1.));
#10103=DIRECTION('',(-0.5,0.866025403784439,0.));
#10104=DIRECTION('center_axis',(0.866025403784439,-0.5,0.));
#10105=DIRECTION('ref_axis',(0.5,0.866025403784439,0.));
#10106=DIRECTION('',(0.5,0.866025403784439,0.));
#10107=DIRECTION('',(0.5,0.866025403784439,0.));
#10108=DIRECTION('center_axis',(0.,0.,1.));
#10109=DIRECTION('ref_axis',(1.,0.,0.));
#10110=DIRECTION('center_axis',(0.,0.,1.));
#10111=DIRECTION('ref_axis',(1.,0.,0.));
#10112=DIRECTION('center_axis',(0.,0.,1.));
#10113=DIRECTION('ref_axis',(1.,0.,0.));
#10114=DIRECTION('center_axis',(0.,0.,1.));
#10115=DIRECTION('ref_axis',(1.,0.,0.));
#10116=DIRECTION('',(0.,0.,-1.));
#10117=DIRECTION('center_axis',(0.,0.,1.));
#10118=DIRECTION('ref_axis',(1.,0.,0.));
#10119=DIRECTION('center_axis',(0.,0.,1.));
#10120=DIRECTION('ref_axis',(1.,0.,0.));
#10121=DIRECTION('center_axis',(0.,0.,1.));
#10122=DIRECTION('ref_axis',(1.,0.,0.));
#70395=CARTESIAN_POINT('',(0.,0.,0.));
#70396=CARTESIAN_POINT('Origin',(0.,0.,-1.2940562256037));
#70397=CARTESIAN_POINT('',(-1.5555,7.45448211670055E-9,0.595401982137319));
#70398=CARTESIAN_POINT('',(-1.5554996707636,0.00101205451123986,0.455943774396298));
#70399=CARTESIAN_POINT('',(-1.5555,-1.46451138874614E-13,-1.2940562256037));
#70400=CARTESIAN_POINT('',(-0.88780425057628,-1.27725638094264,5.87637577487143E-16));
#70401=CARTESIAN_POINT('Ctrl Pts',(-1.5555,7.45448211670055E-9,0.595401982137319));
#70402=CARTESIAN_POINT('Ctrl Pts',(-1.55549999991128,0.018512536755729,
0.594032592656952));
#70403=CARTESIAN_POINT('Ctrl Pts',(-1.55516951495068,0.0370244920773043,
0.592653507332298));
#70404=CARTESIAN_POINT('Ctrl Pts',(-1.55237186799618,0.115346003264795,
0.586777551248481));
#70405=CARTESIAN_POINT('Ctrl Pts',(-1.54678433317852,0.174985822388469,
0.582198572384768));
#70406=CARTESIAN_POINT('Ctrl Pts',(-1.52375452305799,0.326233632272393,
0.570378927484362));
#70407=CARTESIAN_POINT('Ctrl Pts',(-1.50149047938202,0.416873764313208,
0.563089890526641));
#70408=CARTESIAN_POINT('Ctrl Pts',(-1.46287086095033,0.529391380345427,
0.554092311366315));
#70409=CARTESIAN_POINT('Ctrl Pts',(-1.45388505621647,0.553592655730208,
0.552161188814886));
#70410=CARTESIAN_POINT('Ctrl Pts',(-1.44064757834529,0.586695484464925,
0.549535696586906));
#70411=CARTESIAN_POINT('Ctrl Pts',(-1.43690799387877,0.595795658877528,
0.548815630057317));
#70412=CARTESIAN_POINT('Ctrl Pts',(-1.43050774584853,0.610959631805391,
0.547619323005683));
#70413=CARTESIAN_POINT('Ctrl Pts',(-1.42789429642329,0.617042922146608,
0.547140378815347));
#70414=CARTESIAN_POINT('Ctrl Pts',(-1.42237010685853,0.629678430730447,
0.546147849258026));
#70415=CARTESIAN_POINT('Ctrl Pts',(-1.41945279032853,0.636227497509268,
0.54563466220687));
#70416=CARTESIAN_POINT('Ctrl Pts',(-1.41147967660201,0.653798444662134,
0.544260540807749));
#70417=CARTESIAN_POINT('Ctrl Pts',(-1.40633998288666,0.664782039701448,
0.543404502975092));
#70418=CARTESIAN_POINT('Ctrl Pts',(-1.37662258287187,0.726400987288663,
0.538612318112056));
#70419=CARTESIAN_POINT('Ctrl Pts',(-1.34943636016353,0.775739114277784,
0.534814000768419));
#70420=CARTESIAN_POINT('Ctrl Pts',(-1.2575048081127,0.92305641873251,0.523260613003983));
#70421=CARTESIAN_POINT('Ctrl Pts',(-1.1843140339995,1.01525952376867,0.515692469820306));
#70422=CARTESIAN_POINT('Ctrl Pts',(-1.07406526773624,1.12581890886688,0.505129782754011));
#70423=CARTESIAN_POINT('Ctrl Pts',(-1.04566431181909,1.1522457006782,0.50247275350819));
#70424=CARTESIAN_POINT('Ctrl Pts',(-1.00396914072051,1.18823054923343,0.498636166169495));
#70425=CARTESIAN_POINT('Ctrl Pts',(-0.991464697438271,1.19868410853647,
0.497493362131378));
#70426=CARTESIAN_POINT('Ctrl Pts',(-0.969731759193258,1.21627984611124,
0.495518793479236));
#70427=CARTESIAN_POINT('Ctrl Pts',(-0.960582736146466,1.22351834574391,
0.4946909868274));
#70428=CARTESIAN_POINT('Ctrl Pts',(-0.94160356329022,1.23819014938679,0.492980195222397));
#70429=CARTESIAN_POINT('Ctrl Pts',(-0.93176478916661,1.24561088543581,0.492096792847722));
#70430=CARTESIAN_POINT('Ctrl Pts',(-0.90644772642809,1.26423807303257,0.489831747582821));
#70431=CARTESIAN_POINT('Ctrl Pts',(-0.890849618589299,1.27527733557657,
0.488443798170784));
#70432=CARTESIAN_POINT('Ctrl Pts',(-0.81716620132816,1.32541386096325,0.48191916643826));
#70433=CARTESIAN_POINT('Ctrl Pts',(-0.756695027176243,1.3608425814421,0.476649753070564));
#70434=CARTESIAN_POINT('Ctrl Pts',(-0.641075964976838,1.41848718470827,
0.46674807880466));
#70435=CARTESIAN_POINT('Ctrl Pts',(-0.586637715584596,1.44185294601319,
0.462152121432829));
#70436=CARTESIAN_POINT('Ctrl Pts',(-0.460195370473517,1.48777537284252,
0.451724442026016));
#70437=CARTESIAN_POINT('Ctrl Pts',(-0.38760459272556,1.50831713593063,0.445909124683959));
#70438=CARTESIAN_POINT('Ctrl Pts',(-0.30131759167514,1.52608992990789,0.439377069921943));
#70439=CARTESIAN_POINT('Ctrl Pts',(-0.288799865526645,1.52850823710081,
0.438438761604621));
#70440=CARTESIAN_POINT('Ctrl Pts',(-0.269058926096808,1.53207081720116,
0.436975061610269));
#70441=CARTESIAN_POINT('Ctrl Pts',(-0.261855295105846,1.53331846168122,
0.436444292094167));
#70442=CARTESIAN_POINT('Ctrl Pts',(-0.248061104849824,1.5356075187817,0.435434657553588));
#70443=CARTESIAN_POINT('Ctrl Pts',(-0.241472285230778,1.53665737914733,
0.43495536941656));
#70444=CARTESIAN_POINT('Ctrl Pts',(-0.225363062773822,1.53911804710218,
0.433790379706224));
#70445=CARTESIAN_POINT('Ctrl Pts',(-0.215835724210277,1.54048298454096,
0.433107183462439));
#70446=CARTESIAN_POINT('Ctrl Pts',(-0.180539056426624,1.5452058754826,0.430595463113567));
#70447=CARTESIAN_POINT('Ctrl Pts',(-0.15469786646918,1.54800656233667,0.428794695553193));
#70448=CARTESIAN_POINT('Ctrl Pts',(-0.0858993015172276,1.55372277386261,
0.424072194382331));
#70449=CARTESIAN_POINT('Ctrl Pts',(-0.0428691974083889,1.55550503236974,
0.421192210095358));
#70450=CARTESIAN_POINT('Ctrl Pts',(0.132688724120503,1.55548446751562,0.4095484119285));
#70451=CARTESIAN_POINT('Ctrl Pts',(0.264638307722797,1.53853916396096,0.400991220938502));
#70452=CARTESIAN_POINT('Ctrl Pts',(0.415506462100098,1.4991608657509,0.39025704443433));
#70453=CARTESIAN_POINT('Ctrl Pts',(0.438033282177534,1.49273429176367,0.388630102732755));
#70454=CARTESIAN_POINT('Ctrl Pts',(0.473175653277626,1.48184472478897,0.38604897608951));
#70455=CARTESIAN_POINT('Ctrl Pts',(0.485893958995597,1.47772325824553,0.385105867372256));
#70456=CARTESIAN_POINT('Ctrl Pts',(0.509500094666379,1.46973581296729,0.383337735438035));
#70457=CARTESIAN_POINT('Ctrl Pts',(0.520401108730382,1.46591144999129,0.382514134483903));
#70458=CARTESIAN_POINT('Ctrl Pts',(0.54471711145105,1.45707535118003,0.380660497474331));
#70459=CARTESIAN_POINT('Ctrl Pts',(0.558107361196416,1.45199912480921,0.379628374460689));
#70460=CARTESIAN_POINT('Ctrl Pts',(0.598375626252592,1.4360941803677,0.376488887218452));
#70461=CARTESIAN_POINT('Ctrl Pts',(0.625021551629308,1.42469917446781,0.37436284958701));
#70462=CARTESIAN_POINT('Ctrl Pts',(0.722136309462623,1.37991974350355,0.36642767293284));
#70463=CARTESIAN_POINT('Ctrl Pts',(0.79037583793247,1.34199936042264,0.360473755592434));
#70464=CARTESIAN_POINT('Ctrl Pts',(0.938568680933969,1.24441433692573,0.346753356577317));
#70465=CARTESIAN_POINT('Ctrl Pts',(1.01622283282754,1.18185090609348,0.338965801117648));
#70466=CARTESIAN_POINT('Ctrl Pts',(1.10105389802654,1.09892067214589,0.330072917079713));
#70467=CARTESIAN_POINT('Ctrl Pts',(1.11448842922287,1.08529348940666,0.328652143885256));
#70468=CARTESIAN_POINT('Ctrl Pts',(1.13349527551604,1.06528881641021,0.326628207776626));
#70469=CARTESIAN_POINT('Ctrl Pts',(1.13927174794241,1.05910891561717,0.326011190445906));
#70470=CARTESIAN_POINT('Ctrl Pts',(1.14939584061324,1.04809907534924,0.324926851646702));
#70471=CARTESIAN_POINT('Ctrl Pts',(1.15376405127621,1.0432885461509,0.324458030585922));
#70472=CARTESIAN_POINT('Ctrl Pts',(1.16328037687154,1.03267573604481,0.323434671989912));
#70473=CARTESIAN_POINT('Ctrl Pts',(1.16841539625678,1.02686215226696,0.322881087351371));
#70474=CARTESIAN_POINT('Ctrl Pts',(1.18342712058944,1.0096082982659,0.321257765399967));
#70475=CARTESIAN_POINT('Ctrl Pts',(1.19318116961843,0.998061825311609,0.3201965354114));
#70476=CARTESIAN_POINT('Ctrl Pts',(1.23919303860226,0.941955846171118,0.315148492212561));
#70477=CARTESIAN_POINT('Ctrl Pts',(1.27313597606693,0.895548151661867,0.311295152234127));
#70478=CARTESIAN_POINT('Ctrl Pts',(1.37878874923958,0.73290568892236,0.298443712833807));
#70479=CARTESIAN_POINT('Ctrl Pts',(1.43774765055429,0.609170710372294,0.289660951708166));
#70480=CARTESIAN_POINT('Ctrl Pts',(1.48686138503173,0.457545515182043,0.278687813794266));
#70481=CARTESIAN_POINT('Ctrl Pts',(1.49343589198353,0.435607413818198,0.277097145248795));
#70482=CARTESIAN_POINT('Ctrl Pts',(1.50302646506023,0.400830782301211,0.274566387022329));
#70483=CARTESIAN_POINT('Ctrl Pts',(1.50636782967047,0.388084801519073,0.273636930102327));
#70484=CARTESIAN_POINT('Ctrl Pts',(1.51230688445424,0.364196385176079,0.271890591354906));
#70485=CARTESIAN_POINT('Ctrl Pts',(1.51494436661361,0.353064686497044,0.27107506806126));
#70486=CARTESIAN_POINT('Ctrl Pts',(1.52058979791986,0.32800888237305,0.269235007957275));
#70487=CARTESIAN_POINT('Ctrl Pts',(1.52352969850585,0.314070681402649,0.268208346795258));
#70488=CARTESIAN_POINT('Ctrl Pts',(1.53187889563939,0.271606746280942,0.265070235771341));
#70489=CARTESIAN_POINT('Ctrl Pts',(1.53668106773495,0.24296967142752,0.262939763969736));
#70490=CARTESIAN_POINT('Ctrl Pts',(1.55132022252328,0.137682663825198,0.255050320854012));
#70491=CARTESIAN_POINT('Ctrl Pts',(1.55624257647875,0.0604726876665596,
0.249148574607311));
#70492=CARTESIAN_POINT('Ctrl Pts',(1.55434498185425,-0.115492583717271,
0.235537249635111));
#70493=CARTESIAN_POINT('Ctrl Pts',(1.54388465414917,-0.213890375967072,
0.227805643155988));
#70494=CARTESIAN_POINT('Ctrl Pts',(1.52019922850531,-0.330104994002925,
0.218902583673613));
#70495=CARTESIAN_POINT('Ctrl Pts',(1.5158585891988,-0.349496546515298,0.217425528013309));
#70496=CARTESIAN_POINT('Ctrl Pts',(1.50912003263549,-0.37710753046299,0.21533953110097));
#70497=CARTESIAN_POINT('Ctrl Pts',(1.50702421265426,-0.385397708914141,
0.21471544280655));
#70498=CARTESIAN_POINT('Ctrl Pts',(1.50321306886298,-0.399966336773176,
0.213623148259265));
#70499=CARTESIAN_POINT('Ctrl Pts',(1.50152656928863,-0.4062518530699,0.213153379347063));
#70500=CARTESIAN_POINT('Ctrl Pts',(1.49775147457336,-0.419976747098681,
0.212130911627952));
#70501=CARTESIAN_POINT('Ctrl Pts',(1.49564684797744,-0.427411348270103,
0.211579128792934));
#70502=CARTESIAN_POINT('Ctrl Pts',(1.48936534280459,-0.448986082588979,
0.209983097985466));
#70503=CARTESIAN_POINT('Ctrl Pts',(1.48504258151533,-0.463083361146562,
0.208946758638793));
#70504=CARTESIAN_POINT('Ctrl Pts',(1.45306499014261,-0.562311406876981,
0.201684382466008));
#70505=CARTESIAN_POINT('Ctrl Pts',(1.41830384723797,-0.644988908568745,
0.195796136088718));
#70506=CARTESIAN_POINT('Ctrl Pts',(1.32837295625108,-0.815930663028428,
0.183085549891426));
#70507=CARTESIAN_POINT('Ctrl Pts',(1.27109152562521,-0.902574474924967,
0.17628313238586));
#70508=CARTESIAN_POINT('Ctrl Pts',(1.19048746772787,-1.0014458786914,0.167506298012972));
#70509=CARTESIAN_POINT('Ctrl Pts',(1.17492252825074,-1.01966229960277,0.165842849505779));
#70510=CARTESIAN_POINT('Ctrl Pts',(1.14993525016314,-1.04757414413541,0.163215015903657));
#70511=CARTESIAN_POINT('Ctrl Pts',(1.14079626986148,-1.05751903870457,0.162262347650834));
#70512=CARTESIAN_POINT('Ctrl Pts',(1.1235866109884,-1.07576361831739,0.160482980427928));
#70513=CARTESIAN_POINT('Ctrl Pts',(1.11555048431325,-1.08409470923548,0.159657796531519));
#70514=CARTESIAN_POINT('Ctrl Pts',(1.0974314557056,-1.1024639954418,0.157809285018915));
#70515=CARTESIAN_POINT('Ctrl Pts',(1.08730241453723,-1.11245498591742,0.156783972140584));
#70516=CARTESIAN_POINT('Ctrl Pts',(1.05657317118804,-1.14194479017135,0.153696185763408));
#70517=CARTESIAN_POINT('Ctrl Pts',(1.03557625211531,-1.16101955304724,0.151616076757967));
#70518=CARTESIAN_POINT('Ctrl Pts',(0.961915534494003,-1.22434862727732,
0.144413579078096));
#70519=CARTESIAN_POINT('Ctrl Pts',(0.906850190899483,-1.26567436622153,
0.139184051067798));
#70520=CARTESIAN_POINT('Ctrl Pts',(0.77932044943164,-1.34877878841218,0.127455334698482));
#70521=CARTESIAN_POINT('Ctrl Pts',(0.705850183141632,-1.38863971415017,
0.12093952742659));
#70522=CARTESIAN_POINT('Ctrl Pts',(0.594824432243085,-1.43777784001647,
0.111664302209529));
#70523=CARTESIAN_POINT('Ctrl Pts',(0.559557982843611,-1.45186659868798,
0.108797965180966));
#70524=CARTESIAN_POINT('Ctrl Pts',(0.513165740206983,-1.46845800852058,
0.105158298394703));
#70525=CARTESIAN_POINT('Ctrl Pts',(0.502481638082137,-1.47214816607982,
0.104328928711061));
#70526=CARTESIAN_POINT('Ctrl Pts',(0.485733325520589,-1.47772924169189,
0.103043570040798));
#70527=CARTESIAN_POINT('Ctrl Pts',(0.479696407299655,-1.4796999480139,0.102583234316208));
#70528=CARTESIAN_POINT('Ctrl Pts',(0.467059967417248,-1.48373955475198,
0.101626097413697));
#70529=CARTESIAN_POINT('Ctrl Pts',(0.460458355077576,-1.48580153037768,
0.101129706915055));
#70530=CARTESIAN_POINT('Ctrl Pts',(0.443989228673884,-1.49082525710952,
0.0998998893963307));
#70531=CARTESIAN_POINT('Ctrl Pts',(0.434105455498511,-1.49373319261437,
0.0991694173315211));
#70532=CARTESIAN_POINT('Ctrl Pts',(0.395090628935827,-1.50479189613147,
0.0963130647560802));
#70533=CARTESIAN_POINT('Ctrl Pts',(0.365751302103199,-1.51219097026429,
0.0942241858870127));
#70534=CARTESIAN_POINT('Ctrl Pts',(0.282694260721605,-1.53057792609647,
0.0884274226344181));
#70535=CARTESIAN_POINT('Ctrl Pts',(0.228583271129527,-1.53958934235147,
0.0847853164299095));
#70536=CARTESIAN_POINT('Ctrl Pts',(0.0641370703332336,-1.55811210159829,
0.0738323779676044));
#70537=CARTESIAN_POINT('Ctrl Pts',(-0.0468280309652776,-1.55872737574299,
0.0665726339379135));
#70538=CARTESIAN_POINT('Ctrl Pts',(-0.17971458194017,-1.54525341050698,
0.0573627144330893));
#70539=CARTESIAN_POINT('Ctrl Pts',(-0.202459639548319,-1.54243814682873,
0.0557690687999702));
#70540=CARTESIAN_POINT('Ctrl Pts',(-0.23836807715185,-1.53718568105015,
0.0532210487949003));
#70541=CARTESIAN_POINT('Ctrl Pts',(-0.251577002390507,-1.53507920008026,
0.0522768509115466));
#70542=CARTESIAN_POINT('Ctrl Pts',(-0.275173619224738,-1.53100342177695,
0.0505768936094622));
#70543=CARTESIAN_POINT('Ctrl Pts',(-0.285571621136733,-1.52909804703773,
0.0498231723718662));
#70544=CARTESIAN_POINT('Ctrl Pts',(-0.309931777101898,-1.52437705312248,
0.0480460525134765));
#70545=CARTESIAN_POINT('Ctrl Pts',(-0.323876067252991,-1.52147539411363,
0.0470200117010014));
#70546=CARTESIAN_POINT('Ctrl Pts',(-0.365009537565507,-1.51232487739698,
0.0439662258590709));
#70547=CARTESIAN_POINT('Ctrl Pts',(-0.392071328181965,-1.50553591365357,
0.0419217438090517));
#70548=CARTESIAN_POINT('Ctrl Pts',(-0.478070805425748,-1.48148546069609,
0.0353059677852516));
#70549=CARTESIAN_POINT('Ctrl Pts',(-0.536168973236151,-1.46146230507891,
0.0306530148100327));
#70550=CARTESIAN_POINT('Ctrl Pts',(-0.696755658561653,-1.3952509070401,
0.0173030657599812));
#70551=CARTESIAN_POINT('Ctrl Pts',(-0.79562111359592,-1.34133167707247,
0.00847101705034995));
#70552=CARTESIAN_POINT('Ctrl Pts',(-0.88780425057628,-1.27725638094264,
5.87637577487143E-16));
#70553=CARTESIAN_POINT('',(0.903606778650208,-1.26612599672284,0.));
#70554=CARTESIAN_POINT('Origin',(0.,0.,0.));
#70555=CARTESIAN_POINT('Ctrl Pts',(0.903606778650205,-1.26612599672284,
-2.22044604925031E-15));
#70556=CARTESIAN_POINT('Ctrl Pts',(0.951852589186397,-1.23169400373413,
0.00424522636382672));
#70557=CARTESIAN_POINT('Ctrl Pts',(0.998166011006757,-1.19447361099769,
0.00849045272765591));
#70558=CARTESIAN_POINT('Ctrl Pts',(1.04222332457801,-1.15470809805143,0.0127356790914848));
#70559=CARTESIAN_POINT('Ctrl Pts',(1.08625940090756,-1.11496175354151,0.0169788591004388));
#70560=CARTESIAN_POINT('Ctrl Pts',(1.12804116560105,-1.07267304654868,0.0212220391093926));
#70561=CARTESIAN_POINT('Ctrl Pts',(1.16727847323326,-1.02812509741093,0.0254652191183466));
#70562=CARTESIAN_POINT('Ctrl Pts',(1.20650614422342,-0.983588089203271,
0.0297073570066925));
#70563=CARTESIAN_POINT('Ctrl Pts',(1.24319027816322,-0.936793305067274,
0.0339494948950384));
#70564=CARTESIAN_POINT('Ctrl Pts',(1.27707935615917,-0.888058876467136,
0.0381916327833842));
#70565=CARTESIAN_POINT('Ctrl Pts',(1.31097037158942,-0.839321661725895,
0.0424340131942152));
#70566=CARTESIAN_POINT('Ctrl Pts',(1.34206573671913,-0.788644981368028,
0.0466763936050461));
#70567=CARTESIAN_POINT('Ctrl Pts',(1.37015685435733,-0.736376564304986,
0.050918774015877));
#70568=CARTESIAN_POINT('Ctrl Pts',(1.39825808387485,-0.684089332329275,
0.0551626815442565));
#70569=CARTESIAN_POINT('Ctrl Pts',(1.42335268862159,-0.63020965371423,0.0594065890726361));
#70570=CARTESIAN_POINT('Ctrl Pts',(1.4452785167722,-0.575108910517601,0.0636504966010156));
#70571=CARTESIAN_POINT('Ctrl Pts',(1.46723749651958,-0.519924855639086,
0.067900820868144));
#70572=CARTESIAN_POINT('Ctrl Pts',(1.48601795394136,-0.463516502569013,
0.0721511451352726));
#70573=CARTESIAN_POINT('Ctrl Pts',(1.50150660304027,-0.406273517505732,
0.0764014694024009));
#70574=CARTESIAN_POINT('Ctrl Pts',(1.51700725558701,-0.348986170072261,
0.0806550876008007));
#70575=CARTESIAN_POINT('Ctrl Pts',(1.52921091674141,-0.29086337777291,0.0849087057992003));
#70576=CARTESIAN_POINT('Ctrl Pts',(1.5380554381532,-0.232305228454644,0.0891623239976));
#70577=CARTESIAN_POINT('Ctrl Pts',(1.54691876241006,-0.173622588532727,
0.0934249850961493));
#70578=CARTESIAN_POINT('Ctrl Pts',(1.55240863162362,-0.114503227054264,
0.0976876461946983));
#70579=CARTESIAN_POINT('Ctrl Pts',(1.55451484431141,-0.0553520443656737,
0.101950307293247));
#70580=CARTESIAN_POINT('Ctrl Pts',(1.5560237591571,-0.0129754609295238,
0.10500412643079));
#70581=CARTESIAN_POINT('Ctrl Pts',(1.55579713131465,0.0294173901035382,
0.108057945568333));
#70582=CARTESIAN_POINT('Ctrl Pts',(1.55384760097146,0.0716790273038469,
0.111111764705876));
#70583=CARTESIAN_POINT('Ctrl Pts',(1.55122671815316,0.128494146493297,0.115217216121782));
#70584=CARTESIAN_POINT('Ctrl Pts',(1.5454787588811,0.185310342956839,0.119322667537688));
#70585=CARTESIAN_POINT('Ctrl Pts',(1.53659924649562,0.241749882459346,0.123428118953594));
#70586=CARTESIAN_POINT('Ctrl Pts',(1.52769589071,0.298340974261668,0.127544594389351));
#70587=CARTESIAN_POINT('Ctrl Pts',(1.51564409042012,0.354552843155991,0.131661069825108));
#70588=CARTESIAN_POINT('Ctrl Pts',(1.50049208636959,0.410004571611382,0.135777545260865));
#70589=CARTESIAN_POINT('Ctrl Pts',(1.48542844675149,0.465132913107788,0.139870013970232));
#70590=CARTESIAN_POINT('Ctrl Pts',(1.46730077025642,0.519509429534535,0.143962482679598));
#70591=CARTESIAN_POINT('Ctrl Pts',(1.44620795176229,0.57276767564129,0.148054951388965));
#70592=CARTESIAN_POINT('Ctrl Pts',(1.42513055978693,0.625986970607685,0.152144427015856));
#70593=CARTESIAN_POINT('Ctrl Pts',(1.40109251607126,0.678089120794082,0.156233902642746));
#70594=CARTESIAN_POINT('Ctrl Pts',(1.37424213128275,0.72872410047112,0.160323378269637));
#70595=CARTESIAN_POINT('Ctrl Pts',(1.34740052506661,0.779342525345045,0.164411516866983));
#70596=CARTESIAN_POINT('Ctrl Pts',(1.31774865036365,0.82849426020466,0.168499655464329));
#70597=CARTESIAN_POINT('Ctrl Pts',(1.28548137744857,0.87585265783288,0.172587794061675));
#70598=CARTESIAN_POINT('Ctrl Pts',(1.25283388232855,0.923769104305707,0.176724105340849));
#70599=CARTESIAN_POINT('Ctrl Pts',(1.21750922328882,0.969849187380873,0.180860416620023));
#70600=CARTESIAN_POINT('Ctrl Pts',(1.17975365575837,1.01378575731008,0.184996727899197));
#70601=CARTESIAN_POINT('Ctrl Pts',(1.14239287771065,1.0572629063684,0.18908978801577));
#70602=CARTESIAN_POINT('Ctrl Pts',(1.10265221302859,1.0986408140825,0.193182848132343));
#70603=CARTESIAN_POINT('Ctrl Pts',(1.06080812131677,1.13765828777731,0.197275908248916));
#70604=CARTESIAN_POINT('Ctrl Pts',(1.01830078295221,1.17729420502692,0.201433845109391));
#70605=CARTESIAN_POINT('Ctrl Pts',(0.973623180597843,1.21449382674095,0.205591781969865));
#70606=CARTESIAN_POINT('Ctrl Pts',(0.927098415443284,1.24902713264467,0.20974971883034));
#70607=CARTESIAN_POINT('Ctrl Pts',(0.880573650288724,1.28356043854838,0.213907655690814));
#70608=CARTESIAN_POINT('Ctrl Pts',(0.832202237818035,1.31542717887904,0.218065592551289));
#70609=CARTESIAN_POINT('Ctrl Pts',(0.782333459475337,1.34444583683589,0.222223529411763));
#70610=CARTESIAN_POINT('Ctrl Pts',(0.732507149389121,1.3734397825008,0.226377925372803));
#70611=CARTESIAN_POINT('Ctrl Pts',(0.680964149283562,1.39971985823112,0.230532321333844));
#70612=CARTESIAN_POINT('Ctrl Pts',(0.628031163394784,1.42308014806089,0.234686717294884));
#70613=CARTESIAN_POINT('Ctrl Pts',(0.575192226704268,1.44639893226816,0.238833731892435));
#70614=CARTESIAN_POINT('Ctrl Pts',(0.520968677667857,1.46680802087634,0.242980746489986));
#70615=CARTESIAN_POINT('Ctrl Pts',(0.465712498432397,1.48414693302377,0.247127761087537));
#70616=CARTESIAN_POINT('Ctrl Pts',(0.410511312767616,1.50146858866335,0.251270648379445));
#70617=CARTESIAN_POINT('Ctrl Pts',(0.354280026066142,1.51572596806045,0.255413535671353));
#70618=CARTESIAN_POINT('Ctrl Pts',(0.297389711468627,1.52680699812144,0.259556422963261));
#70619=CARTESIAN_POINT('Ctrl Pts',(0.240534338057534,1.53788122237832,0.263696765755315));
#70620=CARTESIAN_POINT('Ctrl Pts',(0.183021247547025,1.54578286595004,0.267837108547369));
#70621=CARTESIAN_POINT('Ctrl Pts',(0.125233629452144,1.55045051132058,0.271977451339423));
#70622=CARTESIAN_POINT('Ctrl Pts',(0.0674594843894061,1.5551170684418,0.276116828821375));
#70623=CARTESIAN_POINT('Ctrl Pts',(0.00941145582046524,1.55655108260044,
0.280256206303327));
#70624=CARTESIAN_POINT('Ctrl Pts',(-0.0485223781685535,1.55474301053803,
0.284395583785279));
#70625=CARTESIAN_POINT('Ctrl Pts',(-0.10650706570377,1.55293335137411,0.288538594757534));
#70626=CARTESIAN_POINT('Ctrl Pts',(-0.164376838372728,1.54787593355955,
0.292681605729789));
#70627=CARTESIAN_POINT('Ctrl Pts',(-0.221745214900975,1.53961336369509,
0.296824616702044));
#70628=CARTESIAN_POINT('Ctrl Pts',(-0.279136622138923,1.53134747679677,
0.300969290898688));
#70629=CARTESIAN_POINT('Ctrl Pts',(-0.336025721732457,1.51987397337167,
0.305113965095331));
#70630=CARTESIAN_POINT('Ctrl Pts',(-0.39203592095745,1.50528671245017,0.309258639291975));
#70631=CARTESIAN_POINT('Ctrl Pts',(-0.448152991738652,1.49067161796805,
0.313411221830091));
#70632=CARTESIAN_POINT('Ctrl Pts',(-0.503387314396123,1.4729310505554,0.317563804368206));
#70633=CARTESIAN_POINT('Ctrl Pts',(-0.557378054162897,1.4522086471088,0.321716386906322));
#70634=CARTESIAN_POINT('Ctrl Pts',(-0.607733336276543,1.43288158331724,
0.325589355976764));
#70635=CARTESIAN_POINT('Ctrl Pts',(-0.657006753231046,1.41096136958093,
0.329462325047206));
#70636=CARTESIAN_POINT('Ctrl Pts',(-0.704925006136371,1.38660051410766,
0.333335294117649));
#70637=CARTESIAN_POINT('Ctrl Pts',(-0.756335755000233,1.36046413085264,
0.337490542445074));
#70638=CARTESIAN_POINT('Ctrl Pts',(-0.806394588382471,1.33141199988986,
0.3416457907725));
#70639=CARTESIAN_POINT('Ctrl Pts',(-0.854751427758667,1.29960772802585,
0.345801039099926));
#70640=CARTESIAN_POINT('Ctrl Pts',(-0.903025134232295,1.26785813263509,
0.349949143911381));
#70641=CARTESIAN_POINT('Ctrl Pts',(-0.949602224940859,1.23336607111526,
0.354097248722836));
#70642=CARTESIAN_POINT('Ctrl Pts',(-0.994157179600198,1.19634098494091,
0.358245353534292));
#70643=CARTESIAN_POINT('Ctrl Pts',(-1.03866934915577,1.15935145310986,0.362389475015585));
#70644=CARTESIAN_POINT('Ctrl Pts',(-1.08116283352943,1.11983404664001,0.366533596496878));
#70645=CARTESIAN_POINT('Ctrl Pts',(-1.12134253402106,1.07804043124329,0.370677717978171));
#70646=CARTESIAN_POINT('Ctrl Pts',(-1.16149894037202,1.03627104565278,0.374819436909231));
#70647=CARTESIAN_POINT('Ctrl Pts',(-1.19934386353526,0.992228440648924,
0.378961155840291));
#70648=CARTESIAN_POINT('Ctrl Pts',(-1.23461828262234,0.946201852785475,
0.383102874771351));
#70649=CARTESIAN_POINT('Ctrl Pts',(-1.2698856734745,0.900184435467712,0.387243768487585));
#70650=CARTESIAN_POINT('Ctrl Pts',(-1.30258326197006,0.852184231805444,
0.391384662203819));
#70651=CARTESIAN_POINT('Ctrl Pts',(-1.3324930326322,0.802522627710056,0.395525555920053));
#70652=CARTESIAN_POINT('Ctrl Pts',(-1.3624305653706,0.752814928000761,0.399670293189902));
#70653=CARTESIAN_POINT('Ctrl Pts',(-1.38957484055183,0.701443191304415,
0.403815030459752));
#70654=CARTESIAN_POINT('Ctrl Pts',(-1.4137525726554,0.648755665339603,0.407959767729602));
#70655=CARTESIAN_POINT('Ctrl Pts',(-1.43794069300726,0.596045501556706,
0.412106285834794));
#70656=CARTESIAN_POINT('Ctrl Pts',(-1.45915953825246,0.542018904870885,
0.416252803939985));
#70657=CARTESIAN_POINT('Ctrl Pts',(-1.47728429048435,0.487043504307524,
0.420399322045177));
#70658=CARTESIAN_POINT('Ctrl Pts',(-1.49544438670223,0.431960899531784,
0.424553926025197));
#70659=CARTESIAN_POINT('Ctrl Pts',(-1.51049819643063,0.375926295918723,
0.428708530005218));
#70660=CARTESIAN_POINT('Ctrl Pts',(-1.52237129403959,0.319320987541107,
0.432863133985238));
#70661=CARTESIAN_POINT('Ctrl Pts',(-1.53340620622867,0.266711750427474,
0.436724442264667));
#70662=CARTESIAN_POINT('Ctrl Pts',(-1.54169413920795,0.213609984417661,
0.440585750544096));
#70663=CARTESIAN_POINT('Ctrl Pts',(-1.54721562759394,0.160324831916597,
0.444447058823525));
#70664=CARTESIAN_POINT('Ctrl Pts',(-1.55269554760363,0.107440835248059,
0.448279297347783));
#70665=CARTESIAN_POINT('Ctrl Pts',(-1.55546502074381,0.054268172421782,
0.452111535872041));
#70666=CARTESIAN_POINT('Ctrl Pts',(-1.5554996707636,0.00101205451123986,
0.455943774396298));
#70667=CARTESIAN_POINT('Origin',(0.,0.,-1.2940562256037));
#70668=CARTESIAN_POINT('',(-1.5555,3.44063942631422E-11,1.29450125422325));
#70669=CARTESIAN_POINT('',(-1.55549984592209,0.000692341893093657,1.15469914294653));
#70670=CARTESIAN_POINT('',(-1.5555,-1.46451138874614E-13,-1.2940562256037));
#70671=CARTESIAN_POINT('Ctrl Pts',(-1.5555,3.44063942631422E-11,1.29450125422325));
#70672=CARTESIAN_POINT('Ctrl Pts',(-1.55549999999854,0.066173945636013,
1.29012001595974));
#70673=CARTESIAN_POINT('Ctrl Pts',(-1.55127736795033,0.132275922252037,
1.28568825759211));
#70674=CARTESIAN_POINT('Ctrl Pts',(-1.54073252750121,0.214482744420159,
1.27997892833963));
#70675=CARTESIAN_POINT('Ctrl Pts',(-1.53833920511577,0.231023858141827,
1.27882022788333));
#70676=CARTESIAN_POINT('Ctrl Pts',(-1.53377098061585,0.259366030837854,
1.27681583757398));
#70677=CARTESIAN_POINT('Ctrl Pts',(-1.53172516204335,0.27118660135864,1.27597415535806));
#70678=CARTESIAN_POINT('Ctrl Pts',(-1.52757693494643,0.293608134394578,
1.27436606438647));
#70679=CARTESIAN_POINT('Ctrl Pts',(-1.5255003593377,0.304213201128698,1.27360051127662));
#70680=CARTESIAN_POINT('Ctrl Pts',(-1.52094071828573,0.32627756375004,1.27199694126935));
#70681=CARTESIAN_POINT('Ctrl Pts',(-1.51843825394136,0.337732101226949,
1.27115834939666));
#70682=CARTESIAN_POINT('Ctrl Pts',(-1.51265106479368,0.362856215182116,
1.26930502282033));
#70683=CARTESIAN_POINT('Ctrl Pts',(-1.50931005894072,0.376511618066541,
1.26828854077887));
#70684=CARTESIAN_POINT('Ctrl Pts',(-1.49723031814387,0.423137046820157,
1.264785311714));
#70685=CARTESIAN_POINT('Ctrl Pts',(-1.48759311794438,0.455861785575783,
1.26227017677252));
#70686=CARTESIAN_POINT('Ctrl Pts',(-1.44502743237814,0.584619452469703,
1.25214220891536));
#70687=CARTESIAN_POINT('Ctrl Pts',(-1.40381235831859,0.677635212499371,
1.24428169122734));
#70688=CARTESIAN_POINT('Ctrl Pts',(-1.32515992381098,0.816654115623695,
1.23189669967755));
#70689=CARTESIAN_POINT('Ctrl Pts',(-1.29365199034441,0.865701003739014,
1.22739257785155));
#70690=CARTESIAN_POINT('Ctrl Pts',(-1.24464284452598,0.933317923564547,
1.22108303769413));
#70691=CARTESIAN_POINT('Ctrl Pts',(-1.22932352548615,0.953405481557837,
1.21919527835678));
#70692=CARTESIAN_POINT('Ctrl Pts',(-1.20754392395819,0.980565752913682,
1.2166336338176));
#70693=CARTESIAN_POINT('Ctrl Pts',(-1.20149840610152,0.987964127211284,
1.21593488078652));
#70694=CARTESIAN_POINT('Ctrl Pts',(-1.19113600430478,1.00040959770847,1.21475845516477));
#70695=CARTESIAN_POINT('Ctrl Pts',(-1.18685433748461,1.00548552090548,1.21427837182051));
#70696=CARTESIAN_POINT('Ctrl Pts',(-1.17779409009436,1.01608793944454,1.21327522601179));
#70697=CARTESIAN_POINT('Ctrl Pts',(-1.17300890288194,1.02160840782781,1.21275264885535));
#70698=CARTESIAN_POINT('Ctrl Pts',(-1.15976245927782,1.03667448580016,1.21132507732875));
#70699=CARTESIAN_POINT('Ctrl Pts',(-1.15122217873001,1.0461503115702,1.2104256514839));
#70700=CARTESIAN_POINT('Ctrl Pts',(-1.09111436901719,1.11121502799647,1.20422986280805));
#70701=CARTESIAN_POINT('Ctrl Pts',(-1.03565183073949,1.16308120668778,1.19918548515016));
#70702=CARTESIAN_POINT('Ctrl Pts',(-0.929738615780285,1.24851683725739,
1.19020616051433));
#70703=CARTESIAN_POINT('Ctrl Pts',(-0.880701311753465,1.28357831839745,
1.18626448535201));
#70704=CARTESIAN_POINT('Ctrl Pts',(-0.790913638996762,1.3402031655219,1.17922265348124));
#70705=CARTESIAN_POINT('Ctrl Pts',(-0.7510093689496,1.36296491309884,1.17614915979125));
#70706=CARTESIAN_POINT('Ctrl Pts',(-0.681231689241316,1.39877116195034,
1.17080726956671));
#70707=CARTESIAN_POINT('Ctrl Pts',(-0.651848040812775,1.4127035278664,1.16856731727388));
#70708=CARTESIAN_POINT('Ctrl Pts',(-0.608372292156527,1.43167249540638,
1.16525347927361));
#70709=CARTESIAN_POINT('Ctrl Pts',(-0.594608721960165,1.4374433624772,1.16420447782444));
#70710=CARTESIAN_POINT('Ctrl Pts',(-0.570023591896887,1.44733804374563,
1.1623296831578));
#70711=CARTESIAN_POINT('Ctrl Pts',(-0.559234863988521,1.45154078890057,
1.16150662349314));
#70712=CARTESIAN_POINT('Ctrl Pts',(-0.536314244002038,1.46017604856547,
1.15975677932745));
#70713=CARTESIAN_POINT('Ctrl Pts',(-0.524172109283518,1.46457865691336,
1.15882906697885));
#70714=CARTESIAN_POINT('Ctrl Pts',(-0.491223805595871,1.47606315587526,
1.15630893603045));
#70715=CARTESIAN_POINT('Ctrl Pts',(-0.4703207841585,1.48285587147171,1.15470716132368));
#70716=CARTESIAN_POINT('Ctrl Pts',(-0.328839710171484,1.52553968913687,
1.14384019863525));
#70717=CARTESIAN_POINT('Ctrl Pts',(-0.20445570935984,1.54712389381478,1.13410707864492));
#70718=CARTESIAN_POINT('Ctrl Pts',(-0.0114200659839933,1.55692327211328,
1.11912579359675));
#70719=CARTESIAN_POINT('Ctrl Pts',(0.0561809398123301,1.55595179554514,
1.11391509028815));
#70720=CARTESIAN_POINT('Ctrl Pts',(0.139731607269046,1.5492966534169,1.10765966348977));
#70721=CARTESIAN_POINT('Ctrl Pts',(0.155932262152015,1.54775005329729,1.10645558004929));
#70722=CARTESIAN_POINT('Ctrl Pts',(0.180080614039595,1.54506168071519,1.1046768685259));
#70723=CARTESIAN_POINT('Ctrl Pts',(0.188047989997336,1.54411223227,1.10409263194985));
#70724=CARTESIAN_POINT('Ctrl Pts',(0.201813506300838,1.54236370795235,1.10308816908085));
#70725=CARTESIAN_POINT('Ctrl Pts',(0.207614846360526,1.54159351894441,1.1026663974491));
#70726=CARTESIAN_POINT('Ctrl Pts',(0.221348387392079,1.53969131176186,1.10167156914738));
#70727=CARTESIAN_POINT('Ctrl Pts',(0.229276365890333,1.53853072757603,1.10110010912347));
#70728=CARTESIAN_POINT('Ctrl Pts',(0.253217737167928,1.53483675322822,1.09938195474112));
#70729=CARTESIAN_POINT('Ctrl Pts',(0.269201422364817,1.53211413736664,1.09824515059708));
#70730=CARTESIAN_POINT('Ctrl Pts',(0.359073598840509,1.51535559468211,1.09189612958587));
#70731=CARTESIAN_POINT('Ctrl Pts',(0.431919275167733,1.49622358005086,1.08691145468797));
#70732=CARTESIAN_POINT('Ctrl Pts',(0.580310450272275,1.44550253334568,1.07657555997579));
#70733=CARTESIAN_POINT('Ctrl Pts',(0.655318700204039,1.41307975129853,1.07124207902358));
#70734=CARTESIAN_POINT('Ctrl Pts',(0.755355148903462,1.36015312366644,1.06363217683254));
#70735=CARTESIAN_POINT('Ctrl Pts',(0.782816396694977,1.34453568583332,1.06148837013198));
#70736=CARTESIAN_POINT('Ctrl Pts',(0.830919075018346,1.31520592316116,1.05761592088477));
#70737=CARTESIAN_POINT('Ctrl Pts',(0.85174445395616,1.30181580789285,1.0558983234026));
#70738=CARTESIAN_POINT('Ctrl Pts',(0.883405250437868,1.28037386614156,1.05321697993251));
#70739=CARTESIAN_POINT('Ctrl Pts',(0.894470886126156,1.27266801917128,1.05226617375764));
#70740=CARTESIAN_POINT('Ctrl Pts',(0.914794916227206,1.25811884367658,1.05049343451662));
#70741=CARTESIAN_POINT('Ctrl Pts',(0.924080284731778,1.25131465980768,1.04967304896571));
#70742=CARTESIAN_POINT('Ctrl Pts',(0.944561091209134,1.23595433644441,1.04783949679965));
#70743=CARTESIAN_POINT('Ctrl Pts',(0.955717386008275,1.22734796638103,1.04682440442133));
#70744=CARTESIAN_POINT('Ctrl Pts',(0.983839068008911,1.20503796834503,1.04422280258073));
#70745=CARTESIAN_POINT('Ctrl Pts',(1.00063548309312,1.19112734737754,1.04262816237686));
#70746=CARTESIAN_POINT('Ctrl Pts',(1.09190984219276,1.11224160219564,1.0337293845014));
#70747=CARTESIAN_POINT('Ctrl Pts',(1.16034425149336,1.04064566170079,1.02615433406886));
#70748=CARTESIAN_POINT('Ctrl Pts',(1.26284734305497,0.910633504833359,1.0133218770693));
#70749=CARTESIAN_POINT('Ctrl Pts',(1.30076274982857,0.855601413603371,1.00812836319334));
#70750=CARTESIAN_POINT('Ctrl Pts',(1.34683281767853,0.778556907172249,1.00128978248354));
#70751=CARTESIAN_POINT('Ctrl Pts',(1.35820064344568,0.758551663580726,0.999551149736661));
#70752=CARTESIAN_POINT('Ctrl Pts',(1.37705959911517,0.723579192941432,0.996583524393833));
#70753=CARTESIAN_POINT('Ctrl Pts',(1.38476058822685,0.70872996351125,0.995345190632082));
#70754=CARTESIAN_POINT('Ctrl Pts',(1.39583807666929,0.686499881086753,0.99352635858116));
#70755=CARTESIAN_POINT('Ctrl Pts',(1.39939847609441,0.67921273248502,0.992935635391156));
#70756=CARTESIAN_POINT('Ctrl Pts',(1.40543105609367,0.666616893088735,0.991924422068322));
#70757=CARTESIAN_POINT('Ctrl Pts',(1.4079304361811,0.661321726472419,0.991502314175194));
#70758=CARTESIAN_POINT('Ctrl Pts',(1.41374361763505,0.648823620193149,0.990513038061281));
#70759=CARTESIAN_POINT('Ctrl Pts',(1.41703232810791,0.641609300853237,0.989947393961184));
#70760=CARTESIAN_POINT('Ctrl Pts',(1.42650514259419,0.62040099032651,0.988299382972986));
#70761=CARTESIAN_POINT('Ctrl Pts',(1.43253833737854,0.606340060173557,0.987225563230212));
#70762=CARTESIAN_POINT('Ctrl Pts',(1.47381100755128,0.506093644539667,0.979686236681375));
#70763=CARTESIAN_POINT('Ctrl Pts',(1.50146162238255,0.416974206890176,0.973581055212101));
#70764=CARTESIAN_POINT('Ctrl Pts',(1.53563626338026,0.257483984088193,0.962848208943956));
#70765=CARTESIAN_POINT('Ctrl Pts',(1.54566279089013,0.18815516542045,0.958244160154274));
#70766=CARTESIAN_POINT('Ctrl Pts',(1.55424527879838,0.0757185524093037,
0.950637991356019));
#70767=CARTESIAN_POINT('Ctrl Pts',(1.55573984246288,0.0329346859891965,
0.947712587502483));
#70768=CARTESIAN_POINT('Ctrl Pts',(1.55536441024355,-0.0263309600484623,
0.943585749178343));
#70769=CARTESIAN_POINT('Ctrl Pts',(1.55499821543606,-0.0428051589004132,
0.942430724169581));
#70770=CARTESIAN_POINT('Ctrl Pts',(1.55392047158784,-0.0710693084944344,
0.940433954213125));
#70771=CARTESIAN_POINT('Ctrl Pts',(1.55333621677948,-0.0828629125835807,
0.939596247208741));
#70772=CARTESIAN_POINT('Ctrl Pts',(1.55187017296961,-0.106911970931832,
0.937878212999806));
#70773=CARTESIAN_POINT('Ctrl Pts',(1.5509773302719,-0.119165885253095,0.936997597002927));
#70774=CARTESIAN_POINT('Ctrl Pts',(1.54833828902965,-0.150293107417539,
0.934746763264206));
#70775=CARTESIAN_POINT('Ctrl Pts',(1.54639216534164,-0.169146939979477,
0.933370381848849));
#70776=CARTESIAN_POINT('Ctrl Pts',(1.53657373629975,-0.249805999471025,
0.927423341283527));
#70777=CARTESIAN_POINT('Ctrl Pts',(1.52533753099491,-0.311135699364405,
0.922749905055785));
#70778=CARTESIAN_POINT('Ctrl Pts',(1.48568590045217,-0.472300638863577,
0.910077219739693));
#70779=CARTESIAN_POINT('Ctrl Pts',(1.45091322431365,-0.570244938439349,
0.901947840269197));
#70780=CARTESIAN_POINT('Ctrl Pts',(1.39456428372374,-0.689618261921028,
0.891832458899489));
#70781=CARTESIAN_POINT('Ctrl Pts',(1.38177220260347,-0.714904653519119,
0.889678711772563));
#70782=CARTESIAN_POINT('Ctrl Pts',(1.35903324482003,-0.756959808063756,
0.886093058320462));
#70783=CARTESIAN_POINT('Ctrl Pts',(1.34944922420061,-0.773916270808348,
0.884646331242522));
#70784=CARTESIAN_POINT('Ctrl Pts',(1.33517432258963,-0.798100140902384,
0.882586126061654));
#70785=CARTESIAN_POINT('Ctrl Pts',(1.33073836765728,-0.805474836808508,
0.881958317218233));
#70786=CARTESIAN_POINT('Ctrl Pts',(1.32283631764262,-0.81836836912185,0.880861964513523));
#70787=CARTESIAN_POINT('Ctrl Pts',(1.31939643941452,-0.823902756535837,
0.880391815074281));
#70788=CARTESIAN_POINT('Ctrl Pts',(1.31174903461766,-0.83603585902308,0.879362142896668));
#70789=CARTESIAN_POINT('Ctrl Pts',(1.30752637984319,-0.842624626073871,
0.878803611552494));
#70790=CARTESIAN_POINT('Ctrl Pts',(1.2951692328433,-0.861589362402017,0.877196902272928));
#70791=CARTESIAN_POINT('Ctrl Pts',(1.28690723169062,-0.873881794136387,
0.876156640225968));
#70792=CARTESIAN_POINT('Ctrl Pts',(1.22141787581551,-0.968375046143511,
0.868153293452749));
#70793=CARTESIAN_POINT('Ctrl Pts',(1.15653919864745,-1.04500466797491,0.861612810327628));
#70794=CARTESIAN_POINT('Ctrl Pts',(1.03754706242522,-1.16078013036358,0.850685718088348));
#70795=CARTESIAN_POINT('Ctrl Pts',(0.987497119244587,-1.20364570616782,
0.846342908330371));
#70796=CARTESIAN_POINT('Ctrl Pts',(0.912422323536318,-1.26010145516987,
0.839998408926332));
#70797=CARTESIAN_POINT('Ctrl Pts',(0.889506811781509,-1.27638068694012,
0.83808300540988));
#70798=CARTESIAN_POINT('Ctrl Pts',(0.847339647100369,-1.3046491408938,0.834583713781654));
#70799=CARTESIAN_POINT('Ctrl Pts',(0.828242705493292,-1.3168552646975,0.833007891812109));
#70800=CARTESIAN_POINT('Ctrl Pts',(0.797733448174011,-1.33542955594234,
0.830499946943618));
#70801=CARTESIAN_POINT('Ctrl Pts',(0.786495405086956,-1.34207887709794,
0.829578154626251));
#70802=CARTESIAN_POINT('Ctrl Pts',(0.765158916519037,-1.35434322035417,
0.827831012091375));
#70803=CARTESIAN_POINT('Ctrl Pts',(0.755078973249932,-1.35998877088987,
0.827006838760781));
#70804=CARTESIAN_POINT('Ctrl Pts',(0.732048652454525,-1.37255257678912,
0.825126024806289));
#70805=CARTESIAN_POINT('Ctrl Pts',(0.719061506810858,-1.37940071318173,
0.824066977559879));
#70806=CARTESIAN_POINT('Ctrl Pts',(0.678256088485306,-1.40018460535361,
0.820743195622856));
#70807=CARTESIAN_POINT('Ctrl Pts',(0.650116956007206,-1.41346946848273,
0.818456294662544));
#70808=CARTESIAN_POINT('Ctrl Pts',(0.505109638405407,-1.47668324460947,
0.80668956913138));
#70809=CARTESIAN_POINT('Ctrl Pts',(0.382849090961857,-1.51299213477604,
0.79677199893315));
#70810=CARTESIAN_POINT('Ctrl Pts',(0.200276156925776,-1.54364644407647,
0.782474536140982));
#70811=CARTESIAN_POINT('Ctrl Pts',(0.142485811906422,-1.5500497410089,0.778030836873473));
#70812=CARTESIAN_POINT('Ctrl Pts',(0.0722771104930077,-1.55386785097514,
0.772823130975401));
#70813=CARTESIAN_POINT('Ctrl Pts',(0.0600794839110052,-1.55438726172793,
0.771925382508288));
#70814=CARTESIAN_POINT('Ctrl Pts',(0.0406912623802615,-1.55498429184524,
0.770510817673444));
#70815=CARTESIAN_POINT('Ctrl Pts',(0.0335043722516422,-1.5551557444108,
0.769989170164399));
#70816=CARTESIAN_POINT('Ctrl Pts',(0.019694468714525,-1.5553894174391,0.768992330454731));
#70817=CARTESIAN_POINT('Ctrl Pts',(0.0130718858168326,-1.55545917331499,
0.768516766739881));
#70818=CARTESIAN_POINT('Ctrl Pts',(-0.00336274671031001,-1.55552731025794,
0.767342331540919));
#70819=CARTESIAN_POINT('Ctrl Pts',(-0.0131749458998763,-1.55547515412416,
0.766646194608348));
#70820=CARTESIAN_POINT('Ctrl Pts',(-0.0485207013566759,-1.55495277678717,
0.764154613184552));
#70821=CARTESIAN_POINT('Ctrl Pts',(-0.0740437748815334,-1.55394662214301,
0.762385633961577));
#70822=CARTESIAN_POINT('Ctrl Pts',(-0.204869799206001,-1.54555822445316,
0.753419844711295));
#70823=CARTESIAN_POINT('Ctrl Pts',(-0.309256457753484,-1.52809909361066,
0.746589414115095));
#70824=CARTESIAN_POINT('Ctrl Pts',(-0.472120577036149,-1.48347172064588,
0.735428391334662));
#70825=CARTESIAN_POINT('Ctrl Pts',(-0.532079558488635,-1.46303669022891,
0.731206452936639));
#70826=CARTESIAN_POINT('Ctrl Pts',(-0.616674170741491,-1.42831585439364,
0.724947530180732));
#70827=CARTESIAN_POINT('Ctrl Pts',(-0.642428242777043,-1.41691883934955,
0.723000153963644));
#70828=CARTESIAN_POINT('Ctrl Pts',(-0.680635374747506,-1.39875512908199,
0.720038968348202));
#70829=CARTESIAN_POINT('Ctrl Pts',(-0.693329369726769,-1.39250665566949,
0.719042881519532));
#70830=CARTESIAN_POINT('Ctrl Pts',(-0.716199741093375,-1.38085873654213,
0.717224875711715));
#70831=CARTESIAN_POINT('Ctrl Pts',(-0.72640484178124,-1.37551768879564,
0.716405052021045));
#70832=CARTESIAN_POINT('Ctrl Pts',(-0.748392457814292,-1.3636970971313,
0.714619404106716));
#70833=CARTESIAN_POINT('Ctrl Pts',(-0.760152066574892,-1.35717716537746,
0.713652191039164));
#70834=CARTESIAN_POINT('Ctrl Pts',(-0.792545644141668,-1.33866396523111,
0.710952936475932));
#70835=CARTESIAN_POINT('Ctrl Pts',(-0.812989548258128,-1.32634749868085,
0.709209413087034));
#70836=CARTESIAN_POINT('Ctrl Pts',(-0.918760733669823,-1.2592611867752,
0.699971078486175));
#70837=CARTESIAN_POINT('Ctrl Pts',(-0.998851292290241,-1.19672442878681,
0.692192415550732));
#70838=CARTESIAN_POINT('Ctrl Pts',(-1.11932734767826,-1.08208354350407,
0.679298953207176));
#70839=CARTESIAN_POINT('Ctrl Pts',(-1.16352957688896,-1.03440715295421,
0.674249426583443));
#70840=CARTESIAN_POINT('Ctrl Pts',(-1.22574374795021,-0.958252039711842,
0.666761307294949));
#70841=CARTESIAN_POINT('Ctrl Pts',(-1.24602837120463,-0.931723347663148,
0.664249040344013));
#70842=CARTESIAN_POINT('Ctrl Pts',(-1.27153936887439,-0.896034436492706,
0.661013006060535));
#70843=CARTESIAN_POINT('Ctrl Pts',(-1.27754758047765,-0.887447054050633,
0.660244896544388));
#70844=CARTESIAN_POINT('Ctrl Pts',(-1.28731987800289,-0.873174809320621,
0.658986417738811));
#70845=CARTESIAN_POINT('Ctrl Pts',(-1.2911341069374,-0.867524892915393,
0.658492839991736));
#70846=CARTESIAN_POINT('Ctrl Pts',(-1.29878653211309,-0.856027286412465,
0.657498001873287));
#70847=CARTESIAN_POINT('Ctrl Pts',(-1.302622656876,-0.850178446013116,0.656996876485008));
#70848=CARTESIAN_POINT('Ctrl Pts',(-1.31257278138028,-0.834782287554142,
0.65569009229947));
#70849=CARTESIAN_POINT('Ctrl Pts',(-1.31862222576262,-0.825193443812122,
0.654888541614257));
#70850=CARTESIAN_POINT('Ctrl Pts',(-1.34514093410318,-0.782122792873095,
0.651338690354689));
#70851=CARTESIAN_POINT('Ctrl Pts',(-1.36444548890473,-0.747936696834765,
0.648655699755602));
#70852=CARTESIAN_POINT('Ctrl Pts',(-1.42450778606151,-0.631490507014228,
0.639831350612569));
#70853=CARTESIAN_POINT('Ctrl Pts',(-1.45927906244556,-0.546360014322117,
0.633875920029916));
#70854=CARTESIAN_POINT('Ctrl Pts',(-1.5084705040553,-0.386947935828809,
0.622841825458153));
#70855=CARTESIAN_POINT('Ctrl Pts',(-1.52537744295723,-0.31374110894365,
0.617817409433293));
#70856=CARTESIAN_POINT('Ctrl Pts',(-1.53998347561593,-0.220051829075397,
0.611253665695753));
#70857=CARTESIAN_POINT('Ctrl Pts',(-1.54265837579021,-0.200441977704697,
0.609873001858645));
#70858=CARTESIAN_POINT('Ctrl Pts',(-1.54640551987449,-0.168419898296888,
0.607604506038478));
#70859=CARTESIAN_POINT('Ctrl Pts',(-1.54770411844452,-0.156036019908814,
0.606723843332135));
#70860=CARTESIAN_POINT('Ctrl Pts',(-1.54993484458716,-0.131982051576268,
0.605006075357329));
#70861=CARTESIAN_POINT('Ctrl Pts',(-1.55088417448401,-0.120314371102912,
0.604169573089886));
#70862=CARTESIAN_POINT('Ctrl Pts',(-1.5528133634839,-0.0927591598438819,
0.602185750767877));
#70863=CARTESIAN_POINT('Ctrl Pts',(-1.55368120297326,-0.0768653887194082,
0.601034997748598));
#70864=CARTESIAN_POINT('Ctrl Pts',(-1.55510168454109,-0.0406481588717827,
0.598397021803662));
#70865=CARTESIAN_POINT('Ctrl Pts',(-1.5555000000974,-0.0203237295583516,
0.596905348382645));
#70866=CARTESIAN_POINT('Ctrl Pts',(-1.5555,7.45448211670055E-9,0.595401982137319));
#70867=CARTESIAN_POINT('Ctrl Pts',(-1.55549962214825,0.00108420323222797,
0.45701132945449));
#70868=CARTESIAN_POINT('Ctrl Pts',(-1.55559222809785,-0.131776975675532,
0.465990612534344));
#70869=CARTESIAN_POINT('Ctrl Pts',(-1.53866326941148,-0.264113784066724,
0.474473953896888));
#70870=CARTESIAN_POINT('Ctrl Pts',(-1.49386726717658,-0.435803972088965,
0.486419820767815));
#70871=CARTESIAN_POINT('Ctrl Pts',(-1.48077610088256,-0.478399474189407,
0.489459784139951));
#70872=CARTESIAN_POINT('Ctrl Pts',(-1.46022645306863,-0.536287411661747,
0.493733536133207));
#70873=CARTESIAN_POINT('Ctrl Pts',(-1.45431789749139,-0.552109496244956,
0.49491660831121));
#70874=CARTESIAN_POINT('Ctrl Pts',(-1.44375505425784,-0.579048136409908,
0.496958435657103));
#70875=CARTESIAN_POINT('Ctrl Pts',(-1.43922696275649,-0.59021278852078,
0.497812891309869));
#70876=CARTESIAN_POINT('Ctrl Pts',(-1.42973896931268,-0.612848175116802,
0.499562673758938));
#70877=CARTESIAN_POINT('Ctrl Pts',(-1.42476961910855,-0.624313960766495,
0.500458271815235));
#70878=CARTESIAN_POINT('Ctrl Pts',(-1.41181107643544,-0.653252501987194,
0.502742967494973));
#70879=CARTESIAN_POINT('Ctrl Pts',(-1.40363552926885,-0.670638938646375,
0.504138396380045));
#70880=CARTESIAN_POINT('Ctrl Pts',(-1.36725250891238,-0.744431240597183,
0.510162070654917));
#70881=CARTESIAN_POINT('Ctrl Pts',(-1.33595455858357,-0.799237610854561,
0.514896133475867));
#70882=CARTESIAN_POINT('Ctrl Pts',(-1.24499532827392,-0.938178953378845,
0.527587555202891));
#70883=CARTESIAN_POINT('Ctrl Pts',(-1.18015101899143,-1.0185454145577,0.535669321779819));
#70884=CARTESIAN_POINT('Ctrl Pts',(-1.08792313130614,-1.11211900459493,
0.545742557369242));
#70885=CARTESIAN_POINT('Ctrl Pts',(-1.06745393217973,-1.13178077363924,
0.547900739243709));
#70886=CARTESIAN_POINT('Ctrl Pts',(-1.03198308789238,-1.16403344440843,
0.551497782500001));
#70887=CARTESIAN_POINT('Ctrl Pts',(-1.0172612049225,-1.17692085014791,0.552951506823508));
#70888=CARTESIAN_POINT('Ctrl Pts',(-0.995639225204317,-1.19513958630086,
0.555026143112321));
#70889=CARTESIAN_POINT('Ctrl Pts',(-0.988931983560631,-1.20069548140919,
0.555661548166732));
#70890=CARTESIAN_POINT('Ctrl Pts',(-0.977065314993787,-1.21035825081999,
0.556770966315458));
#70891=CARTESIAN_POINT('Ctrl Pts',(-0.971926028505627,-1.21448899752712,
0.557246621559516));
#70892=CARTESIAN_POINT('Ctrl Pts',(-0.960440653869167,-1.22360086432171,
0.558298987468403));
#70893=CARTESIAN_POINT('Ctrl Pts',(-0.954081912521708,-1.22856543849585,
0.558874554832622));
#70894=CARTESIAN_POINT('Ctrl Pts',(-0.935487546849195,-1.2428515138766,
0.560538195715148));
#70895=CARTESIAN_POINT('Ctrl Pts',(-0.923151516896774,-1.25204159646333,
0.561617730230413));
#70896=CARTESIAN_POINT('Ctrl Pts',(-0.834443992119293,-1.31610279440216,
0.569226789975005));
#70897=CARTESIAN_POINT('Ctrl Pts',(-0.753360876617966,-1.36413916058978,
0.575390220523253));
#70898=CARTESIAN_POINT('Ctrl Pts',(-0.60614640690851,-1.43419795321606,
0.58612089256293));
#70899=CARTESIAN_POINT('Ctrl Pts',(-0.541969828151479,-1.45965922560717,
0.590661972331486));
#70900=CARTESIAN_POINT('Ctrl Pts',(-0.435741462610644,-1.49382946295933,
0.598190459943658));
#70901=CARTESIAN_POINT('Ctrl Pts',(-0.394648655385648,-1.50520729431177,
0.601104513386016));
#70902=CARTESIAN_POINT('Ctrl Pts',(-0.336846680359906,-1.51868185493772,
0.605237084806839));
#70903=CARTESIAN_POINT('Ctrl Pts',(-0.320490387296837,-1.52221750620717,
0.606410071391811));
#70904=CARTESIAN_POINT('Ctrl Pts',(-0.292200495609419,-1.52785662599148,
0.608446722203742));
#70905=CARTESIAN_POINT('Ctrl Pts',(-0.28029326737502,-1.53008583695195,
0.609306323867898));
#70906=CARTESIAN_POINT('Ctrl Pts',(-0.255825916384155,-1.53437130855106,
0.611078133434445));
#70907=CARTESIAN_POINT('Ctrl Pts',(-0.243264198761912,-1.53641294053229,
0.611990733851619));
#70908=CARTESIAN_POINT('Ctrl Pts',(-0.210980316102215,-1.54125414113151,
0.614344370188822));
#70909=CARTESIAN_POINT('Ctrl Pts',(-0.191227416351517,-1.5438293391593,
0.615792314669233));
#70910=CARTESIAN_POINT('Ctrl Pts',(-0.100912577616179,-1.55384392442836,
0.622451611889749));
#70911=CARTESIAN_POINT('Ctrl Pts',(-0.0299519142444876,-1.55682834827152,
0.627797506409655));
#70912=CARTESIAN_POINT('Ctrl Pts',(0.134700830305024,-1.55249160655785,
0.640428994785667));
#70913=CARTESIAN_POINT('Ctrl Pts',(0.228026725137361,-1.54155038163138,
0.647765603871157));
#70914=CARTESIAN_POINT('Ctrl Pts',(0.346494571530747,-1.51666277175438,
0.657027971589266));
#70915=CARTESIAN_POINT('Ctrl Pts',(0.373041333769766,-1.51035253843597,
0.659098910664312));
#70916=CARTESIAN_POINT('Ctrl Pts',(0.417818956285551,-1.49845600077114,
0.662570475163492));
#70917=CARTESIAN_POINT('Ctrl Pts',(0.436137775119659,-1.49322703992496,
0.6639844547229));
#70918=CARTESIAN_POINT('Ctrl Pts',(0.46266215851283,-1.48512605104798,0.66601827279117));
#70919=CARTESIAN_POINT('Ctrl Pts',(0.47094623509352,-1.4825199201197,0.666651529664496));
#70920=CARTESIAN_POINT('Ctrl Pts',(0.484971186319934,-1.47797831233667,
0.66771982510586));
#70921=CARTESIAN_POINT('Ctrl Pts',(0.490723175654049,-1.47607849148383,
0.668156845773352));
#70922=CARTESIAN_POINT('Ctrl Pts',(0.503976228395926,-1.47161511326572,
0.669161126042264));
#70923=CARTESIAN_POINT('Ctrl Pts',(0.511468990133657,-1.46902776006226,
0.669726998119038));
#70924=CARTESIAN_POINT('Ctrl Pts',(0.532797491404099,-1.46147976549026,
0.671333210290149));
#70925=CARTESIAN_POINT('Ctrl Pts',(0.546583585810319,-1.45637999727997,
0.672365899101507));
#70926=CARTESIAN_POINT('Ctrl Pts',(0.655603763529275,-1.41428490882571,
0.680504131455665));
#70927=CARTESIAN_POINT('Ctrl Pts',(0.74706844026402,-1.368178689696,0.687170240203545));
#70928=CARTESIAN_POINT('Ctrl Pts',(0.85612686663686,-1.29898192507432,0.695676226158675));
#70929=CARTESIAN_POINT('Ctrl Pts',(0.878514028559614,-1.28394716241009,
0.6974540226012));
#70930=CARTESIAN_POINT('Ctrl Pts',(0.939197004647554,-1.24086327567092,
0.702386879951735));
#70931=CARTESIAN_POINT('Ctrl Pts',(0.97661497617679,-1.21163334327879,0.705559521268203));
#70932=CARTESIAN_POINT('Ctrl Pts',(1.03799619983705,-1.15899106544816,0.71106261919988));
#70933=CARTESIAN_POINT('Ctrl Pts',(1.06264704234687,-1.13643186922587,0.713362660632223));
#70934=CARTESIAN_POINT('Ctrl Pts',(1.09750695625718,-1.10240334469373,0.716764811806982));
#70935=CARTESIAN_POINT('Ctrl Pts',(1.10830393765384,-1.0915479859966,0.717840711788879));
#70936=CARTESIAN_POINT('Ctrl Pts',(1.12719648717863,-1.07198397756297,0.719764566217214));
#70937=CARTESIAN_POINT('Ctrl Pts',(1.13535585941975,-1.06333843485334,0.720609656162315));
#70938=CARTESIAN_POINT('Ctrl Pts',(1.15242066131286,-1.04483649601181,0.722408138872987));
#70939=CARTESIAN_POINT('Ctrl Pts',(1.16130048480583,-1.03495789659564,0.723362523171695));
#70940=CARTESIAN_POINT('Ctrl Pts',(1.18500763224571,-1.00789497227222,0.725962223662884));
#70941=CARTESIAN_POINT('Ctrl Pts',(1.19958659492175,-0.990498492767489,
0.727617530659071));
#70942=CARTESIAN_POINT('Ctrl Pts',(1.30039971917826,-0.864710968863832,
0.739482643387864));
#70943=CARTESIAN_POINT('Ctrl Pts',(1.37218219636709,-0.745563409998109,
0.750268706956153));
#70944=CARTESIAN_POINT('Ctrl Pts',(1.45116588071695,-0.563311225532864,
0.76561946739305));
#70945=CARTESIAN_POINT('Ctrl Pts',(1.47187425060517,-0.506744290007288,
0.770228891819041));
#70946=CARTESIAN_POINT('Ctrl Pts',(1.4928596724745,-0.437156966989877,0.775614632176288));
#70947=CARTESIAN_POINT('Ctrl Pts',(1.49632149209804,-0.425156717247051,
0.776533355658679));
#70948=CARTESIAN_POINT('Ctrl Pts',(1.501594232799,-0.406016298289001,0.777981440068602));
#70949=CARTESIAN_POINT('Ctrl Pts',(1.5034995369481,-0.398903024395469,0.778515833978629));
#70950=CARTESIAN_POINT('Ctrl Pts',(1.5070673596748,-0.385194085373924,0.779538154195339));
#70951=CARTESIAN_POINT('Ctrl Pts',(1.50873723574029,-0.378600667892621,
0.780026455637771));
#70952=CARTESIAN_POINT('Ctrl Pts',(1.51278907379748,-0.362149568528122,
0.781236821726823));
#70953=CARTESIAN_POINT('Ctrl Pts',(1.51511804048059,-0.35227890908491,0.781955939948439));
#70954=CARTESIAN_POINT('Ctrl Pts',(1.52329259849065,-0.31605174178774,0.784571698156795));
#70955=CARTESIAN_POINT('Ctrl Pts',(1.528548701326,-0.289565417157093,0.786438697744324));
#70956=CARTESIAN_POINT('Ctrl Pts',(1.54865968620811,-0.172311294572819,
0.794558890861106));
#70957=CARTESIAN_POINT('Ctrl Pts',(1.55613860216703,-0.0804602061068882,
0.80054836749639));
#70958=CARTESIAN_POINT('Ctrl Pts',(1.55491905320242,0.0841967079041952,
0.811401617338453));
#70959=CARTESIAN_POINT('Ctrl Pts',(1.54928814381692,0.156738856062114,0.816223034879309));
#70960=CARTESIAN_POINT('Ctrl Pts',(1.53427759584364,0.257760749117066,0.823202677273314));
#70961=CARTESIAN_POINT('Ctrl Pts',(1.52912035680635,0.286773583659468,0.825237737280817));
#70962=CARTESIAN_POINT('Ctrl Pts',(1.52018021177721,0.329917474840088,0.828319739719143));
#70963=CARTESIAN_POINT('Ctrl Pts',(1.51701668816986,0.344171118133979,0.829347130060704));
#70964=CARTESIAN_POINT('Ctrl Pts',(1.5109320704643,0.369870262939396,0.8312172583201));
#70965=CARTESIAN_POINT('Ctrl Pts',(1.50808032319764,0.381331165352149,0.832057711287271));
#70966=CARTESIAN_POINT('Ctrl Pts',(1.50163583492686,0.406027248325023,0.83388326014716));
#70967=CARTESIAN_POINT('Ctrl Pts',(1.49799803953429,0.41924951795191,0.834869753205673));
#70968=CARTESIAN_POINT('Ctrl Pts',(1.48746349982297,0.455650480893109,0.83761167867197));
#70969=CARTESIAN_POINT('Ctrl Pts',(1.48020059711373,0.478718178854514,0.839378813515945));
#70970=CARTESIAN_POINT('Ctrl Pts',(1.44561745438315,0.580232770910194,0.84729182666431));
#70971=CARTESIAN_POINT('Ctrl Pts',(1.41258085929661,0.656575422198195,0.853618566900436));
#70972=CARTESIAN_POINT('Ctrl Pts',(1.33697110850095,0.798865910015656,0.866070037158325));
#70973=CARTESIAN_POINT('Ctrl Pts',(1.29518614811871,0.864969230372958,0.872165185939581));
#70974=CARTESIAN_POINT('Ctrl Pts',(1.22656771051593,0.957328770611055,0.88095217671356));
#70975=CARTESIAN_POINT('Ctrl Pts',(1.20346945985135,0.986209151402802,0.883741917856108));
#70976=CARTESIAN_POINT('Ctrl Pts',(1.17219511628505,1.02257501996507,0.887283767590779));
#70977=CARTESIAN_POINT('Ctrl Pts',(1.16493988953768,1.0308327382976,0.888090045246842));
#70978=CARTESIAN_POINT('Ctrl Pts',(1.15289676090454,1.04425036922231,0.889402500673036));
#70979=CARTESIAN_POINT('Ctrl Pts',(1.14816041907011,1.04945577962064,0.889912268140033));
#70980=CARTESIAN_POINT('Ctrl Pts',(1.1385453918034,1.05988002714475,0.890934009704774));
#70981=CARTESIAN_POINT('Ctrl Pts',(1.13366577932167,1.06509773610221,0.891445899212164));
#70982=CARTESIAN_POINT('Ctrl Pts',(1.1208639580628,1.07859890871543,0.892772280668619));
#70983=CARTESIAN_POINT('Ctrl Pts',(1.11288565992149,1.08682894093078,0.893582638543893));
#70984=CARTESIAN_POINT('Ctrl Pts',(1.0776165971945,1.12241515870123,0.897098781588745));
#70985=CARTESIAN_POINT('Ctrl Pts',(1.04940052499586,1.14883960078862,0.899741852092821));
#70986=CARTESIAN_POINT('Ctrl Pts',(0.906744814047346,1.27279010744027,0.912477734325908));
#70987=CARTESIAN_POINT('Ctrl Pts',(0.779570311632964,1.35442067617543,0.92203587703761));
#70988=CARTESIAN_POINT('Ctrl Pts',(0.615756303871838,1.42873955618678,0.934329076352657));
#70989=CARTESIAN_POINT('Ctrl Pts',(0.588519711417521,1.44017252519928,0.936369049803746));
#70990=CARTESIAN_POINT('Ctrl Pts',(0.547333698359148,1.45609752368984,0.939457888815914));
#70991=CARTESIAN_POINT('Ctrl Pts',(0.533618472968219,1.46117948087086,0.94048712334576));
#70992=CARTESIAN_POINT('Ctrl Pts',(0.508685894298989,1.47002000567117,0.942360393314172));
#70993=CARTESIAN_POINT('Ctrl Pts',(0.497493325218803,1.47384549168836,0.943202136259653));
#70994=CARTESIAN_POINT('Ctrl Pts',(0.473215110276006,1.4818354380438,0.945030301710871));
#70995=CARTESIAN_POINT('Ctrl Pts',(0.460115859099777,1.48595497233822,0.946018121336703));
#70996=CARTESIAN_POINT('Ctrl Pts',(0.423774595164706,1.49685720612247,0.948763473124544));
#70997=CARTESIAN_POINT('Ctrl Pts',(0.400427045964196,1.50327125365992,0.950532715142734));
#70998=CARTESIAN_POINT('Ctrl Pts',(0.287446758967202,1.53149058065117,0.959125167818554));
#70999=CARTESIAN_POINT('Ctrl Pts',(0.19615670761787,1.54583517391963,0.966176765304142));
#71000=CARTESIAN_POINT('Ctrl Pts',(0.0334843880084227,1.55675141941361,
0.97879900278409));
#71001=CARTESIAN_POINT('Ctrl Pts',(-0.0374232788441268,1.55666191856376,
0.984314846594833));
#71002=CARTESIAN_POINT('Ctrl Pts',(-0.131880126116507,1.55008292680199,
0.991534843764174));
#71003=CARTESIAN_POINT('Ctrl Pts',(-0.155640418922857,1.54787778446996,
0.993339640488362));
#71004=CARTESIAN_POINT('Ctrl Pts',(-0.196489056925793,1.54313651001296,
0.996413303548926));
#71005=CARTESIAN_POINT('Ctrl Pts',(-0.213602905328831,1.54086083150488,
0.997692153280786));
#71006=CARTESIAN_POINT('Ctrl Pts',(-0.238922876000515,1.53706396930472,
0.999567673935903));
#71007=CARTESIAN_POINT('Ctrl Pts',(-0.247159697958938,1.53576100960163,
1.00017518830595));
#71008=CARTESIAN_POINT('Ctrl Pts',(-0.261319108792152,1.53340430143648,
1.00121457917991));
#71009=CARTESIAN_POINT('Ctrl Pts',(-0.267246509880269,1.53238237231014,
1.00164816269389));
#71010=CARTESIAN_POINT('Ctrl Pts',(-0.28120592498404,1.52989219849192,1.00266569714525));
#71011=CARTESIAN_POINT('Ctrl Pts',(-0.289232499173429,1.52839506693504,
1.00324802753633));
#71012=CARTESIAN_POINT('Ctrl Pts',(-0.313310747236021,1.52370746691639,
1.00498768038198));
#71013=CARTESIAN_POINT('Ctrl Pts',(-0.329324827126571,1.52032670267708,
1.00613501485091));
#71014=CARTESIAN_POINT('Ctrl Pts',(-0.415928134730588,1.50061099860013,
1.01230195857146));
#71015=CARTESIAN_POINT('Ctrl Pts',(-0.485371964030678,1.47961015371916,
1.01711245896106));
#71016=CARTESIAN_POINT('Ctrl Pts',(-0.613870513446562,1.43072360236324,
1.02618087146745));
#71017=CARTESIAN_POINT('Ctrl Pts',(-0.673124875431059,1.40381968665097,
1.03043598953591));
#71018=CARTESIAN_POINT('Ctrl Pts',(-0.767073201720941,1.35384380712579,
1.03752016919881));
#71019=CARTESIAN_POINT('Ctrl Pts',(-0.802831926286873,1.3329496867159,1.04030224056641));
#71020=CARTESIAN_POINT('Ctrl Pts',(-0.863280611184542,1.29431356272571,
1.04520045266843));
#71021=CARTESIAN_POINT('Ctrl Pts',(-0.888363127674324,1.27722815442603,
1.04729481949152));
#71022=CARTESIAN_POINT('Ctrl Pts',(-0.924887434124145,1.25075243075224,
1.0504491633037));
#71023=CARTESIAN_POINT('Ctrl Pts',(-0.936721772073318,1.24191412906317,
1.05148819933784));
#71024=CARTESIAN_POINT('Ctrl Pts',(-0.957806965145237,1.22569412320197,
1.05337151349873));
#71025=CARTESIAN_POINT('Ctrl Pts',(-0.96710294939559,1.21837274151374,1.05421337455123));
#71026=CARTESIAN_POINT('Ctrl Pts',(-0.986912342666978,1.20240159978864,
1.05603298124082));
#71027=CARTESIAN_POINT('Ctrl Pts',(-0.997397461981246,1.19371850126346,
1.05701202471686));
#71028=CARTESIAN_POINT('Ctrl Pts',(-1.02580090396011,1.1695611285888,1.05970913338976));
#71029=CARTESIAN_POINT('Ctrl Pts',(-1.04348136141507,1.15381422351143,1.06143825587099));
#71030=CARTESIAN_POINT('Ctrl Pts',(-1.14131694306618,1.06258970350716,1.07130132611706));
#71031=CARTESIAN_POINT('Ctrl Pts',(-1.21362659262786,0.979185027256165,
1.07977639651119));
#71032=CARTESIAN_POINT('Ctrl Pts',(-1.32470051676394,0.819669853337824,
1.09485004100646));
#71033=CARTESIAN_POINT('Ctrl Pts',(-1.36718278928739,0.746662120492023,
1.10138986949551));
#71034=CARTESIAN_POINT('Ctrl Pts',(-1.40933026401122,0.658444271783863,
1.10864840838774));
#71035=CARTESIAN_POINT('Ctrl Pts',(-1.41496347625935,0.646249986748281,
1.10963803485002));
#71036=CARTESIAN_POINT('Ctrl Pts',(-1.42352197205447,0.62707470753663,1.11117121190658));
#71037=CARTESIAN_POINT('Ctrl Pts',(-1.42655531089423,0.620143084458317,
1.11172079679926));
#71038=CARTESIAN_POINT('Ctrl Pts',(-1.43221718429254,0.606943470684567,
1.11275819686319));
#71039=CARTESIAN_POINT('Ctrl Pts',(-1.43485528551005,0.60068024038802,1.11324652107264));
#71040=CARTESIAN_POINT('Ctrl Pts',(-1.44115854644419,0.585436896212434,
1.1144258795316));
#71041=CARTESIAN_POINT('Ctrl Pts',(-1.44478092145409,0.576439430732838,
1.11511439915468));
#71042=CARTESIAN_POINT('Ctrl Pts',(-1.45706253830672,0.545090405231021,
1.11748904274888));
#71043=CARTESIAN_POINT('Ctrl Pts',(-1.46528962750255,0.522571771381402,
1.11915221299581));
#71044=CARTESIAN_POINT('Ctrl Pts',(-1.50336086093163,0.410385349732555,
1.12727193303035));
#71045=CARTESIAN_POINT('Ctrl Pts',(-1.52551390061082,0.318309759635744,
1.13342720236391));
#71046=CARTESIAN_POINT('Ctrl Pts',(-1.55001067948958,0.150572425861762,
1.14459839210316));
#71047=CARTESIAN_POINT('Ctrl Pts',(-1.55546646918372,0.0756807431247202,
1.1495710878573));
#71048=CARTESIAN_POINT('Ctrl Pts',(-1.55549984592239,0.000692340549475381,
1.15469914303843));
#71049=CARTESIAN_POINT('Origin',(0.,0.,-1.2940562256037));
#71050=CARTESIAN_POINT('',(-1.55549999695016,-9.74065728153838E-5,1.9925897317728));
#71051=CARTESIAN_POINT('',(-1.5555,-2.74013238336738E-11,1.8552873792152));
#71052=CARTESIAN_POINT('',(-1.5555,-1.46451138874614E-13,-1.2940562256037));
#71053=CARTESIAN_POINT('',(-1.55549944251185,-0.00131694544789358,1.29458843968849));
#71054=CARTESIAN_POINT('Ctrl Pts',(-1.55549999695016,-9.74065733091837E-5,
1.99258973177283));
#71055=CARTESIAN_POINT('Ctrl Pts',(-1.55550042240159,0.00669669026298216,
1.99209974652595));
#71056=CARTESIAN_POINT('Ctrl Pts',(-1.55545633515302,0.0134908251544085,
1.99161230739549));
#71057=CARTESIAN_POINT('Ctrl Pts',(-1.55523249795908,0.030654068342381,
1.99038689780355));
#71058=CARTESIAN_POINT('Ctrl Pts',(-1.5549935624627,0.0410223211014157,
1.98965211790128));
#71059=CARTESIAN_POINT('Ctrl Pts',(-1.55358192282881,0.0837291063027906,
1.98664527636159));
#71060=CARTESIAN_POINT('Ctrl Pts',(-1.55150387733412,0.116032038609492,
1.98441748339199));
#71061=CARTESIAN_POINT('Ctrl Pts',(-1.54256037562029,0.209444232643618,
1.9780492879162));
#71062=CARTESIAN_POINT('Ctrl Pts',(-1.53307841464066,0.270242600687175,
1.97399543916995));
#71063=CARTESIAN_POINT('Ctrl Pts',(-1.49743200941476,0.434273455668504,
1.9629455430482));
#71064=CARTESIAN_POINT('Ctrl Pts',(-1.46424194660417,0.535619591522633,
1.95597394652533));
#71065=CARTESIAN_POINT('Ctrl Pts',(-1.41133476944503,0.654427914580389,
1.94702542055528));
#71066=CARTESIAN_POINT('Ctrl Pts',(-1.40120248882616,0.675849990047823,
1.94538029727317));
#71067=CARTESIAN_POINT('Ctrl Pts',(-1.38457797880069,0.709016073637523,
1.94277822597506));
#71068=CARTESIAN_POINT('Ctrl Pts',(-1.37841611833844,0.720922295846305,
1.94183274415279));
#71069=CARTESIAN_POINT('Ctrl Pts',(-1.36667691411272,0.742904475360018,
1.94006500008127));
#71070=CARTESIAN_POINT('Ctrl Pts',(-1.36114003768344,0.753001083522817,
1.9392442195225));
#71071=CARTESIAN_POINT('Ctrl Pts',(-1.34853406815254,0.775394926802664,
1.93740338952845));
#71072=CARTESIAN_POINT('Ctrl Pts',(-1.34140792262617,0.787658673411109,
1.93638133735227));
#71073=CARTESIAN_POINT('Ctrl Pts',(-1.31952881339227,0.824153320517702,
1.93329673518592));
#71074=CARTESIAN_POINT('Ctrl Pts',(-1.30428044598937,0.848078597914033,
1.93121637744028));
#71075=CARTESIAN_POINT('Ctrl Pts',(-1.24984305865419,0.928549775038145,
1.92401222878502));
#71076=CARTESIAN_POINT('Ctrl Pts',(-1.20756654330442,0.982900391575368,
1.91878016273706));
#71077=CARTESIAN_POINT('Ctrl Pts',(-1.12693314945042,1.07347923964885,1.90942986312774));
#71078=CARTESIAN_POINT('Ctrl Pts',(-1.09006641680109,1.1108964928434,1.90534825770143));
#71079=CARTESIAN_POINT('Ctrl Pts',(-1.00185600507271,1.19179710344253,1.89608068486811));
#71080=CARTESIAN_POINT('Ctrl Pts',(-0.949435266784904,1.2339653672362,1.89091384742753));
#71081=CARTESIAN_POINT('Ctrl Pts',(-0.8840976239087,1.27988734630444,1.88499330068621));
#71082=CARTESIAN_POINT('Ctrl Pts',(-0.873660844490999,1.28703418138462,
1.8840624401335));
#71083=CARTESIAN_POINT('Ctrl Pts',(-0.85707909131719,1.29809426351719,1.88260815267143));
#71084=CARTESIAN_POINT('Ctrl Pts',(-0.850992100570774,1.30209282938476,
1.8820794410913));
#71085=CARTESIAN_POINT('Ctrl Pts',(-0.839293226527584,1.30966077943526,
1.88107341521404));
#71086=CARTESIAN_POINT('Ctrl Pts',(-0.833686247326268,1.31323711498445,
1.8805956860591));
#71087=CARTESIAN_POINT('Ctrl Pts',(-0.819920535842528,1.32189369206497,
1.87943322593413));
#71088=CARTESIAN_POINT('Ctrl Pts',(-0.811737154130547,1.32693459648706,
1.87875101196142));
#71089=CARTESIAN_POINT('Ctrl Pts',(-0.781185091089543,1.34536602146513,
1.87623457341919));
#71090=CARTESIAN_POINT('Ctrl Pts',(-0.758526195414836,1.35827025675906,
1.87442846067734));
#71091=CARTESIAN_POINT('Ctrl Pts',(-0.697421538640053,1.3910629471175,1.86968622527334));
#71092=CARTESIAN_POINT('Ctrl Pts',(-0.658450929898505,1.40992759909519,
1.86679261128791));
#71093=CARTESIAN_POINT('Ctrl Pts',(-0.496755171104799,1.48003120496167,
1.8551114163104));
#71094=CARTESIAN_POINT('Ctrl Pts',(-0.368502769447701,1.51705692645734,
1.8465321251534));
#71095=CARTESIAN_POINT('Ctrl Pts',(-0.213882348908616,1.54090452907775,
1.83576475283433));
#71096=CARTESIAN_POINT('Ctrl Pts',(-0.190581448328274,1.54395953243374,
1.83413296822417));
#71097=CARTESIAN_POINT('Ctrl Pts',(-0.15393487376396,1.54792212275118,1.8315473473044));
#71098=CARTESIAN_POINT('Ctrl Pts',(-0.140630856025979,1.54918745988524,
1.8306047349969));
#71099=CARTESIAN_POINT('Ctrl Pts',(-0.115833139937345,1.55122390364735,
1.82883960791086));
#71100=CARTESIAN_POINT('Ctrl Pts',(-0.104343906238084,1.55203906254514,
1.82801853869876));
#71101=CARTESIAN_POINT('Ctrl Pts',(-0.0786348425843992,1.55357636373879,
1.82617346295836));
#71102=CARTESIAN_POINT('Ctrl Pts',(-0.0644121854129839,1.55423100011759,
1.82514740990195));
#71103=CARTESIAN_POINT('Ctrl Pts',(-0.0215409314190439,1.55561481727486,
1.82203751776997));
#71104=CARTESIAN_POINT('Ctrl Pts',(0.00711931223707813,1.55574759709805,
1.81993543250216));
#71105=CARTESIAN_POINT('Ctrl Pts',(0.110600894710714,1.55336764378502,1.81225748584931));
#71106=CARTESIAN_POINT('Ctrl Pts',(0.18520459516661,1.54624709059672,1.80654937089049));
#71107=CARTESIAN_POINT('Ctrl Pts',(0.35108186265785,1.51823687986099,1.7935530488995));
#71108=CARTESIAN_POINT('Ctrl Pts',(0.441581636394824,1.49442582896406,1.78624540831788));
#71109=CARTESIAN_POINT('Ctrl Pts',(0.5533774719476,1.45396141400024,1.77725642090986));
#71110=CARTESIAN_POINT('Ctrl Pts',(0.577138477655064,1.44469435755366,1.77534921137645));
#71111=CARTESIAN_POINT('Ctrl Pts',(0.609704926740366,1.43106123081994,1.7727496259907));
#71112=CARTESIAN_POINT('Ctrl Pts',(0.618711659046347,1.42719033082052,1.77203223172054));
#71113=CARTESIAN_POINT('Ctrl Pts',(0.63373690278963,1.4205638274673,1.77083878944275));
#71114=CARTESIAN_POINT('Ctrl Pts',(0.639775405183407,1.41785453685955,1.77036007229562));
#71115=CARTESIAN_POINT('Ctrl Pts',(0.652335418883908,1.41212266124957,1.76936650272906));
#71116=CARTESIAN_POINT('Ctrl Pts',(0.658853555281885,1.40909329266088,1.76885206428689));
#71117=CARTESIAN_POINT('Ctrl Pts',(0.67638355853743,1.40079781393772,1.76747109696171));
#71118=CARTESIAN_POINT('Ctrl Pts',(0.68735510211705,1.39544696133576,1.76660954685675));
#71119=CARTESIAN_POINT('Ctrl Pts',(0.750160335241729,1.36389616965809,1.76168709577322));
#71120=CARTESIAN_POINT('Ctrl Pts',(0.800563480618143,1.33493560235412,1.75777304416725));
#71121=CARTESIAN_POINT('Ctrl Pts',(0.955618548785537,1.23389507517694,1.74547188316114));
#71122=CARTESIAN_POINT('Ctrl Pts',(1.05310874978011,1.15180957201234,1.73729255546327));
#71123=CARTESIAN_POINT('Ctrl Pts',(1.16077135661094,1.0359358906346,1.72650397885697));
#71124=CARTESIAN_POINT('Ctrl Pts',(1.18131070279753,1.01245153504198,1.72435256141543));
#71125=CARTESIAN_POINT('Ctrl Pts',(1.21046688852601,0.977019002578325,1.72114512266678));
#71126=CARTESIAN_POINT('Ctrl Pts',(1.21964310643819,0.965539686559332,1.72011169744114));
#71127=CARTESIAN_POINT('Ctrl Pts',(1.23574085882477,0.944805949004342,1.71825409328068));
#71128=CARTESIAN_POINT('Ctrl Pts',(1.24272459877097,0.935601042044511,1.71743246121537));
#71129=CARTESIAN_POINT('Ctrl Pts',(1.2573754703902,0.915837014798329,1.71567425670148));
#71130=CARTESIAN_POINT('Ctrl Pts',(1.26501353062137,0.905257565162052,1.71473663596056));
#71131=CARTESIAN_POINT('Ctrl Pts',(1.28552592735114,0.876079317055153,1.71215943502555));
#71132=CARTESIAN_POINT('Ctrl Pts',(1.29812863689277,0.85729447789019,1.71050975608045));
#71133=CARTESIAN_POINT('Ctrl Pts',(1.32542466723428,0.814626099995463,1.70678160612249));
#71134=CARTESIAN_POINT('Ctrl Pts',(1.33989048112244,0.790607077749816,1.70469572743318));
#71135=CARTESIAN_POINT('Ctrl Pts',(1.38598984211966,0.709161378820918,1.69766434437611));
#71136=CARTESIAN_POINT('Ctrl Pts',(1.41463909913779,0.650132541306723,1.69263183984459));
#71137=CARTESIAN_POINT('Ctrl Pts',(1.47761320598073,0.496352884787545,1.6797678566552));
#71138=CARTESIAN_POINT('Ctrl Pts',(1.50662473965882,0.399739869686322,1.67189971801405));
#71139=CARTESIAN_POINT('Ctrl Pts',(1.52895671009825,0.286512702427338,1.66330608376524));
#71140=CARTESIAN_POINT('Ctrl Pts',(1.53160694539565,0.271989626569737,1.66221571267937));
#71141=CARTESIAN_POINT('Ctrl Pts',(1.53534361392497,0.249722488311717,1.66056423800519));
#71142=CARTESIAN_POINT('Ctrl Pts',(1.53657900224458,0.242004774604928,1.65999555613959));
#71143=CARTESIAN_POINT('Ctrl Pts',(1.53873794463341,0.227833878964166,1.65895856983725));
#71144=CARTESIAN_POINT('Ctrl Pts',(1.53967914809701,0.221383970630543,1.65848935479183));
#71145=CARTESIAN_POINT('Ctrl Pts',(1.54177111077939,0.206389012378765,1.65740476614938));
#71146=CARTESIAN_POINT('Ctrl Pts',(1.54289140977704,0.197840060014053,1.65679107949262));
#71147=CARTESIAN_POINT('Ctrl Pts',(1.54632126300174,0.169863334843644,1.65479667149174));
#71148=CARTESIAN_POINT('Ctrl Pts',(1.5483355024413,0.150400346591329,1.65343105919379));
#71149=CARTESIAN_POINT('Ctrl Pts',(1.55238145260537,0.102493641838777,1.65011178396755));
#71150=CARTESIAN_POINT('Ctrl Pts',(1.55399940246688,0.0740214853586055,
1.64817531826315));
#71151=CARTESIAN_POINT('Ctrl Pts',(1.55791639385685,-0.0597739854922687,
1.63917876770213));
#71152=CARTESIAN_POINT('Ctrl Pts',(1.55029571732122,-0.165111385533724,
1.63237794902716));
#71153=CARTESIAN_POINT('Ctrl Pts',(1.52163349124112,-0.328433055147209,
1.62133646806496));
#71154=CARTESIAN_POINT('Ctrl Pts',(1.50771830971467,-0.387325391405457,
1.61725319240488));
#71155=CARTESIAN_POINT('Ctrl Pts',(1.4850068635085,-0.463348125058852,1.61175240737552));
#71156=CARTESIAN_POINT('Ctrl Pts',(1.47927246579131,-0.481341653742719,
1.61043333478162));
#71157=CARTESIAN_POINT('Ctrl Pts',(1.469273085226,-0.510849769315237,1.60823930132945));
#71158=CARTESIAN_POINT('Ctrl Pts',(1.46519670696532,-0.522426530785203,
1.6073705882895));
#71159=CARTESIAN_POINT('Ctrl Pts',(1.45692694211236,-0.545053954192963,
1.60565634690366));
#71160=CARTESIAN_POINT('Ctrl Pts',(1.45274374687497,-0.556107471000831,
1.60481120821579));
#71161=CARTESIAN_POINT('Ctrl Pts',(1.44240814363397,-0.582505169100086,
1.60277368091914));
#71162=CARTESIAN_POINT('Ctrl Pts',(1.43613640247646,-0.597800735251731,
1.60157734841902));
#71163=CARTESIAN_POINT('Ctrl Pts',(1.41260315075026,-0.652684994311897,
1.59722572760465));
#71164=CARTESIAN_POINT('Ctrl Pts',(1.39394004659215,-0.691647197437364,
1.5940237954592));
#71165=CARTESIAN_POINT('Ctrl Pts',(1.34034412812436,-0.792532141444396,
1.58542535729496));
#71166=CARTESIAN_POINT('Ctrl Pts',(1.30274868731775,-0.852920589182869,
1.5799529953886));
#71167=CARTESIAN_POINT('Ctrl Pts',(1.20787084878965,-0.984335611636769,
1.56738943898602));
#71168=CARTESIAN_POINT('Ctrl Pts',(1.1481981189719,-1.05333398858936,1.56029576845));
#71169=CARTESIAN_POINT('Ctrl Pts',(1.07150392429687,-1.12770048087016,1.55232942889065));
#71170=CARTESIAN_POINT('Ctrl Pts',(1.06001334522495,-1.13850814365394,1.5511630932229));
#71171=CARTESIAN_POINT('Ctrl Pts',(1.0425042943951,-1.15448164534395,1.54942875078616));
#71172=CARTESIAN_POINT('Ctrl Pts',(1.03660788913597,-1.15977892928544,1.54885179553724));
#71173=CARTESIAN_POINT('Ctrl Pts',(1.02628516539578,-1.16891116030012,1.54785439818787));
#71174=CARTESIAN_POINT('Ctrl Pts',(1.02187744487876,-1.17276640123739,1.54743249534417));
#71175=CARTESIAN_POINT('Ctrl Pts',(1.01131073451146,-1.18190383523552,1.5464304374402));
#71176=CARTESIAN_POINT('Ctrl Pts',(1.00513205217448,-1.18716285444679,1.54585196317003));
#71177=CARTESIAN_POINT('Ctrl Pts',(0.986077218852454,-1.20312606454267,
1.54408964291304));
#71178=CARTESIAN_POINT('Ctrl Pts',(0.973068654093634,-1.2136713156748,1.54291644901125));
#71179=CARTESIAN_POINT('Ctrl Pts',(0.941761815017421,-1.2382228280371,1.54015616641951));
#71180=CARTESIAN_POINT('Ctrl Pts',(0.923317285083143,-1.25203689947955,
1.53857960897408));
#71181=CARTESIAN_POINT('Ctrl Pts',(0.850111614545197,-1.30436647718886,
1.53248349762847));
#71182=CARTESIAN_POINT('Ctrl Pts',(0.793191335935832,-1.3397426743099,1.52808407595263));
#71183=CARTESIAN_POINT('Ctrl Pts',(0.647271099905978,-1.41786284018175,
1.51719273302274));
#71184=CARTESIAN_POINT('Ctrl Pts',(0.556162694338765,-1.45601337694449,
1.51070689246357));
#71185=CARTESIAN_POINT('Ctrl Pts',(0.44123597303963,-1.49176634374891,1.50242804825739));
#71186=CARTESIAN_POINT('Ctrl Pts',(0.420275595667262,-1.49780651353516,
1.50091525607307));
#71187=CARTESIAN_POINT('Ctrl Pts',(0.385577225897743,-1.5070199071476,1.49840202778982));
#71188=CARTESIAN_POINT('Ctrl Pts',(0.37191035792813,-1.51045074733249,1.49740989195976));
#71189=CARTESIAN_POINT('Ctrl Pts',(0.346997833771406,-1.51634601891086,
1.49559634807217));
#71190=CARTESIAN_POINT('Ctrl Pts',(0.335767716777587,-1.51887220430872,
1.49477699249018));
#71191=CARTESIAN_POINT('Ctrl Pts',(0.311325844056116,-1.52408602914984,
1.49298918127931));
#71192=CARTESIAN_POINT('Ctrl Pts',(0.298105210515063,-1.52672697874053,
1.49201930197494));
#71193=CARTESIAN_POINT('Ctrl Pts',(0.260523985397398,-1.53372745520851,
1.48925338129883));
#71194=CARTESIAN_POINT('Ctrl Pts',(0.236092369202305,-1.53767776749234,
1.48744461066454));
#71195=CARTESIAN_POINT('Ctrl Pts',(0.180301525189084,-1.54533759374342,
1.48328767599053));
#71196=CARTESIAN_POINT('Ctrl Pts',(0.148903490368004,-1.54867828173776,
1.48092923947184));
#71197=CARTESIAN_POINT('Ctrl Pts',(0.0361448519108882,-1.55721499115108,
1.47239293873807));
#71198=CARTESIAN_POINT('Ctrl Pts',(-0.0454882902225601,-1.55696927000366,
1.46608092289781));
#71199=CARTESIAN_POINT('Ctrl Pts',(-0.201811487278772,-1.54419207842826,
1.4539163793286));
#71200=CARTESIAN_POINT('Ctrl Pts',(-0.276367856641488,-1.53260564010354,
1.44808284438709));
#71201=CARTESIAN_POINT('Ctrl Pts',(-0.36559277444116,-1.51201355057665,
1.4412493200826));
#71202=CARTESIAN_POINT('Ctrl Pts',(-0.381331667675789,-1.50812110521511,
1.44004986295108));
#71203=CARTESIAN_POINT('Ctrl Pts',(-0.404753775105823,-1.50193835271276,
1.43827658676716));
#71204=CARTESIAN_POINT('Ctrl Pts',(-0.412484239437945,-1.4998337219893,
1.43769324099884));
#71205=CARTESIAN_POINT('Ctrl Pts',(-0.425832689426701,-1.49608857214347,
1.43668969785668));
#71206=CARTESIAN_POINT('Ctrl Pts',(-0.431458026469112,-1.49447598495009,
1.43626796496759));
#71207=CARTESIAN_POINT('Ctrl Pts',(-0.444774238752368,-1.49057723566151,
1.4352724121881));
#71208=CARTESIAN_POINT('Ctrl Pts',(-0.452456699423105,-1.48826327027236,
1.43470019850365));
#71209=CARTESIAN_POINT('Ctrl Pts',(-0.475663733470028,-1.48107697275505,
1.43297719427063));
#71210=CARTESIAN_POINT('Ctrl Pts',(-0.491130665509083,-1.47602022708121,
1.43183637779808));
#71211=CARTESIAN_POINT('Ctrl Pts',(-0.570348505492139,-1.44873761801244,
1.42601839445595));
#71212=CARTESIAN_POINT('Ctrl Pts',(-0.632689836800856,-1.42261865655347,
1.42152217420117));
#71213=CARTESIAN_POINT('Ctrl Pts',(-0.805837881249277,-1.33643271326311,
1.40875072909323));
#71214=CARTESIAN_POINT('Ctrl Pts',(-0.911294795102424,-1.26687235284656,
1.40057790419277));
#71215=CARTESIAN_POINT('Ctrl Pts',(-1.02393193334483,-1.17116390031802,
1.39037892928127));
#71216=CARTESIAN_POINT('Ctrl Pts',(-1.04034595860708,-1.15660783717111,
1.38885234592013));
#71217=CARTESIAN_POINT('Ctrl Pts',(-1.06591969417315,-1.13294397573777,
1.38640470642414));
#71218=CARTESIAN_POINT('Ctrl Pts',(-1.0752836360918,-1.124060465681,1.38549313448061));
#71219=CARTESIAN_POINT('Ctrl Pts',(-1.09283701789119,-1.10698762630689,
1.38375409753356));
#71220=CARTESIAN_POINT('Ctrl Pts',(-1.10104770441881,-1.09882131927994,
1.3829276725442));
#71221=CARTESIAN_POINT('Ctrl Pts',(-1.10953585517822,-1.09018838463639,
1.38205935470084));
#71222=CARTESIAN_POINT('Ctrl Pts',(-1.10990527288889,-1.08981228343891,
1.38202153614781));
#71223=CARTESIAN_POINT('Ctrl Pts',(-1.11100381338066,-1.08869273029426,
1.38190899142423));
#71224=CARTESIAN_POINT('Ctrl Pts',(-1.11173237965975,-1.0879487351655,1.38183424090737));
#71225=CARTESIAN_POINT('Ctrl Pts',(-1.11312712635291,-1.08652158794629,
1.38169093048727));
#71226=CARTESIAN_POINT('Ctrl Pts',(-1.11379342658473,-1.08583855309392,
1.38162237587091));
#71227=CARTESIAN_POINT('Ctrl Pts',(-1.11508251506942,-1.08451465327213,
1.38148956463998));
#71228=CARTESIAN_POINT('Ctrl Pts',(-1.11570538054872,-1.08387386368707,
1.38142531143358));
#71229=CARTESIAN_POINT('Ctrl Pts',(-1.1169218050378,-1.08262027473558,1.38129966937235));
#71230=CARTESIAN_POINT('Ctrl Pts',(-1.11751541288339,-1.08200752298683,
1.38123828267683));
#71231=CARTESIAN_POINT('Ctrl Pts',(-1.1186846087931,-1.08079863190838,1.38111722636629));
#71232=CARTESIAN_POINT('Ctrl Pts',(-1.11926022524283,-1.0802025203035,1.38105755801418));
#71233=CARTESIAN_POINT('Ctrl Pts',(-1.13216040008558,-1.06682164555934,
1.37971875127788));
#71234=CARTESIAN_POINT('Ctrl Pts',(-1.14426511282732,-1.05382773635198,
1.37843018740865));
#71235=CARTESIAN_POINT('Ctrl Pts',(-1.17030020272246,-1.02490264108695,
1.37558546007939));
#71236=CARTESIAN_POINT('Ctrl Pts',(-1.18413308080033,-1.00888887162499,
1.37402562893014));
#71237=CARTESIAN_POINT('Ctrl Pts',(-1.22410267252708,-0.96066297481476,
1.36937091883344));
#71238=CARTESIAN_POINT('Ctrl Pts',(-1.24928078478142,-0.9276840534824,1.36624188408179));
#71239=CARTESIAN_POINT('Ctrl Pts',(-1.32767018534053,-0.816020517526509,
1.35583114064007));
#71240=CARTESIAN_POINT('Ctrl Pts',(-1.37499774255554,-0.733469067908072,
1.34840530939154));
#71241=CARTESIAN_POINT('Ctrl Pts',(-1.4353620536622,-0.601523801398121,
1.33723289275254));
#71242=CARTESIAN_POINT('Ctrl Pts',(-1.45400983333373,-0.554933859497567,
1.33341324503986));
#71243=CARTESIAN_POINT('Ctrl Pts',(-1.47432505632885,-0.496077023277669,
1.32880261628201));
#71244=CARTESIAN_POINT('Ctrl Pts',(-1.47814111446276,-0.484588128944107,
1.32791256703494));
#71245=CARTESIAN_POINT('Ctrl Pts',(-1.48400202963421,-0.466229099546399,
1.32650732027827));
#71246=CARTESIAN_POINT('Ctrl Pts',(-1.48613411007386,-0.459387646398022,
1.32598739335756));
#71247=CARTESIAN_POINT('Ctrl Pts',(-1.49017028977825,-0.446114054117088,
1.32498618701739));
#71248=CARTESIAN_POINT('Ctrl Pts',(-1.49208017156295,-0.439683983852518,
1.32450461491047));
#71249=CARTESIAN_POINT('Ctrl Pts',(-1.49671384447043,-0.423705676292738,
1.32331601758002));
#71250=CARTESIAN_POINT('Ctrl Pts',(-1.49938798582166,-0.414143108185379,
1.32261178730915));
#71251=CARTESIAN_POINT('Ctrl Pts',(-1.50499488347232,-0.39332668194911,
1.32109283446394));
#71252=CARTESIAN_POINT('Ctrl Pts',(-1.50789339518977,-0.382064138797969,
1.32027987779891));
#71253=CARTESIAN_POINT('Ctrl Pts',(-1.5403387351931,-0.249868743657241,
1.31082954772173));
#71254=CARTESIAN_POINT('Ctrl Pts',(-1.55539402393791,-0.125831239692401,
1.30283100004325));
#71255=CARTESIAN_POINT('Ctrl Pts',(-1.55549944251185,-0.00131694544789358,
1.29458843968849));
#71256=CARTESIAN_POINT('Ctrl Pts',(-1.55549944365257,-0.00131559740958673,
1.29458835045145));
#71257=CARTESIAN_POINT('Ctrl Pts',(-1.55549981455353,-0.000877061857157378,
1.29455932040035));
#71258=CARTESIAN_POINT('Ctrl Pts',(-1.55550000000001,-0.000438529336851416,
1.29453028833394));
#71259=CARTESIAN_POINT('Ctrl Pts',(-1.5555,3.44063942631422E-11,1.29450125422325));
#71260=CARTESIAN_POINT('Ctrl Pts',(-1.55549984592239,0.000692340549475381,
1.15469914303843));
#71261=CARTESIAN_POINT('Ctrl Pts',(-1.55551257150503,-0.027898562953657,
1.1566543217835));
#71262=CARTESIAN_POINT('Ctrl Pts',(-1.55473702459326,-0.0564827265290557,
1.15862986850662));
#71263=CARTESIAN_POINT('Ctrl Pts',(-1.55237477829611,-0.0996330809139592,
1.1616526805757));
#71264=CARTESIAN_POINT('Ctrl Pts',(-1.55136927411398,-0.114225884010962,
1.16268195301729));
#71265=CARTESIAN_POINT('Ctrl Pts',(-1.54917927419936,-0.140582995622195,
1.16455478456607));
#71266=CARTESIAN_POINT('Ctrl Pts',(-1.54806614344282,-0.152352235574461,
1.16539604474447));
#71267=CARTESIAN_POINT('Ctrl Pts',(-1.54537199378593,-0.177746355919815,
1.16722255598176));
#71268=CARTESIAN_POINT('Ctrl Pts',(-1.54374470130584,-0.191365203346941,
1.16820919653007));
#71269=CARTESIAN_POINT('Ctrl Pts',(-1.53866421279967,-0.229586234511424,
1.17099902838866));
#71270=CARTESIAN_POINT('Ctrl Pts',(-1.53480156302857,-0.254128765242878,
1.172814870643));
#71271=CARTESIAN_POINT('Ctrl Pts',(-1.52470483006877,-0.309596804834773,
1.17697686031794));
#71272=CARTESIAN_POINT('Ctrl Pts',(-1.51811448268113,-0.340445546959844,
1.1793330596931));
#71273=CARTESIAN_POINT('Ctrl Pts',(-1.48004058039864,-0.495440521408541,
1.19138082780159));
#71274=CARTESIAN_POINT('Ctrl Pts',(-1.43424687375455,-0.6155572796414,1.20145975086901));
#71275=CARTESIAN_POINT('Ctrl Pts',(-1.35684646593193,-0.761531711890244,
1.21408418243729));
#71276=CARTESIAN_POINT('Ctrl Pts',(-1.33825356437203,-0.793751086447115,
1.21689229799129));
#71277=CARTESIAN_POINT('Ctrl Pts',(-1.31250936790574,-0.834881931413758,
1.22047830722698));
#71278=CARTESIAN_POINT('Ctrl Pts',(-1.3063917238745,-0.844422503343065,
1.22131017186896));
#71279=CARTESIAN_POINT('Ctrl Pts',(-1.29626455838588,-0.859842463322647,
1.22265372547877));
#71280=CARTESIAN_POINT('Ctrl Pts',(-1.29231813935291,-0.865762495861777,
1.22316931104151));
#71281=CARTESIAN_POINT('Ctrl Pts',(-1.28436899039843,-0.87751156100424,
1.22419176570673));
#71282=CARTESIAN_POINT('Ctrl Pts',(-1.28036686423132,-0.883340784289243,
1.22469865208484));
#71283=CARTESIAN_POINT('Ctrl Pts',(-1.26996638378299,-0.898270214723518,
1.22599640002921));
#71284=CARTESIAN_POINT('Ctrl Pts',(-1.26350976646733,-0.907329644355399,
1.22678345419836));
#71285=CARTESIAN_POINT('Ctrl Pts',(-1.23437541166623,-0.947294542114509,
1.2302573524832));
#71286=CARTESIAN_POINT('Ctrl Pts',(-1.21065506531935,-0.977427482498418,
1.23288177181989));
#71287=CARTESIAN_POINT('Ctrl Pts',(-1.13143761463001,-1.07074585326335,
1.24113752833254));
#71288=CARTESIAN_POINT('Ctrl Pts',(-1.07192267362721,-1.13032352718731,
1.24661343932134));
#71289=CARTESIAN_POINT('Ctrl Pts',(-0.944573608882746,-1.23865614171747,
1.2576475089124));
#71290=CARTESIAN_POINT('Ctrl Pts',(-0.877059837393692,-1.28734290569844,
1.26318774073735));
#71291=CARTESIAN_POINT('Ctrl Pts',(-0.788633023455372,-1.34091381355098,
1.27034088175279));
#71292=CARTESIAN_POINT('Ctrl Pts',(-0.771076631976693,-1.35108573467332,
1.27175581641909));
#71293=CARTESIAN_POINT('Ctrl Pts',(-0.742145474283537,-1.36710046495544,
1.27408209854847));
#71294=CARTESIAN_POINT('Ctrl Pts',(-0.730888403587942,-1.37315174334064,
1.2749859449404));
#71295=CARTESIAN_POINT('Ctrl Pts',(-0.708885840312691,-1.38463209095437,
1.27675077615059));
#71296=CARTESIAN_POINT('Ctrl Pts',(-0.69814933997256,-1.39007648925562,
1.27761114211641));
#71297=CARTESIAN_POINT('Ctrl Pts',(-0.672619022808428,-1.4026523417733,
1.27965570167936));
#71298=CARTESIAN_POINT('Ctrl Pts',(-0.657773593015741,-1.40967507023487,
1.2808435643331));
#71299=CARTESIAN_POINT('Ctrl Pts',(-0.605866449725281,-1.43323163787405,
1.28499507257164));
#71300=CARTESIAN_POINT('Ctrl Pts',(-0.568273906151289,-1.44854799615041,
1.2879989965888));
#71301=CARTESIAN_POINT('Ctrl Pts',(-0.470213808685758,-1.4840959402274,
1.29583206701084));
#71302=CARTESIAN_POINT('Ctrl Pts',(-0.409026695516784,-1.50211100029218,
1.30071944156057));
#71303=CARTESIAN_POINT('Ctrl Pts',(-0.246432125887757,-1.53931035147845,
1.31362272494032));
#71304=CARTESIAN_POINT('Ctrl Pts',(-0.143908487441227,-1.55225597248363,
1.32168746925037));
#71305=CARTESIAN_POINT('Ctrl Pts',(-0.0262605372461818,-1.55534680592977,
1.33044705839491));
#71306=CARTESIAN_POINT('Ctrl Pts',(-0.011663871183709,-1.55552476592351,
1.33152483795714));
#71307=CARTESIAN_POINT('Ctrl Pts',(0.0108322838024829,-1.55548233600033,
1.33316987070728));
#71308=CARTESIAN_POINT('Ctrl Pts',(0.0187307543558288,-1.55540727853855,
1.33374440185324));
#71309=CARTESIAN_POINT('Ctrl Pts',(0.0326658240077856,-1.55516868970386,
1.33475226496763));
#71310=CARTESIAN_POINT('Ctrl Pts',(0.0387022994507902,-1.55503017453997,
1.33518691171666));
#71311=CARTESIAN_POINT('Ctrl Pts',(0.0533941646873858,-1.55460744296237,
1.33624019030064));
#71312=CARTESIAN_POINT('Ctrl Pts',(0.0620482142251911,-1.5542860956146,
1.33685677870773));
#71313=CARTESIAN_POINT('Ctrl Pts',(0.0897163930256136,-1.5530272417345,
1.33881714514677));
#71314=CARTESIAN_POINT('Ctrl Pts',(0.108717018673513,-1.55181292015254,
1.34014684359232));
#71315=CARTESIAN_POINT('Ctrl Pts',(0.154876773261621,-1.54801081393482,
1.34334741189554));
#71316=CARTESIAN_POINT('Ctrl Pts',(0.181999974660383,-1.54505679005421,
1.34520291656093));
#71317=CARTESIAN_POINT('Ctrl Pts',(0.301853865953547,-1.52880301365944,
1.35334565183725));
#71318=CARTESIAN_POINT('Ctrl Pts',(0.393352308920886,-1.50785619871998,
1.35942162203061));
#71319=CARTESIAN_POINT('Ctrl Pts',(0.550756781489194,-1.45650781133415,
1.37038728987654));
#71320=CARTESIAN_POINT('Ctrl Pts',(0.617463816418402,-1.42950500001155,
1.37520862876884));
#71321=CARTESIAN_POINT('Ctrl Pts',(0.699991560594923,-1.38924085535629,
1.38156522741266));
#71322=CARTESIAN_POINT('Ctrl Pts',(0.71775263057027,-1.38014833886309,1.38295725327239));
#71323=CARTESIAN_POINT('Ctrl Pts',(0.74653352768383,-1.36470857363931,1.38525554956542));
#71324=CARTESIAN_POINT('Ctrl Pts',(0.757659457834445,-1.35856318498824,
1.38615466879788));
#71325=CARTESIAN_POINT('Ctrl Pts',(0.779202002284005,-1.34631726724444,
1.38791722402732));
#71326=CARTESIAN_POINT('Ctrl Pts',(0.789625397322583,-1.34023045078361,
1.38878011861224));
#71327=CARTESIAN_POINT('Ctrl Pts',(0.814234697877007,-1.32547293614791,
1.39084211302042));
#71328=CARTESIAN_POINT('Ctrl Pts',(0.828354232074695,-1.31669505734386,
1.39204505832186));
#71329=CARTESIAN_POINT('Ctrl Pts',(0.877666280145273,-1.28493147432753,
1.39631882515552));
#71330=CARTESIAN_POINT('Ctrl Pts',(0.912062229832128,-1.26074932862043,
1.39943321547664));
#71331=CARTESIAN_POINT('Ctrl Pts',(0.999023160485334,-1.1941889227265,1.40766800360979));
#71332=CARTESIAN_POINT('Ctrl Pts',(1.04988087345275,-1.14973167300025,1.41285496363954));
#71333=CARTESIAN_POINT('Ctrl Pts',(1.16594204046471,-1.03413708914863,1.42554079724708));
#71334=CARTESIAN_POINT('Ctrl Pts',(1.22773952772954,-0.959957803233155,
1.43306005944108));
#71335=CARTESIAN_POINT('Ctrl Pts',(1.29089633946304,-0.867985343697893,
1.44137365188863));
#71336=CARTESIAN_POINT('Ctrl Pts',(1.29932816584917,-0.855311802421614,
1.44249856602405));
#71337=CARTESIAN_POINT('Ctrl Pts',(1.31192292172241,-0.835764916296272,
1.44419991867356));
#71338=CARTESIAN_POINT('Ctrl Pts',(1.31622061783963,-0.828980120800091,
1.44478439106641));
#71339=CARTESIAN_POINT('Ctrl Pts',(1.32400347370087,-0.816480160460945,
1.44584968199021));
#71340=CARTESIAN_POINT('Ctrl Pts',(1.32750444140163,-0.810775562005542,
1.44633146119466));
#71341=CARTESIAN_POINT('Ctrl Pts',(1.33556365660579,-0.797451436410707,
1.4474467674408));
#71342=CARTESIAN_POINT('Ctrl Pts',(1.34009364045356,-0.789815243676535,
1.44807849773311));
#71343=CARTESIAN_POINT('Ctrl Pts',(1.35476716712116,-0.764590349720044,
1.45014235520998));
#71344=CARTESIAN_POINT('Ctrl Pts',(1.36463223592371,-0.746840974847227,
1.45155823997507));
#71345=CARTESIAN_POINT('Ctrl Pts',(1.38812950264298,-0.702543263330322,
1.45501610980875));
#71346=CARTESIAN_POINT('Ctrl Pts',(1.40135103580084,-0.675785507508407,
1.45703927776334));
#71347=CARTESIAN_POINT('Ctrl Pts',(1.4629273713598,-0.541576485620519,1.46694761101303));
#71348=CARTESIAN_POINT('Ctrl Pts',(1.4997347762154,-0.429254379257706,1.47452560104263));
#71349=CARTESIAN_POINT('Ctrl Pts',(1.53316489514631,-0.266975749424769,
1.48564912598903));
#71350=CARTESIAN_POINT('Ctrl Pts',(1.54065188686204,-0.219685456308865,
1.48890634097348));
#71351=CARTESIAN_POINT('Ctrl Pts',(1.54792193181771,-0.154390672883636,
1.49347069055151));
#71352=CARTESIAN_POINT('Ctrl Pts',(1.5495914081969,-0.136620674365634,1.49471949700427));
#71353=CARTESIAN_POINT('Ctrl Pts',(1.55179975548467,-0.107796746571169,
1.4967578160672));
#71354=CARTESIAN_POINT('Ctrl Pts',(1.55252709828289,-0.0967585518690566,
1.49754139472352));
#71355=CARTESIAN_POINT('Ctrl Pts',(1.55380743017729,-0.0735588971693167,
1.49919508457876));
#71356=CARTESIAN_POINT('Ctrl Pts',(1.55433550093533,-0.0613968762544586,
1.50006591919336));
#71357=CARTESIAN_POINT('Ctrl Pts',(1.55526574173982,-0.0320192986339642,
1.5021795079022));
#71358=CARTESIAN_POINT('Ctrl Pts',(1.5555248772087,-0.0148011832395994,
1.5034266309181));
#71359=CARTESIAN_POINT('Ctrl Pts',(1.55542572861681,0.0490058399249677,
1.50808108886355));
#71360=CARTESIAN_POINT('Ctrl Pts',(1.55326033473315,0.095562957666692,1.51154312652778));
#71361=CARTESIAN_POINT('Ctrl Pts',(1.53766015553395,0.265799421837773,1.52444773895408));
#71362=CARTESIAN_POINT('Ctrl Pts',(1.5114973187938,0.387837244620299,1.53422214620163));
#71363=CARTESIAN_POINT('Ctrl Pts',(1.45802138765674,0.543481681710278,1.54682386148311));
#71364=CARTESIAN_POINT('Ctrl Pts',(1.44347687063239,0.581011059182153,1.54986871499844));
#71365=CARTESIAN_POINT('Ctrl Pts',(1.42287269650239,0.628608582388586,1.55370439541757));
#71366=CARTESIAN_POINT('Ctrl Pts',(1.41813366400091,0.639227966347026,1.55455842492058));
#71367=CARTESIAN_POINT('Ctrl Pts',(1.41027692292235,0.65631607193709,1.55592871710326));
#71368=CARTESIAN_POINT('Ctrl Pts',(1.40723284337583,0.662817860162931,1.55644915529748));
#71369=CARTESIAN_POINT('Ctrl Pts',(1.40112559332492,0.675630464633236,1.55747254949708));
#71370=CARTESIAN_POINT('Ctrl Pts',(1.39806455405764,0.681942050096462,1.55797560217759));
#71371=CARTESIAN_POINT('Ctrl Pts',(1.39015684955491,0.697969966190883,1.55925086584494));
#71372=CARTESIAN_POINT('Ctrl Pts',(1.38525083952554,0.707656886710863,1.56001952369793));
#71373=CARTESIAN_POINT('Ctrl Pts',(1.36387219920556,0.748794570914391,1.56327829901729));
#71374=CARTESIAN_POINT('Ctrl Pts',(1.34642553425715,0.779730354962053,1.56571513538569));
#71375=CARTESIAN_POINT('Ctrl Pts',(1.2903384129393,0.871675893619082,1.5729993716271));
#71376=CARTESIAN_POINT('Ctrl Pts',(1.24849551460942,0.930619386303604,1.57772995021185));
#71377=CARTESIAN_POINT('Ctrl Pts',(1.14528698412185,1.05645452911,1.58844445020901));
#71378=CARTESIAN_POINT('Ctrl Pts',(1.08187098220137,1.12130770439264,1.59442727919992));
#71379=CARTESIAN_POINT('Ctrl Pts',(0.994802021677467,1.19605008474157,1.60231797567165));
#71380=CARTESIAN_POINT('Ctrl Pts',(0.976059315127333,1.21139381350646,1.6039987673587));
#71381=CARTESIAN_POINT('Ctrl Pts',(0.946142661906033,1.23473998391124,1.60665969638051));
#71382=CARTESIAN_POINT('Ctrl Pts',(0.93520739655663,1.24304298735971,1.60762790182591));
#71383=CARTESIAN_POINT('Ctrl Pts',(0.914654227584452,1.25822401300077,1.60944043382414));
#71384=CARTESIAN_POINT('Ctrl Pts',(0.90506497447117,1.26513928116891,1.61028322786175));
#71385=CARTESIAN_POINT('Ctrl Pts',(0.883448598878422,1.28035634638747,1.61217731387228));
#71386=CARTESIAN_POINT('Ctrl Pts',(0.871381578612699,1.28859920766093,1.61323075527442));
#71387=CARTESIAN_POINT('Ctrl Pts',(0.834620903696914,1.31295758678308,1.61642937380675));
#71388=CARTESIAN_POINT('Ctrl Pts',(0.809584740152224,1.32854130837422,1.6185938419179));
#71389=CARTESIAN_POINT('Ctrl Pts',(0.721856723471828,1.37974670813473,1.62613579498519));
#71390=CARTESIAN_POINT('Ctrl Pts',(0.657147802997672,1.41171257530011,1.63163162669835));
#71391=CARTESIAN_POINT('Ctrl Pts',(0.506220749502165,1.47363919492169,1.64422774132595));
#71392=CARTESIAN_POINT('Ctrl Pts',(0.419103963830437,1.50074138114655,1.65134993321597));
#71393=CARTESIAN_POINT('Ctrl Pts',(0.302649773761244,1.52603186864642,1.66038410610987));
#71394=CARTESIAN_POINT('Ctrl Pts',(0.275026020676002,1.53125147590902,1.66249126283635));
#71395=CARTESIAN_POINT('Ctrl Pts',(0.237105395459742,1.53735726550729,1.66532237734685));
#71396=CARTESIAN_POINT('Ctrl Pts',(0.226920450895822,1.53889358134582,1.66607675158115));
#71397=CARTESIAN_POINT('Ctrl Pts',(0.209952695918003,1.54128090470716,1.66732269243146));
#71398=CARTESIAN_POINT('Ctrl Pts',(0.203178314171763,1.54218855579942,1.66781727121354));
#71399=CARTESIAN_POINT('Ctrl Pts',(0.189139504293926,1.54397539989931,1.66883600407346));
#71400=CARTESIAN_POINT('Ctrl Pts',(0.181874495306422,1.54484803829491,1.66935979824651));
#71401=CARTESIAN_POINT('Ctrl Pts',(0.162414179944644,1.54704633323502,1.67075443368066));
#71402=CARTESIAN_POINT('Ctrl Pts',(0.150208594530881,1.54827908530454,1.67162032234984));
#71403=CARTESIAN_POINT('Ctrl Pts',(0.0830005288571901,1.55426474608517,
1.676346061959));
#71404=CARTESIAN_POINT('Ctrl Pts',(0.0277833220635295,1.5562318355235,1.68007429016936));
#71405=CARTESIAN_POINT('Ctrl Pts',(-0.140239859767713,1.55326868444381,
1.69126299485227));
#71406=CARTESIAN_POINT('Ctrl Pts',(-0.252497950296415,1.53901135578109,
1.69854799371766));
#71407=CARTESIAN_POINT('Ctrl Pts',(-0.403246828051388,1.50291427434431,
1.70900208242791));
#71408=CARTESIAN_POINT('Ctrl Pts',(-0.443846497152932,1.49142854308859,
1.71188403980153));
#71409=CARTESIAN_POINT('Ctrl Pts',(-0.500171001422126,1.47299062280338,
1.71600733469374));
#71410=CARTESIAN_POINT('Ctrl Pts',(-0.516325999066684,1.46740581562399,
1.71720469678339));
#71411=CARTESIAN_POINT('Ctrl Pts',(-0.543688776177104,1.45743867457308,
1.71925976410873));
#71412=CARTESIAN_POINT('Ctrl Pts',(-0.554943963526747,1.45319033786993,
1.7201129769381));
#71413=CARTESIAN_POINT('Ctrl Pts',(-0.577831255460509,1.44424673080798,
1.72186478539408));
#71414=CARTESIAN_POINT('Ctrl Pts',(-0.589458076228139,1.43954046089804,
1.72276369793834));
#71415=CARTESIAN_POINT('Ctrl Pts',(-0.618673774303046,1.42730133312625,
1.72504595951518));
#71416=CARTESIAN_POINT('Ctrl Pts',(-0.63618247323713,1.41958378923593,1.72643546846558));
#71417=CARTESIAN_POINT('Ctrl Pts',(-0.71369947185705,1.38369352512946,1.73268812983505));
#71418=CARTESIAN_POINT('Ctrl Pts',(-0.772004757824122,1.35202852354838,
1.73766877120883));
#71419=CARTESIAN_POINT('Ctrl Pts',(-0.880427981112995,1.28384077901513,
1.74746702913104));
#71420=CARTESIAN_POINT('Ctrl Pts',(-0.930739652452833,1.24784757436664,
1.75226387614408));
#71421=CARTESIAN_POINT('Ctrl Pts',(-1.03802670040422,1.16098791015851,1.76296460702661));
#71422=CARTESIAN_POINT('Ctrl Pts',(-1.09367941760893,1.10872011016489,1.76885292769043));
#71423=CARTESIAN_POINT('Ctrl Pts',(-1.15405160970268,1.04303077528815,1.77547029210355));
#71424=CARTESIAN_POINT('Ctrl Pts',(-1.16270482748837,1.03337593814659,1.77642473732977));
#71425=CARTESIAN_POINT('Ctrl Pts',(-1.1761503154436,1.01799137467532,1.77791578627785));
#71426=CARTESIAN_POINT('Ctrl Pts',(-1.18102353109491,1.01233365482285,1.77845791677759));
#71427=CARTESIAN_POINT('Ctrl Pts',(-1.19028084987463,1.00142823014288,1.77949070877013));
#71428=CARTESIAN_POINT('Ctrl Pts',(-1.1946713437654,0.996186420375517,1.77998179122058));
#71429=CARTESIAN_POINT('Ctrl Pts',(-1.20536009966606,0.983252818872716,
1.78118087611187));
#71430=CARTESIAN_POINT('Ctrl Pts',(-1.21161960069142,0.975529103969746,
1.78188616563002));
#71431=CARTESIAN_POINT('Ctrl Pts',(-1.23465144262714,0.946545983429047,
1.78449521453369));
#71432=CARTESIAN_POINT('Ctrl Pts',(-1.25094289736705,0.92490841334122,1.78636882566694));
#71433=CARTESIAN_POINT('Ctrl Pts',(-1.29922754135232,0.85716736673855,1.79204924855407));
#71434=CARTESIAN_POINT('Ctrl Pts',(-1.32929980899916,0.80974756851155,1.79577248435407));
#71435=CARTESIAN_POINT('Ctrl Pts',(-1.40762443979197,0.670070649317171,
1.80633762550688));
#71436=CARTESIAN_POINT('Ctrl Pts',(-1.44926962485242,0.574470986770568,
1.81311762730602));
#71437=CARTESIAN_POINT('Ctrl Pts',(-1.49104929188769,0.444319804641668,
1.82242663502483));
#71438=CARTESIAN_POINT('Ctrl Pts',(-1.50005353975116,0.412900959941094,
1.82467756808877));
#71439=CARTESIAN_POINT('Ctrl Pts',(-1.51178196458939,0.366505143153333,
1.8280204900524));
#71440=CARTESIAN_POINT('Ctrl Pts',(-1.51528687048223,0.351733421468968,
1.82908755968414));
#71441=CARTESIAN_POINT('Ctrl Pts',(-1.52114564853001,0.325326047490414,
1.83100126535571));
#71442=CARTESIAN_POINT('Ctrl Pts',(-1.52358362316759,0.313710137203169,
1.8318451398117));
#71443=CARTESIAN_POINT('Ctrl Pts',(-1.52804418057769,0.291177733102495,
1.83348663208431));
#71444=CARTESIAN_POINT('Ctrl Pts',(-1.53008329414758,0.280265215790429,
1.83428366605995));
#71445=CARTESIAN_POINT('Ctrl Pts',(-1.53428158358357,0.256384650306407,
1.83603273479997));
#71446=CARTESIAN_POINT('Ctrl Pts',(-1.53639349389318,0.243409282611066,
1.83698620286335));
#71447=CARTESIAN_POINT('Ctrl Pts',(-1.54251818793367,0.202517377611905,
1.84000154654074));
#71448=CARTESIAN_POINT('Ctrl Pts',(-1.54593614980552,0.174518998350778,
1.84208156461047));
#71449=CARTESIAN_POINT('Ctrl Pts',(-1.55319495060664,0.097760279318961,
1.84782834642718));
#71450=CARTESIAN_POINT('Ctrl Pts',(-1.55550000000086,0.0488912887219831,
1.85153659513319));
#71451=CARTESIAN_POINT('Ctrl Pts',(-1.5555,-2.74013238336738E-11,1.8552873792152));
#71452=CARTESIAN_POINT('Origin',(0.,0.,-1.2940562256037));
#71453=CARTESIAN_POINT('',(-1.55549941625285,0.00134760418419674,2.6940562256037));
#71454=CARTESIAN_POINT('',(-1.55549999398642,0.000136778062909979,2.55740452554329));
#71455=CARTESIAN_POINT('',(-1.5555,-1.46451138874614E-13,-1.2940562256037));
#71456=CARTESIAN_POINT('Ctrl Pts',(-1.55549937946843,0.0013894147425314,
2.69460090097471));
#71457=CARTESIAN_POINT('Ctrl Pts',(-1.55538731803193,0.126846191331773,
2.68497053713314));
#71458=CARTESIAN_POINT('Ctrl Pts',(-1.54009868858362,0.251831453706691,
2.67506939719058));
#71459=CARTESIAN_POINT('Ctrl Pts',(-1.50718157259488,0.384860815458307,
2.66484140237633));
#71460=CARTESIAN_POINT('Ctrl Pts',(-1.50427686849575,0.396062195069036,
2.66398304455757));
#71461=CARTESIAN_POINT('Ctrl Pts',(-1.49865793622203,0.416776279059666,
2.66240231052651));
#71462=CARTESIAN_POINT('Ctrl Pts',(-1.49597745984636,0.426297466496353,
2.66167832884848));
#71463=CARTESIAN_POINT('Ctrl Pts',(-1.4913290659897,0.442224786329797,2.66047233255536));
#71464=CARTESIAN_POINT('Ctrl Pts',(-1.48941027402812,0.448644834414615,
2.65998761956497));
#71465=CARTESIAN_POINT('Ctrl Pts',(-1.48534986958436,0.46191725370731,2.65898871930838));
#71466=CARTESIAN_POINT('Ctrl Pts',(-1.48320221671903,0.468767505521267,
2.65847487960452));
#71467=CARTESIAN_POINT('Ctrl Pts',(-1.47728743102513,0.487185898851621,
2.65709732565416));
#71468=CARTESIAN_POINT('Ctrl Pts',(-1.47343179155847,0.498725409237205,
2.65623854810703));
#71469=CARTESIAN_POINT('Ctrl Pts',(-1.45249565967407,0.559021895269329,
2.65176788787174));
#71470=CARTESIAN_POINT('Ctrl Pts',(-1.43312755540957,0.606956138145253,
2.64827081138505));
#71471=CARTESIAN_POINT('Ctrl Pts',(-1.37077081508216,0.741561594571889,
2.63837505717821));
#71472=CARTESIAN_POINT('Ctrl Pts',(-1.32204520338672,0.825302114826695,
2.63211279749097));
#71473=CARTESIAN_POINT('Ctrl Pts',(-1.24282707217797,0.936232842896575,
2.62302467603076));
#71474=CARTESIAN_POINT('Ctrl Pts',(-1.21857117371497,0.967592380453974,
2.62035694460501));
#71475=CARTESIAN_POINT('Ctrl Pts',(-1.17996201399898,1.01375151310462,2.61624350410729));
#71476=CARTESIAN_POINT('Ctrl Pts',(-1.16646794206675,1.02924970792222,2.61482838873042));
#71477=CARTESIAN_POINT('Ctrl Pts',(-1.14102586457854,1.05732729653718,2.61219661074604));
#71478=CARTESIAN_POINT('Ctrl Pts',(-1.12916670423239,1.06998296603336,2.61098360781891));
#71479=CARTESIAN_POINT('Ctrl Pts',(-1.11651372554014,1.08304111539856,2.60970235692377));
#71480=CARTESIAN_POINT('Ctrl Pts',(-1.11592813564962,1.08364447722668,2.6096430881903));
#71481=CARTESIAN_POINT('Ctrl Pts',(-1.11473285812393,1.0848740336368,2.60952216973579));
#71482=CARTESIAN_POINT('Ctrl Pts',(-1.11412313145297,1.08550018968049,2.6094605183518));
#71483=CARTESIAN_POINT('Ctrl Pts',(-1.10522359663464,1.09462412942643,2.60856110380358));
#71484=CARTESIAN_POINT('Ctrl Pts',(-1.09683751380288,1.10302703384602,2.60771920656324));
#71485=CARTESIAN_POINT('Ctrl Pts',(-1.08066647767016,1.11886373624548,2.60610581458366));
#71486=CARTESIAN_POINT('Ctrl Pts',(-1.07289890360038,1.1263143558157,2.60533512678551));
#71487=CARTESIAN_POINT('Ctrl Pts',(-1.05447583125259,1.14362216721686,2.60351677129868));
#71488=CARTESIAN_POINT('Ctrl Pts',(-1.04375860196292,1.15341184937758,2.60246630520392));
#71489=CARTESIAN_POINT('Ctrl Pts',(-1.0051450586133,1.18770459469041,2.59870612107435));
#71490=CARTESIAN_POINT('Ctrl Pts',(-0.976512357557173,1.2113554314497,2.59596213449223));
#71491=CARTESIAN_POINT('Ctrl Pts',(-0.860393500237104,1.30047671650134,
2.5849970225351));
#71492=CARTESIAN_POINT('Ctrl Pts',(-0.766966199039916,1.35767201562551,
2.57649439843529));
#71493=CARTESIAN_POINT('Ctrl Pts',(-0.613813654634173,1.43054494715563,
2.56336739180946));
#71494=CARTESIAN_POINT('Ctrl Pts',(-0.557820602450821,1.45329408370597,
2.55872669280604));
#71495=CARTESIAN_POINT('Ctrl Pts',(-0.485967510277927,1.47771987787638,
2.55307005043627));
#71496=CARTESIAN_POINT('Ctrl Pts',(-0.47121904885204,1.48248882456758,2.55192442637811));
#71497=CARTESIAN_POINT('Ctrl Pts',(-0.448875447652583,1.48934651847286,
2.55021448773321));
#71498=CARTESIAN_POINT('Ctrl Pts',(-0.441332203420827,1.49159917975371,
2.54964157845548));
#71499=CARTESIAN_POINT('Ctrl Pts',(-0.427517687808653,1.49561067491995,
2.54860073702107));
#71500=CARTESIAN_POINT('Ctrl Pts',(-0.421252225197364,1.49738746828486,
2.54813184290923));
#71501=CARTESIAN_POINT('Ctrl Pts',(-0.406877505106342,1.50136655967539,
2.5470631672131));
#71502=CARTESIAN_POINT('Ctrl Pts',(-0.398761332315587,1.50354256976768,
2.54646487882233));
#71503=CARTESIAN_POINT('Ctrl Pts',(-0.372413409347209,1.51037829458614,
2.54453790590667));
#71504=CARTESIAN_POINT('Ctrl Pts',(-0.354113827462144,1.51477319078226,
2.54322315409331));
#71505=CARTESIAN_POINT('Ctrl Pts',(-0.238387588028007,1.54035443349811,
2.53503032226885));
#71506=CARTESIAN_POINT('Ctrl Pts',(-0.139181094682225,1.5524671141496,2.52853618842363));
#71507=CARTESIAN_POINT('Ctrl Pts',(0.0383606594663556,1.55697556753864,
2.51684006157532));
#71508=CARTESIAN_POINT('Ctrl Pts',(0.116239512612371,1.5531036858916,2.51168478884959));
#71509=CARTESIAN_POINT('Ctrl Pts',(0.22227982715778,1.53980954575471,2.50437740128042));
#71510=CARTESIAN_POINT('Ctrl Pts',(0.250955007850187,1.53539674339928,2.50237288563666));
#71511=CARTESIAN_POINT('Ctrl Pts',(0.293558426393745,1.52761522161944,2.4993427387498));
#71512=CARTESIAN_POINT('Ctrl Pts',(0.307591735686541,1.52485150586117,2.49833614767991));
#71513=CARTESIAN_POINT('Ctrl Pts',(0.332857657336027,1.51951268093812,2.49650746870956));
#71514=CARTESIAN_POINT('Ctrl Pts',(0.344103679479624,1.51700548854042,2.49568760669109));
#71515=CARTESIAN_POINT('Ctrl Pts',(0.368283005257328,1.5113322446563,2.49391158695646));
#71516=CARTESIAN_POINT('Ctrl Pts',(0.381205499332206,1.5081246210074,2.49295414789157));
#71517=CARTESIAN_POINT('Ctrl Pts',(0.416593994985894,1.49885659938431,2.49030861601903));
#71518=CARTESIAN_POINT('Ctrl Pts',(0.438966827899616,1.49245759657769,2.48860976148115));
#71519=CARTESIAN_POINT('Ctrl Pts',(0.568836187261001,1.45214011829659,2.4785880684266));
#71520=CARTESIAN_POINT('Ctrl Pts',(0.672515419378876,1.40712454988079,2.46990361764407));
#71521=CARTESIAN_POINT('Ctrl Pts',(0.820318677154777,1.32286015823109,2.45670735443873));
#71522=CARTESIAN_POINT('Ctrl Pts',(0.868622464217616,1.29165686114389,2.4522533726896));
#71523=CARTESIAN_POINT('Ctrl Pts',(0.940247678765377,1.23954925415527,2.4455221429992));
#71524=CARTESIAN_POINT('Ctrl Pts',(0.964851773310903,1.22049556795271,2.44318526346992));
#71525=CARTESIAN_POINT('Ctrl Pts',(0.996768367475079,1.19421010551509,2.44013720841082));
#71526=CARTESIAN_POINT('Ctrl Pts',(1.00460292111922,1.18762702078202,2.43938762772936));
#71527=CARTESIAN_POINT('Ctrl Pts',(1.01750929331096,1.17656316031375,2.43815128775061));
#71528=CARTESIAN_POINT('Ctrl Pts',(1.02261775867184,1.17212582879304,2.43766153525754));
#71529=CARTESIAN_POINT('Ctrl Pts',(1.03234963440209,1.16356043808607,2.43672802485861));
#71530=CARTESIAN_POINT('Ctrl Pts',(1.03697756388193,1.15943787946948,2.43628385628941));
#71531=CARTESIAN_POINT('Ctrl Pts',(1.04958323065644,1.14807289976351,2.43507293719761));
#71532=CARTESIAN_POINT('Ctrl Pts',(1.05751074295105,1.1407749063971,2.43431020806476));
#71533=CARTESIAN_POINT('Ctrl Pts',(1.08957021177264,1.11063982860917,2.43121750546881));
#71534=CARTESIAN_POINT('Ctrl Pts',(1.11304524561238,1.08711303032182,2.42893367217328));
#71535=CARTESIAN_POINT('Ctrl Pts',(1.19538539273192,0.999125225509335,2.42076826750388));
#71536=CARTESIAN_POINT('Ctrl Pts',(1.24955549341899,0.930489550683917,2.41508510310124));
#71537=CARTESIAN_POINT('Ctrl Pts',(1.32944070314122,0.809620069684692,2.40553136922015));
#71538=CARTESIAN_POINT('Ctrl Pts',(1.35850125887831,0.759849217181745,2.40171121374538));
#71539=CARTESIAN_POINT('Ctrl Pts',(1.40199781615542,0.674847099985842,2.39524236315461));
#71540=CARTESIAN_POINT('Ctrl Pts',(1.41802154801234,0.640492770933341,2.39264249811136));
#71541=CARTESIAN_POINT('Ctrl Pts',(1.43891974784693,0.591049408493478,2.38889948765799));
#71542=CARTESIAN_POINT('Ctrl Pts',(1.44484362646754,0.57641678224768,2.38779167058978));
#71543=CARTESIAN_POINT('Ctrl Pts',(1.4547667579778,0.550790982212269,2.3858500182355));
#71544=CARTESIAN_POINT('Ctrl Pts',(1.45886667721435,0.539837967078563,2.38501963012689));
#71545=CARTESIAN_POINT('Ctrl Pts',(1.46709905332136,0.517066108313143,2.38329165773792));
#71546=CARTESIAN_POINT('Ctrl Pts',(1.47121308585006,0.505241557717529,2.38239353038934));
#71547=CARTESIAN_POINT('Ctrl Pts',(1.48155184089338,0.474328456558938,2.38004263559217));
#71548=CARTESIAN_POINT('Ctrl Pts',(1.48755032635559,0.455167330100504,2.37858257724474));
#71549=CARTESIAN_POINT('Ctrl Pts',(1.51704220779918,0.354141989310401,2.37086582298681));
#71550=CARTESIAN_POINT('Ctrl Pts',(1.5341498494065,0.270579713124991,2.36440730304874));
#71551=CARTESIAN_POINT('Ctrl Pts',(1.55427327142607,0.103542958193033,2.35142699245007));
#71552=CARTESIAN_POINT('Ctrl Pts',(1.5575852321844,0.0203718502983426,2.34493238733094));
#71553=CARTESIAN_POINT('Ctrl Pts',(1.55320140247792,-0.0883552993543667,
2.33661633755969));
#71554=CARTESIAN_POINT('Ctrl Pts',(1.55152881887798,-0.114016377704457,
2.33466721279431));
#71555=CARTESIAN_POINT('Ctrl Pts',(1.54759139744469,-0.157704170990874,
2.33138372148261));
#71556=CARTESIAN_POINT('Ctrl Pts',(1.54564562241275,-0.175753873677335,
2.33003736834424));
#71557=CARTESIAN_POINT('Ctrl Pts',(1.54234111524195,-0.202074870726715,
2.32809283802791));
#71558=CARTESIAN_POINT('Ctrl Pts',(1.54123090756904,-0.210375063372572,
2.32748238390657));
#71559=CARTESIAN_POINT('Ctrl Pts',(1.53913951238114,-0.225104645774646,
2.3264044191252));
#71560=CARTESIAN_POINT('Ctrl Pts',(1.53818497186468,-0.231537334833427,
2.32593550320462));
#71561=CARTESIAN_POINT('Ctrl Pts',(1.53596437888963,-0.245881814914582,
2.32489398764974));
#71562=CARTESIAN_POINT('Ctrl Pts',(1.53467751366932,-0.253790024817268,
2.32432254654461));
#71563=CARTESIAN_POINT('Ctrl Pts',(1.53060192905334,-0.277670410362816,
2.32260432535035));
#71564=CARTESIAN_POINT('Ctrl Pts',(1.52762443960365,-0.293609856442446,
2.32146743871919));
#71565=CARTESIAN_POINT('Ctrl Pts',(1.50974770917352,-0.381658959976725,
2.31522789121622));
#71566=CARTESIAN_POINT('Ctrl Pts',(1.48999037025805,-0.452695366466934,
2.31034289757394));
#71567=CARTESIAN_POINT('Ctrl Pts',(1.44282686400929,-0.585066636100503,
2.30107826171337));
#71568=CARTESIAN_POINT('Ctrl Pts',(1.41634372454438,-0.646546594597441,
2.29670279499597));
#71569=CARTESIAN_POINT('Ctrl Pts',(1.36776434477102,-0.74189776665953,2.28957135770917));
#71570=CARTESIAN_POINT('Ctrl Pts',(1.34816522475285,-0.776943864119547,
2.28687072576075));
#71571=CARTESIAN_POINT('Ctrl Pts',(1.31182505428172,-0.836401996948736,
2.28210893498225));
#71572=CARTESIAN_POINT('Ctrl Pts',(1.2957020762172,-0.861167353290425,2.28006820415153));
#71573=CARTESIAN_POINT('Ctrl Pts',(1.27068671733997,-0.897297560800229,
2.27699426400264));
#71574=CARTESIAN_POINT('Ctrl Pts',(1.26232512224383,-0.909023051010533,
2.27598094388079));
#71575=CARTESIAN_POINT('Ctrl Pts',(1.24697875331156,-0.929923197739378,
2.27414510532413));
#71576=CARTESIAN_POINT('Ctrl Pts',(1.24005240429697,-0.939139598993209,
2.27332489330736));
#71577=CARTESIAN_POINT('Ctrl Pts',(1.22495124452529,-0.958775296530983,
2.27155380197568));
#71578=CARTESIAN_POINT('Ctrl Pts',(1.21674458903061,-0.969168822037419,
2.27060170324061));
#71579=CARTESIAN_POINT('Ctrl Pts',(1.1939648351247,-0.997273404188338,2.26798602442701));
#71580=CARTESIAN_POINT('Ctrl Pts',(1.17913166831744,-1.01476828632398,2.26631207982835));
#71581=CARTESIAN_POINT('Ctrl Pts',(1.07392893634551,-1.13342708539449,2.25463055130822));
#71582=CARTESIAN_POINT('Ctrl Pts',(0.971063849893259,-1.22270215999018,
2.24407412871352));
#71583=CARTESIAN_POINT('Ctrl Pts',(0.82277362573525,-1.32075866088322,2.23032683404809));
#71584=CARTESIAN_POINT('Ctrl Pts',(0.78665092684456,-1.34258729850469,2.2270835643428));
#71585=CARTESIAN_POINT('Ctrl Pts',(0.727219688405929,-1.37527781461728,
2.22195719271888));
#71586=CARTESIAN_POINT('Ctrl Pts',(0.704452290761252,-1.38707775785196,
2.22004053039881));
#71587=CARTESIAN_POINT('Ctrl Pts',(0.672815076671022,-1.40249469406085,
2.21745098099835));
#71588=CARTESIAN_POINT('Ctrl Pts',(0.66418952089079,-1.40660008070629,2.21675234546226));
#71589=CARTESIAN_POINT('Ctrl Pts',(0.649504677449499,-1.41342421650912,
2.21557604913213));
#71590=CARTESIAN_POINT('Ctrl Pts',(0.643464902652125,-1.41618405163887,
2.21509597902856));
#71591=CARTESIAN_POINT('Ctrl Pts',(0.630742594695907,-1.42189922704868,
2.2140927826862));
#71592=CARTESIAN_POINT('Ctrl Pts',(0.624056657428621,-1.42484628181611,
2.21357014255493));
#71593=CARTESIAN_POINT('Ctrl Pts',(0.605638667570506,-1.43281012471862,
2.21214224019816));
#71594=CARTESIAN_POINT('Ctrl Pts',(0.593864950902522,-1.43772998056109,
2.2112425505208));
#71595=CARTESIAN_POINT('Ctrl Pts',(0.51161977071174,-1.4709148229566,2.20503926334067));
#71596=CARTESIAN_POINT('Ctrl Pts',(0.439212034146059,-1.49413560587586,
2.19998833393911));
#71597=CARTESIAN_POINT('Ctrl Pts',(0.306755854313112,-1.52614536433074,
2.19099654745206));
#71598=CARTESIAN_POINT('Ctrl Pts',(0.247349219848664,-1.53689202634323,
2.18704907088973));
#71599=CARTESIAN_POINT('Ctrl Pts',(0.142001991818524,-1.54968171085334,
2.18000869855851));
#71600=CARTESIAN_POINT('Ctrl Pts',(0.0963163463532044,-1.55319047515296,
2.17694287312981));
#71601=CARTESIAN_POINT('Ctrl Pts',(0.018107810677906,-1.55573314981053,
2.17161280567155));
#71602=CARTESIAN_POINT('Ctrl Pts',(-0.0143522159617565,-1.55577224857403,
2.16937682813084));
#71603=CARTESIAN_POINT('Ctrl Pts',(-0.0616951794880102,-1.55434757484017,
2.16606775977228));
#71604=CARTESIAN_POINT('Ctrl Pts',(-0.0765947715009059,-1.55368461800005,
2.16501944782693));
#71605=CARTESIAN_POINT('Ctrl Pts',(-0.103039274247553,-1.5521266669576,
2.16314541829147));
#71606=CARTESIAN_POINT('Ctrl Pts',(-0.114588211648479,-1.55131679898818,
2.16232242594881));
#71607=CARTESIAN_POINT('Ctrl Pts',(-0.139005380404212,-1.54933040728745,
2.16057223416413));
#71608=CARTESIAN_POINT('Ctrl Pts',(-0.151870079932455,-1.54812230357828,
2.15964410172136));
#71609=CARTESIAN_POINT('Ctrl Pts',(-0.186598870437028,-1.54442394400177,
2.15712156247851));
#71610=CARTESIAN_POINT('Ctrl Pts',(-0.208426849186091,-1.54162985625917,
2.15551776871427));
#71611=CARTESIAN_POINT('Ctrl Pts',(-0.354420788616174,-1.51978475107023,
2.14466217164243));
#71612=CARTESIAN_POINT('Ctrl Pts',(-0.475922905125124,-1.4862182913149,
2.13494408974712));
#71613=CARTESIAN_POINT('Ctrl Pts',(-0.654598557060875,-1.41267745780737,
2.11996763470592));
#71614=CARTESIAN_POINT('Ctrl Pts',(-0.715417583243432,-1.38287250046008,
2.11474723840267));
#71615=CARTESIAN_POINT('Ctrl Pts',(-0.788232551768143,-1.34109466083933,
2.10848170970822));
#71616=CARTESIAN_POINT('Ctrl Pts',(-0.802230172532691,-1.33276864117463,
2.10727669009433));
#71617=CARTESIAN_POINT('Ctrl Pts',(-0.822927552905985,-1.32001322114888,
2.10549688802283));
#71618=CARTESIAN_POINT('Ctrl Pts',(-0.829727455348345,-1.31574960338492,
2.10491248018596));
#71619=CARTESIAN_POINT('Ctrl Pts',(-0.841428013752229,-1.30828643393038,
2.10390786565032));
#71620=CARTESIAN_POINT('Ctrl Pts',(-0.846343925988586,-1.30511166481538,
2.10348611136737));
#71621=CARTESIAN_POINT('Ctrl Pts',(-0.85794516680684,-1.29752629284738,
2.10249153910797));
#71622=CARTESIAN_POINT('Ctrl Pts',(-0.864614499983425,-1.2930917074296,
2.10192031521566));
#71623=CARTESIAN_POINT('Ctrl Pts',(-0.884667456810305,-1.27953354259813,
2.10020344563143));
#71624=CARTESIAN_POINT('Ctrl Pts',(-0.897943611344265,-1.27025191231025,
2.09906767057882));
#71625=CARTESIAN_POINT('Ctrl Pts',(-0.969382346623749,-1.2186277392443,
2.09294642539172));
#71626=CARTESIAN_POINT('Ctrl Pts',(-1.02470574589138,-1.17249152587738,
2.08816833050163));
#71627=CARTESIAN_POINT('Ctrl Pts',(-1.12190979149695,-1.07927402318772,
2.07928552843029));
#71628=CARTESIAN_POINT('Ctrl Pts',(-1.16450997141931,-1.03316521502718,
2.07518124081249));
#71629=CARTESIAN_POINT('Ctrl Pts',(-1.24533709583144,-0.934311137469707,
2.06669487242445));
#71630=CARTESIAN_POINT('Ctrl Pts',(-1.28326786800508,-0.88148953936091,
2.06231608436082));
#71631=CARTESIAN_POINT('Ctrl Pts',(-1.32774473711978,-0.810571234795339,
2.0565111089062));
#71632=CARTESIAN_POINT('Ctrl Pts',(-1.33741843583963,-0.794508456979942,
2.05520118404223));
#71633=CARTESIAN_POINT('Ctrl Pts',(-1.352926216453,-0.767672369896671,2.05301826887636));
#71634=CARTESIAN_POINT('Ctrl Pts',(-1.35892776707444,-0.756997703453047,
2.05215139546252));
#71635=CARTESIAN_POINT('Ctrl Pts',(-1.37041631025434,-0.735986624449652,
2.05044725806438));
#71636=CARTESIAN_POINT('Ctrl Pts',(-1.37591393992763,-0.725656937446091,
2.04961044549914));
#71637=CARTESIAN_POINT('Ctrl Pts',(-1.38889634092822,-0.700585836960875,
2.04758124882784));
#71638=CARTESIAN_POINT('Ctrl Pts',(-1.39626350263485,-0.685785500525342,
2.04638483559864));
#71639=CARTESIAN_POINT('Ctrl Pts',(-1.42071587397855,-0.634633660818418,
2.0422533391069));
#71640=CARTESIAN_POINT('Ctrl Pts',(-1.43662701924741,-0.597742209261008,
2.03927903598984));
#71641=CARTESIAN_POINT('Ctrl Pts',(-1.49703788902239,-0.441281493234144,
2.02668054718635));
#71642=CARTESIAN_POINT('Ctrl Pts',(-1.52816783187321,-0.317091084462268,
2.01666570016941));
#71643=CARTESIAN_POINT('Ctrl Pts',(-1.54931440220941,-0.145742777560349,
2.00341007027543));
#71644=CARTESIAN_POINT('Ctrl Pts',(-1.55289043748145,-0.100738299445941,
1.9999858901203));
#71645=CARTESIAN_POINT('Ctrl Pts',(-1.55491545829476,-0.0441597243189167,
1.99579942571185));
#71646=CARTESIAN_POINT('Ctrl Pts',(-1.55519914969052,-0.0326770470229673,
1.99495590995198));
#71647=CARTESIAN_POINT('Ctrl Pts',(-1.55545143281546,-0.0141609537247806,
1.9936066933907));
#71648=CARTESIAN_POINT('Ctrl Pts',(-1.55549955660677,-0.00712931545088431,
1.99309686784853));
#71649=CARTESIAN_POINT('Ctrl Pts',(-1.55549999695016,-9.74065733091837E-5,
1.99258973177283));
#71650=CARTESIAN_POINT('',(-1.55549938663868,-0.00138136406952889,1.85539336356033));
#71651=CARTESIAN_POINT('Ctrl Pts',(-1.5555,-2.74013238336738E-11,1.8552873792152));
#71652=CARTESIAN_POINT('Ctrl Pts',(-1.55549999999999,-0.000460452766239691,
1.85532270368398));
#71653=CARTESIAN_POINT('Ctrl Pts',(-1.55549979554798,-0.000920907491934938,
1.85535803180706));
#71654=CARTESIAN_POINT('Ctrl Pts',(-1.55549938663868,-0.00138136406952337,
1.85539336356033));
#71655=CARTESIAN_POINT('Ctrl Pts',(-1.55549938786299,-0.00137998473721819,
1.85539325772142));
#71656=CARTESIAN_POINT('Ctrl Pts',(-1.55538895339302,-0.125860166144892,
1.86494486888977));
#71657=CARTESIAN_POINT('Ctrl Pts',(-1.54033730079042,-0.249879935971551,
1.87476439976426));
#71658=CARTESIAN_POINT('Ctrl Pts',(-1.50776464436006,-0.382588199128195,
1.88497621214416));
#71659=CARTESIAN_POINT('Ctrl Pts',(-1.50472931714602,-0.394357270960365,
1.88587878350894));
#71660=CARTESIAN_POINT('Ctrl Pts',(-1.49886077654995,-0.416056756393507,
1.88753581801422));
#71661=CARTESIAN_POINT('Ctrl Pts',(-1.49606603794035,-0.425996804714526,
1.88829208838697));
#71662=CARTESIAN_POINT('Ctrl Pts',(-1.49123663290028,-0.442539570210456,
1.8895452384819));
#71663=CARTESIAN_POINT('Ctrl Pts',(-1.48925661774329,-0.4491577680103,1.89004510407235));
#71664=CARTESIAN_POINT('Ctrl Pts',(-1.48508452641398,-0.462772019206191,
1.89107004065383));
#71665=CARTESIAN_POINT('Ctrl Pts',(-1.48288697859833,-0.469766119442804,
1.89159479668266));
#71666=CARTESIAN_POINT('Ctrl Pts',(-1.47686050901928,-0.488482706249938,
1.89299492924222));
#71667=CARTESIAN_POINT('Ctrl Pts',(-1.4729414056685,-0.500175927131773,
1.89386528496247));
#71668=CARTESIAN_POINT('Ctrl Pts',(-1.45207732788873,-0.560053994973987,
1.89830561736203));
#71669=CARTESIAN_POINT('Ctrl Pts',(-1.43290375404118,-0.607434815703687,
1.90176420414499));
#71670=CARTESIAN_POINT('Ctrl Pts',(-1.36879750231898,-0.745830041297932,
1.91194243722714));
#71671=CARTESIAN_POINT('Ctrl Pts',(-1.3172636407411,-0.833478532759328,
1.91850581248235));
#71672=CARTESIAN_POINT('Ctrl Pts',(-1.23576813988254,-0.945425090500928,
1.92776092931786));
#71673=CARTESIAN_POINT('Ctrl Pts',(-1.21291318763459,-0.974573138543642,
1.93025970686544));
#71674=CARTESIAN_POINT('Ctrl Pts',(-1.17117840361002,-1.02405518021531,
1.93469146115071));
#71675=CARTESIAN_POINT('Ctrl Pts',(-1.15275397548987,-1.04475163413647,
1.93660760361265));
#71676=CARTESIAN_POINT('Ctrl Pts',(-1.1243214114316,-1.0750222291773,1.93951409624123));
#71677=CARTESIAN_POINT('Ctrl Pts',(-1.11472149983761,-1.08497344915393,
1.94048726209598));
#71678=CARTESIAN_POINT('Ctrl Pts',(-1.09666547333496,-1.1031976240658,1.94230365227641));
#71679=CARTESIAN_POINT('Ctrl Pts',(-1.08824511798946,-1.11150470408145,
1.9431452721247));
#71680=CARTESIAN_POINT('Ctrl Pts',(-1.0698992049,-1.12919550631676,1.94496793051884));
#71681=CARTESIAN_POINT('Ctrl Pts',(-1.05994321362271,-1.13854607370604,
1.94595030674817));
#71682=CARTESIAN_POINT('Ctrl Pts',(-1.03224187762911,-1.16388462787798,
1.9486662123565));
#71683=CARTESIAN_POINT('Ctrl Pts',(-1.01425009016321,-1.17959626926235,
1.95041105639542));
#71684=CARTESIAN_POINT('Ctrl Pts',(-0.913570936574439,-1.26350952510231,
1.96007754882727));
#71685=CARTESIAN_POINT('Ctrl Pts',(-0.824379246614064,-1.32342707469424,
1.96831981862014));
#71686=CARTESIAN_POINT('Ctrl Pts',(-0.653479893284431,-1.41421513709615,
1.98332565504959));
#71687=CARTESIAN_POINT('Ctrl Pts',(-0.573952423149791,-1.4483169776219,
1.99003197518426));
#71688=CARTESIAN_POINT('Ctrl Pts',(-0.479021574910063,-1.479968135154,1.99746477994711));
#71689=CARTESIAN_POINT('Ctrl Pts',(-0.465988253622172,-1.48412342205631,
1.99847300502116));
#71690=CARTESIAN_POINT('Ctrl Pts',(-0.445612709828477,-1.49032466462937,
2.0000284568485));
#71691=CARTESIAN_POINT('Ctrl Pts',(-0.438307779542034,-1.49248939365378,
2.0005819916172));
#71692=CARTESIAN_POINT('Ctrl Pts',(-0.424473033983126,-1.49647881841761,
2.00162218217989));
#71693=CARTESIAN_POINT('Ctrl Pts',(-0.417947040954146,-1.49831454758053,
2.00210939938525));
#71694=CARTESIAN_POINT('Ctrl Pts',(-0.402163576260625,-1.50264320880102,
2.00327980011711));
#71695=CARTESIAN_POINT('Ctrl Pts',(-0.392894698115519,-1.50509332722969,
2.00396056830364));
#71696=CARTESIAN_POINT('Ctrl Pts',(-0.361161071179086,-1.51316859786325,
2.00627086512746));
#71697=CARTESIAN_POINT('Ctrl Pts',(-0.338592439014884,-1.5183780257571,
2.00787911439485));
#71698=CARTESIAN_POINT('Ctrl Pts',(-0.222722533241381,-1.54241151626245,
2.01599881315053));
#71699=CARTESIAN_POINT('Ctrl Pts',(-0.127943171529968,-1.55314940330456,
2.02219851355788));
#71700=CARTESIAN_POINT('Ctrl Pts',(0.0275662866768698,-1.55642610834329,
2.03244837243229));
#71701=CARTESIAN_POINT('Ctrl Pts',(0.0879203693184907,-1.55418511138195,
2.03644357891812));
#71702=CARTESIAN_POINT('Ctrl Pts',(0.174732533722277,-1.54588828315864,
2.04234449835434));
#71703=CARTESIAN_POINT('Ctrl Pts',(0.201404849295889,-1.54263994447678,
2.04417835725252));
#71704=CARTESIAN_POINT('Ctrl Pts',(0.249740767191859,-1.53547835907496,
2.04755026612022));
#71705=CARTESIAN_POINT('Ctrl Pts',(0.271431167863581,-1.53179283181913,
2.04908133579775));
#71706=CARTESIAN_POINT('Ctrl Pts',(0.305934563681394,-1.52517435345614,
2.0515495651768));
#71707=CARTESIAN_POINT('Ctrl Pts',(0.318801687986122,-1.52253677474816,
2.05247734732059));
#71708=CARTESIAN_POINT('Ctrl Pts',(0.34327365389699,-1.51719655721571,2.0542566899509));
#71709=CARTESIAN_POINT('Ctrl Pts',(0.354883911083687,-1.51452289180877,
2.05510726542497));
#71710=CARTESIAN_POINT('Ctrl Pts',(0.381341200355258,-1.5081092596013,2.05706078451662));
#71711=CARTESIAN_POINT('Ctrl Pts',(0.396165804548793,-1.50428297675511,
2.05816643444416));
#71712=CARTESIAN_POINT('Ctrl Pts',(0.444134347228622,-1.49114389166325,
2.06178134930234));
#71713=CARTESIAN_POINT('Ctrl Pts',(0.477023974661305,-1.48095010332295,
2.06431850993454));
#71714=CARTESIAN_POINT('Ctrl Pts',(0.637074778030712,-1.42545940099006,
2.07696415963508));
#71715=CARTESIAN_POINT('Ctrl Pts',(0.758294454130408,-1.36483596205011,
2.08755599361962));
#71716=CARTESIAN_POINT('Ctrl Pts',(0.895957060259923,-1.2719320463403,2.10031308382366));
#71717=CARTESIAN_POINT('Ctrl Pts',(0.921244745709634,-1.2537378289102,2.10268701357591));
#71718=CARTESIAN_POINT('Ctrl Pts',(0.962585255199995,-1.22206707633824,
2.10660037029232));
#71719=CARTESIAN_POINT('Ctrl Pts',(0.978942463008052,-1.20900375424844,
2.10815768705266));
#71720=CARTESIAN_POINT('Ctrl Pts',(1.00193667335043,-1.18986715515646,2.11035417749409));
#71721=CARTESIAN_POINT('Ctrl Pts',(1.00879165204961,-1.1840609602348,2.11100994111039));
#71722=CARTESIAN_POINT('Ctrl Pts',(1.02067296297553,-1.17381935464664,2.11214763870729));
#71723=CARTESIAN_POINT('Ctrl Pts',(1.02572148103765,-1.16941037475094,2.11263138761461));
#71724=CARTESIAN_POINT('Ctrl Pts',(1.03670203881312,-1.15969499015047,2.11368417373872));
#71725=CARTESIAN_POINT('Ctrl Pts',(1.04262204078994,-1.15437553462164,2.11425224329532));
#71726=CARTESIAN_POINT('Ctrl Pts',(1.05949151441324,-1.13898171646649,2.11587328420474));
#71727=CARTESIAN_POINT('Ctrl Pts',(1.07033797298595,-1.12879505917099,2.11691835845458));
#71728=CARTESIAN_POINT('Ctrl Pts',(1.15329314593588,-1.04861506785732,2.12494931511784));
#71729=CARTESIAN_POINT('Ctrl Pts',(1.21862217906004,-0.971928217588851,
2.13151123968312));
#71730=CARTESIAN_POINT('Ctrl Pts',(1.31333186829491,-0.836049552033223,
2.14241586659887));
#71731=CARTESIAN_POINT('Ctrl Pts',(1.34717019026984,-0.780353175971586,
2.14671284302865));
#71732=CARTESIAN_POINT('Ctrl Pts',(1.39652400543303,-0.686288624063325,
2.15388834069765));
#71733=CARTESIAN_POINT('Ctrl Pts',(1.41417726793712,-0.649132921379771,
2.1567026166598));
#71734=CARTESIAN_POINT('Ctrl Pts',(1.4368208200654,-0.596152986482158,2.16071586962058));
#71735=CARTESIAN_POINT('Ctrl Pts',(1.44306287758538,-0.580880320742302,
2.1618727409201));
#71736=CARTESIAN_POINT('Ctrl Pts',(1.45344132644151,-0.554286706428067,
2.16388870521874));
#71737=CARTESIAN_POINT('Ctrl Pts',(1.45769133138501,-0.543011427032976,
2.16474391518476));
#71738=CARTESIAN_POINT('Ctrl Pts',(1.46616875584323,-0.519703814812717,
2.16651333373831));
#71739=CARTESIAN_POINT('Ctrl Pts',(1.47038003700313,-0.507666627421351,
2.16742800329111));
#71740=CARTESIAN_POINT('Ctrl Pts',(1.48086483408395,-0.476472363747926,
2.16980127808126));
#71741=CARTESIAN_POINT('Ctrl Pts',(1.48691463419079,-0.457243228543902,
2.17126707616361));
#71742=CARTESIAN_POINT('Ctrl Pts',(1.5144007327763,-0.363557037144884,2.17842570562278));
#71743=CARTESIAN_POINT('Ctrl Pts',(1.5306240803864,-0.287697408101522,2.18428207894123));
#71744=CARTESIAN_POINT('Ctrl Pts',(1.55652738760939,-0.098461874207653,
2.1989765761342));
#71745=CARTESIAN_POINT('Ctrl Pts',(1.55956301776891,0.0153796263588531,
2.20790529566261));
#71746=CARTESIAN_POINT('Ctrl Pts',(1.54852402745033,0.148509800108015,2.21793150997985));
#71747=CARTESIAN_POINT('Ctrl Pts',(1.54648220304895,0.168447969809931,2.21942108444098));
#71748=CARTESIAN_POINT('Ctrl Pts',(1.5429859294184,0.197110892601732,2.22154013866877));
#71749=CARTESIAN_POINT('Ctrl Pts',(1.54184163492863,0.205870505797548,2.22218471586751));
#71750=CARTESIAN_POINT('Ctrl Pts',(1.53969971545498,0.221245993681795,2.2233102594707));
#71751=CARTESIAN_POINT('Ctrl Pts',(1.53873395162544,0.227865828319695,2.22379290989689));
#71752=CARTESIAN_POINT('Ctrl Pts',(1.53650984271501,0.242451610065509,2.22485200281617));
#71753=CARTESIAN_POINT('Ctrl Pts',(1.53523222850838,0.25041424125383,2.22542737811352));
#71754=CARTESIAN_POINT('Ctrl Pts',(1.53133861678548,0.273530146183861,2.22709052510622));
#71755=CARTESIAN_POINT('Ctrl Pts',(1.52855969292173,0.288655524553191,2.22816975820267));
#71756=CARTESIAN_POINT('Ctrl Pts',(1.50277060528302,0.418184017971041,2.23735396464956));
#71757=CARTESIAN_POINT('Ctrl Pts',(1.46717508273175,0.529719477436725,2.24489309309676));
#71758=CARTESIAN_POINT('Ctrl Pts',(1.38872008483013,0.704751246615246,2.25755873807192));
#71759=CARTESIAN_POINT('Ctrl Pts',(1.35309220528608,0.770945742191927,2.26256493559077));
#71760=CARTESIAN_POINT('Ctrl Pts',(1.30028940479976,0.85403405388403,2.26934507074808));
#71761=CARTESIAN_POINT('Ctrl Pts',(1.28730879893311,0.873477337068966,2.2709694313602));
#71762=CARTESIAN_POINT('Ctrl Pts',(1.26619530931275,0.903609290306081,2.2735518475855));
#71763=CARTESIAN_POINT('Ctrl Pts',(1.25835337942552,0.914498257607495,2.274498897505));
#71764=CARTESIAN_POINT('Ctrl Pts',(1.2433186903096,0.93481520745987,2.27629306513166));
#71765=CARTESIAN_POINT('Ctrl Pts',(1.23615704743023,0.944265099195209,2.27713892953889));
#71766=CARTESIAN_POINT('Ctrl Pts',(1.219654736508,0.965530636501451,2.27906899082795));
#71767=CARTESIAN_POINT('Ctrl Pts',(1.21024920931724,0.977294176806536,2.28015570944413));
#71768=CARTESIAN_POINT('Ctrl Pts',(1.18034183258107,1.01360557567902,2.2835715894737));
#71769=CARTESIAN_POINT('Ctrl Pts',(1.15925397644534,1.03765748019393,2.28592413217753));
#71770=CARTESIAN_POINT('Ctrl Pts',(1.05174425678653,1.15290845025216,2.29765932807919));
#71771=CARTESIAN_POINT('Ctrl Pts',(0.955242908549995,1.23404411774343,2.30746298039647));
#71772=CARTESIAN_POINT('Ctrl Pts',(0.817293234500351,1.32406311370377,2.3201816895712));
#71773=CARTESIAN_POINT('Ctrl Pts',(0.783726272767845,1.34420418108044,2.32318362421356));
#71774=CARTESIAN_POINT('Ctrl Pts',(0.734635837831378,1.37119495302055,2.32741201073855));
#71775=CARTESIAN_POINT('Ctrl Pts',(0.71970601770741,1.37908981385141,2.32867732168767));
#71776=CARTESIAN_POINT('Ctrl Pts',(0.692787766165383,1.39276789278243,2.33091839535678));
#71777=CARTESIAN_POINT('Ctrl Pts',(0.680848228462122,1.39864327599412,2.33189855421603));
#71778=CARTESIAN_POINT('Ctrl Pts',(0.662027113144578,1.40760690485269,2.3334204260006));
#71779=CARTESIAN_POINT('Ctrl Pts',(0.655196305437748,1.41079938506277,2.33396803417576));
#71780=CARTESIAN_POINT('Ctrl Pts',(0.642154512448631,1.41677950725701,2.33500422071643));
#71781=CARTESIAN_POINT('Ctrl Pts',(0.635948295355103,1.41957611900225,2.3354932803866));
#71782=CARTESIAN_POINT('Ctrl Pts',(0.620796744562882,1.42628431986702,2.33667785229888));
#71783=CARTESIAN_POINT('Ctrl Pts',(0.61183257624404,1.43015260406258,2.33737079449766));
#71784=CARTESIAN_POINT('Ctrl Pts',(0.58037540697374,1.44337731709365,2.33977705460789));
#71785=CARTESIAN_POINT('Ctrl Pts',(0.557698272922248,1.45229008614372,2.3414666131695));
#71786=CARTESIAN_POINT('Ctrl Pts',(0.446402948902243,1.49304059043542,2.34958533411337));
#71787=CARTESIAN_POINT('Ctrl Pts',(0.355220357095774,1.51732263070553,2.35571844497338));
#71788=CARTESIAN_POINT('Ctrl Pts',(0.203285018399969,1.54332484730588,2.36587707175755));
#71789=CARTESIAN_POINT('Ctrl Pts',(0.143644426684709,1.55001351257482,2.3698481304727));
#71790=CARTESIAN_POINT('Ctrl Pts',(0.0447726383139681,1.55534590614523,
2.37654898994093));
#71791=CARTESIAN_POINT('Ctrl Pts',(0.00571275325077085,1.55597957098679,
2.37922572645748));
#71792=CARTESIAN_POINT('Ctrl Pts',(-0.0495231557783744,1.55479585136106,
2.38307644808628));
#71793=CARTESIAN_POINT('Ctrl Pts',(-0.065712232184456,1.554195788892,2.3842129480116));
#71794=CARTESIAN_POINT('Ctrl Pts',(-0.093874162099351,1.55271116049058,
2.38620524099852));
#71795=CARTESIAN_POINT('Ctrl Pts',(-0.105851831056515,1.55194061787074,
2.38705740960886));
#71796=CARTESIAN_POINT('Ctrl Pts',(-0.130642781109732,1.55005745371851,
2.38883178575243));
#71797=CARTESIAN_POINT('Ctrl Pts',(-0.143453535061102,1.54892437225602,
2.38975457168524));
#71798=CARTESIAN_POINT('Ctrl Pts',(-0.176824166531395,1.54555528559057,
2.39217440274962));
#71799=CARTESIAN_POINT('Ctrl Pts',(-0.197355473352966,1.54306793998091,
2.39367918954526));
#71800=CARTESIAN_POINT('Ctrl Pts',(-0.308233837236498,1.52738614960515,
2.40189653002818));
#71801=CARTESIAN_POINT('Ctrl Pts',(-0.397320308485734,1.50666776780901,
2.40884220181864));
#71802=CARTESIAN_POINT('Ctrl Pts',(-0.557274061624737,1.45429040141275,
2.42185154414691));
#71803=CARTESIAN_POINT('Ctrl Pts',(-0.628604739612074,1.4249110537569,2.42786221698135));
#71804=CARTESIAN_POINT('Ctrl Pts',(-0.719722226644113,1.37920271984165,
2.43564526011264));
#71805=CARTESIAN_POINT('Ctrl Pts',(-0.741708254627189,1.36750474707354,
2.43753119524499));
#71806=CARTESIAN_POINT('Ctrl Pts',(-0.778924694583664,1.3465414390679,2.44072667019765));
#71807=CARTESIAN_POINT('Ctrl Pts',(-0.794293837946009,1.33753313871166,
2.44204721312236));
#71808=CARTESIAN_POINT('Ctrl Pts',(-0.816711093926893,1.3238710060714,2.44397107509786));
#71809=CARTESIAN_POINT('Ctrl Pts',(-0.823880879694541,1.31942099290638,
2.44458603964271));
#71810=CARTESIAN_POINT('Ctrl Pts',(-0.83665534650042,1.31134763211018,2.44568060993475));
#71811=CARTESIAN_POINT('Ctrl Pts',(-0.842273313293819,1.30774632535656,
2.44616154882484));
#71812=CARTESIAN_POINT('Ctrl Pts',(-0.854912911102718,1.29952867154592,
2.44724266204309));
#71813=CARTESIAN_POINT('Ctrl Pts',(-0.861920520228475,1.29489145458927,
2.44784146003915));
#71814=CARTESIAN_POINT('Ctrl Pts',(-0.883505862549115,1.28035469056066,
2.44968524167102));
#71815=CARTESIAN_POINT('Ctrl Pts',(-0.897953806441506,1.27026366260986,
2.45091839191383));
#71816=CARTESIAN_POINT('Ctrl Pts',(-0.993818641449694,1.20085451539209,
2.45911707311284));
#71817=CARTESIAN_POINT('Ctrl Pts',(-1.06948921135085,1.13398645770458,2.46568082264389));
#71818=CARTESIAN_POINT('Ctrl Pts',(-1.18063253729121,1.01467643010332,2.47642103133751));
#71819=CARTESIAN_POINT('Ctrl Pts',(-1.2203177894895,0.966584258016473,2.48054004427704));
#71820=CARTESIAN_POINT('Ctrl Pts',(-1.27313355837751,0.894125506974991,
2.48660283746285));
#71821=CARTESIAN_POINT('Ctrl Pts',(-1.28866922124142,0.871585326068368,
2.48847002155155));
#71822=CARTESIAN_POINT('Ctrl Pts',(-1.31577620498229,0.829946503707971,
2.49189702238606));
#71823=CARTESIAN_POINT('Ctrl Pts',(-1.32754652642819,0.810986038004548,
2.49344948364089));
#71824=CARTESIAN_POINT('Ctrl Pts',(-1.34562343665252,0.780417871368361,
2.49594389695653));
#71825=CARTESIAN_POINT('Ctrl Pts',(-1.35219735111069,0.768971255395661,
2.49687610783986));
#71826=CARTESIAN_POINT('Ctrl Pts',(-1.36441842097084,0.747050327296673,
2.49865866202314));
#71827=CARTESIAN_POINT('Ctrl Pts',(-1.37009264297018,0.736592122012945,
2.49950795709923));
#71828=CARTESIAN_POINT('Ctrl Pts',(-1.38273491576973,0.712639484286972,
2.50145111392439));
#71829=CARTESIAN_POINT('Ctrl Pts',(-1.38962633138911,0.699106222670906,
2.50254758089147));
#71830=CARTESIAN_POINT('Ctrl Pts',(-1.41115771808279,0.655246587514691,
2.50609783020888));
#71831=CARTESIAN_POINT('Ctrl Pts',(-1.42501052816707,0.6245469307339,2.5085781263187));
#71832=CARTESIAN_POINT('Ctrl Pts',(-1.48498723162047,0.479224498839212,
2.52030496068836));
#71833=CARTESIAN_POINT('Ctrl Pts',(-1.51834019358153,0.359829211161852,
2.52994815320353));
#71834=CARTESIAN_POINT('Ctrl Pts',(-1.54315895425967,0.19937522749374,2.54248287376783));
#71835=CARTESIAN_POINT('Ctrl Pts',(-1.54765799975354,0.16076423955664,2.54546324943519));
#71836=CARTESIAN_POINT('Ctrl Pts',(-1.55261918076152,0.0977160113661703,
2.550236099301));
#71837=CARTESIAN_POINT('Ctrl Pts',(-1.55396022927822,0.0733656160231017,
2.55205674173795));
#71838=CARTESIAN_POINT('Ctrl Pts',(-1.55502807326686,0.0394783775701928,
2.55455026825913));
#71839=CARTESIAN_POINT('Ctrl Pts',(-1.55524054590962,0.0299617693615345,
2.55524612591083));
#71840=CARTESIAN_POINT('Ctrl Pts',(-1.55545461412657,0.0136751995529757,
2.55642880848515));
#71841=CARTESIAN_POINT('Ctrl Pts',(-1.55549939873703,0.00690621489850628,
2.55691791433138));
#71842=CARTESIAN_POINT('Ctrl Pts',(-1.55549999398642,0.000136778059410365,
2.55740452554354));
#71843=CARTESIAN_POINT('Origin',(0.,0.,-1.2940562256037));
#71844=CARTESIAN_POINT('',(-1.55549982468662,-0.000738511954293953,3.3940562256037));
#71845=CARTESIAN_POINT('',(-1.5555,-2.78355693781297E-11,3.25542335925836));
#71846=CARTESIAN_POINT('',(-1.5555,-1.46451138874614E-13,-1.2940562256037));
#71847=CARTESIAN_POINT('Ctrl Pts',(-1.55549941625285,0.00134760418419674,
2.6940562256037));
#71848=CARTESIAN_POINT('Ctrl Pts',(-1.55554919476569,-0.0561102521829977,
2.69816386501832));
#71849=CARTESIAN_POINT('Ctrl Pts',(-1.55241106539883,-0.113626806645204,
2.70227150443293));
#71850=CARTESIAN_POINT('Ctrl Pts',(-1.54609216886034,-0.170819364794349,
2.70637914384755));
#71851=CARTESIAN_POINT('Ctrl Pts',(-1.53977588609704,-0.227988265570853,
2.71048508416075));
#71852=CARTESIAN_POINT('Ctrl Pts',(-1.53028150231367,-0.284832911193982,
2.71459102447395));
#71853=CARTESIAN_POINT('Ctrl Pts',(-1.51766808417958,-0.340974832300971,
2.71869696478716));
#71854=CARTESIAN_POINT('Ctrl Pts',(-1.50505487515628,-0.39711582266256,
2.72280283703028));
#71855=CARTESIAN_POINT('Ctrl Pts',(-1.48932285319747,-0.452553597006042,
2.7269087092734));
#71856=CARTESIAN_POINT('Ctrl Pts',(-1.470581879495,-0.506921281562494,2.73101458151653));
#71857=CARTESIAN_POINT('Ctrl Pts',(-1.45182095795932,-0.561346834910656,
2.7351248240371));
#71858=CARTESIAN_POINT('Ctrl Pts',(-1.43004486854431,-0.614699526164613,
2.73923506655766));
#71859=CARTESIAN_POINT('Ctrl Pts',(-1.40541240745189,-0.666630493587175,
2.74334530907823));
#71860=CARTESIAN_POINT('Ctrl Pts',(-1.38076460904644,-0.718593795639242,
2.74745811082648));
#71861=CARTESIAN_POINT('Ctrl Pts',(-1.35325715531117,-0.769133149955912,
2.75157091257473));
#71862=CARTESIAN_POINT('Ctrl Pts',(-1.32309423869949,-0.817925354491605,
2.75568371432297));
#71863=CARTESIAN_POINT('Ctrl Pts',(-1.29287728787355,-0.86680496597365,
2.7598038837941));
#71864=CARTESIAN_POINT('Ctrl Pts',(-1.25999568941062,-0.91393075368594,
2.76392405326522));
#71865=CARTESIAN_POINT('Ctrl Pts',(-1.22469538727744,-0.9590106664586,2.76804422273635));
#71866=CARTESIAN_POINT('Ctrl Pts',(-1.21231302893473,-0.97482343859588,
2.76948946291112));
#71867=CARTESIAN_POINT('Ctrl Pts',(-1.19963341132009,-0.990384807910173,
2.77093470308588));
#71868=CARTESIAN_POINT('Ctrl Pts',(-1.18666820409511,-1.00568326196158,
2.77237994326064));
#71869=CARTESIAN_POINT('Ctrl Pts',(-1.14946026765927,-1.04958721937883,
2.77652753640158));
#71870=CARTESIAN_POINT('Ctrl Pts',(-1.10973421380613,-1.09151588262236,
2.78067512954252));
#71871=CARTESIAN_POINT('Ctrl Pts',(-1.06772786924713,-1.13116641005335,
2.78482272268345));
#71872=CARTESIAN_POINT('Ctrl Pts',(-1.02579635357129,-1.17074630518545,
2.78896292742233));
#71873=CARTESIAN_POINT('Ctrl Pts',(-0.981592985373571,-1.20805576476433,
2.79310313216121));
#71874=CARTESIAN_POINT('Ctrl Pts',(-0.935394673694029,-1.24282623661751,
2.79724333690009));
#71875=CARTESIAN_POINT('Ctrl Pts',(-0.889242412098968,-1.27756204955983,
2.80137941471807));
#71876=CARTESIAN_POINT('Ctrl Pts',(-0.841099560958813,-1.30976357736525,
2.80551549253606));
#71877=CARTESIAN_POINT('Ctrl Pts',(-0.791277263798694,-1.33920145676267,
2.80965157035404));
#71878=CARTESIAN_POINT('Ctrl Pts',(-0.741485463799256,-1.36862131668308,
2.81378511640137));
#71879=CARTESIAN_POINT('Ctrl Pts',(-0.690016703152289,-1.39528061706911,
2.81791866244869));
#71880=CARTESIAN_POINT('Ctrl Pts',(-0.637210522527536,-1.41899365748413,
2.82205220849602));
#71881=CARTESIAN_POINT('Ctrl Pts',(-0.584416353486958,-1.4427013040006,
2.82618481430424));
#71882=CARTESIAN_POINT('Ctrl Pts',(-0.530285843394223,-1.46346380767148,
2.83031742011246));
#71883=CARTESIAN_POINT('Ctrl Pts',(-0.475180504680632,-1.48114271357336,
2.83445002592068));
#71884=CARTESIAN_POINT('Ctrl Pts',(-0.420025304777168,-1.49883761595225,
2.83858637105158));
#71885=CARTESIAN_POINT('Ctrl Pts',(-0.363894010408683,-1.5134431839856,
2.84272271618248));
#71886=CARTESIAN_POINT('Ctrl Pts',(-0.307164078818147,-1.5248706432625,
2.84685906131337));
#71887=CARTESIAN_POINT('Ctrl Pts',(-0.250410771305569,-1.53630281129525,
2.85099711085107));
#71888=CARTESIAN_POINT('Ctrl Pts',(-0.193058851394598,-1.5445541842286,
2.85513516038878));
#71889=CARTESIAN_POINT('Ctrl Pts',(-0.135493559801193,-1.54958760489764,
2.85927320992648));
#71890=CARTESIAN_POINT('Ctrl Pts',(-0.0778156612983488,-1.55463087174186,
2.86341935415035));
#71891=CARTESIAN_POINT('Ctrl Pts',(-0.019924079591581,-1.55644358914889,
2.86756549837421));
#71892=CARTESIAN_POINT('Ctrl Pts',(0.0377941783268421,-1.55504078727363,
2.87171164259808));
#71893=CARTESIAN_POINT('Ctrl Pts',(0.0928761285919074,-1.55370205901136,
2.87566840980082));
#71894=CARTESIAN_POINT('Ctrl Pts',(0.147799846995512,-1.54943528185692,
2.87962517700356));
#71895=CARTESIAN_POINT('Ctrl Pts',(0.20223592217179,-1.54229727412822,2.8835819442063));
#71896=CARTESIAN_POINT('Ctrl Pts',(0.259297326209693,-1.53481501642109,
2.88772953734758));
#71897=CARTESIAN_POINT('Ctrl Pts',(0.316063027217814,-1.52414602651293,
2.89187713048887));
#71898=CARTESIAN_POINT('Ctrl Pts',(0.372149627444133,-1.51032609220433,
2.89602472363015));
#71899=CARTESIAN_POINT('Ctrl Pts',(0.428136316628248,-1.49653077632569,
2.90016492836936));
#71900=CARTESIAN_POINT('Ctrl Pts',(0.483445804533315,-1.47959578054093,
2.90430513310856));
#71901=CARTESIAN_POINT('Ctrl Pts',(0.537702335435016,-1.45960832022421,
2.90844533784777));
#71902=CARTESIAN_POINT('Ctrl Pts',(0.591904783887736,-1.43964078323809,
2.91258141566608));
#71903=CARTESIAN_POINT('Ctrl Pts',(0.645055868486251,-1.41662698921405,
2.91671749348438));
#71904=CARTESIAN_POINT('Ctrl Pts',(0.696794220209838,-1.39070416145281,
2.92085357130269));
#71905=CARTESIAN_POINT('Ctrl Pts',(0.748500901919766,-1.36479720153973,
2.92498711735033));
#71906=CARTESIAN_POINT('Ctrl Pts',(0.79879610012921,-1.33598497050557,2.92912066339797));
#71907=CARTESIAN_POINT('Ctrl Pts',(0.847339755745634,-1.30445221772702,
2.93325420944561));
#71908=CARTESIAN_POINT('Ctrl Pts',(0.895872369355102,-1.27292663756188,
2.93738681525413));
#71909=CARTESIAN_POINT('Ctrl Pts',(0.942653794652543,-1.23868204778156,
2.94151942106265));
#71910=CARTESIAN_POINT('Ctrl Pts',(0.987371775264395,-1.20194726482123,
2.94565202687117));
#71911=CARTESIAN_POINT('Ctrl Pts',(1.03213021823005,-1.16517924297657,2.94978837200235));
#71912=CARTESIAN_POINT('Ctrl Pts',(1.07482108101088,-1.1259168556243,2.95392471713353));
#71913=CARTESIAN_POINT('Ctrl Pts',(1.11516522225963,-1.08442924022853,2.95806106226472));
#71914=CARTESIAN_POINT('Ctrl Pts',(1.15552598756321,-1.04292452960228,2.96219911180269));
#71915=CARTESIAN_POINT('Ctrl Pts',(1.19353776009774,-0.999193156172173,
2.96633716134066));
#71916=CARTESIAN_POINT('Ctrl Pts',(1.22896056361456,-0.953538768525005,
2.97047521087863));
#71917=CARTESIAN_POINT('Ctrl Pts',(1.26445265979554,-0.90779507360014,2.97462135510275));
#71918=CARTESIAN_POINT('Ctrl Pts',(1.29734536823604,-0.860121276720506,
2.97876749932687));
#71919=CARTESIAN_POINT('Ctrl Pts',(1.32744161739779,-0.810850789233342,
2.98291364355099));
#71920=CARTESIAN_POINT('Ctrl Pts',(1.35616320668628,-0.763830753678599,
2.98687041075131));
#71921=CARTESIAN_POINT('Ctrl Pts',(1.38233812416302,-0.715357112159338,
2.99082717795163));
#71922=CARTESIAN_POINT('Ctrl Pts',(1.40583562872532,-0.665737512092028,
2.99478394515196));
#71923=CARTESIAN_POINT('Ctrl Pts',(1.43046636484214,-0.61372487082453,2.99893153829439));
#71924=CARTESIAN_POINT('Ctrl Pts',(1.4522585237969,-0.560233993408507,3.00307913143682));
#71925=CARTESIAN_POINT('Ctrl Pts',(1.47103443589969,-0.50560650549342,3.00722672457926));
#71926=CARTESIAN_POINT('Ctrl Pts',(1.48977690113767,-0.451076329399633,
3.01136692931966));
#71927=CARTESIAN_POINT('Ctrl Pts',(1.50551361623966,-0.395414050122525,
3.01550713406006));
#71928=CARTESIAN_POINT('Ctrl Pts',(1.51811427567436,-0.338982737014302,
3.01964733880046));
#71929=CARTESIAN_POINT('Ctrl Pts',(1.53070237487886,-0.282607674159265,
3.02378341661997));
#71930=CARTESIAN_POINT('Ctrl Pts',(1.54016049888285,-0.225465602079293,
3.02791949443948));
#71931=CARTESIAN_POINT('Ctrl Pts',(1.54640816782067,-0.167934595892287,
3.032055572259));
#71932=CARTESIAN_POINT('Ctrl Pts',(1.55265201244341,-0.110438805510911,
3.03618911830786));
#71933=CARTESIAN_POINT('Ctrl Pts',(1.5556892413464,-0.052555069776979,3.04032266435673));
#71934=CARTESIAN_POINT('Ctrl Pts',(1.55549086583674,0.0053306939939586,
3.0444562104056));
#71935=CARTESIAN_POINT('Ctrl Pts',(1.55529253545068,0.0632032907508674,
3.04858881621536));
#71936=CARTESIAN_POINT('Ctrl Pts',(1.55186006351953,0.121077393943223,3.05272142202512));
#71937=CARTESIAN_POINT('Ctrl Pts',(1.54521656351735,0.178566575348327,3.05685402783489));
#71938=CARTESIAN_POINT('Ctrl Pts',(1.5385670522498,0.236107774925385,3.06099037296732));
#71939=CARTESIAN_POINT('Ctrl Pts',(1.52870076533746,0.293262837779958,3.06512671809976));
#71940=CARTESIAN_POINT('Ctrl Pts',(1.51569264853327,0.349651319434369,3.0692630632322));
#71941=CARTESIAN_POINT('Ctrl Pts',(1.50267917165344,0.406063036314289,3.07340111277144));
#71942=CARTESIAN_POINT('Ctrl Pts',(1.48652142831699,0.461707040531794,3.07753916231068));
#71943=CARTESIAN_POINT('Ctrl Pts',(1.46734459181078,0.516217104408279,3.08167721184993));
#71944=CARTESIAN_POINT('Ctrl Pts',(1.44813024234798,0.570833798680196,3.08582335607531));
#71945=CARTESIAN_POINT('Ctrl Pts',(1.42588519719966,0.624311636572228,3.0899695003007));
#71946=CARTESIAN_POINT('Ctrl Pts',(1.40078289268773,0.676304323181071,3.09411564452609));
#71947=CARTESIAN_POINT('Ctrl Pts',(1.37682714742183,0.725922220035861,3.09807241171659));
#71948=CARTESIAN_POINT('Ctrl Pts',(1.35026975093779,0.774187372099828,3.1020291789071));
#71949=CARTESIAN_POINT('Ctrl Pts',(1.32129842765043,0.820823193561499,3.10598594609761));
#71950=CARTESIAN_POINT('Ctrl Pts',(1.2909298828292,0.869708155435229,3.1101335392393));
#71951=CARTESIAN_POINT('Ctrl Pts',(1.25778081383162,0.917008381459534,3.11428113238098));
#71952=CARTESIAN_POINT('Ctrl Pts',(1.22204207394009,0.962389432361037,3.11842872552267));
#71953=CARTESIAN_POINT('Ctrl Pts',(1.1863669980026,1.00768964277551,3.1225689302623));
#71954=CARTESIAN_POINT('Ctrl Pts',(1.14811172718562,1.05107705788631,3.12670913500193));
#71955=CARTESIAN_POINT('Ctrl Pts',(1.10751080230268,1.09224542699106,3.13084933974157));
#71956=CARTESIAN_POINT('Ctrl Pts',(1.0669503480766,1.13337275981536,3.1349854175603));
#71957=CARTESIAN_POINT('Ctrl Pts',(1.02404923616821,1.17228506001833,3.13912149537904));
#71958=CARTESIAN_POINT('Ctrl Pts',(0.979081617834388,1.20870982275267,3.14325757319777));
#71959=CARTESIAN_POINT('Ctrl Pts',(0.934141525021421,1.24511228920797,3.14739111924586));
#71960=CARTESIAN_POINT('Ctrl Pts',(0.887137837190999,1.27902990927621,3.15152466529394));
#71961=CARTESIAN_POINT('Ctrl Pts',(0.838379197764765,1.31022920542755,3.15565821134203));
#71962=CARTESIAN_POINT('Ctrl Pts',(0.789631649246822,1.34142140481539,3.159790817151));
#71963=CARTESIAN_POINT('Ctrl Pts',(0.739130380193175,1.36989622714469,3.16392342295997));
#71964=CARTESIAN_POINT('Ctrl Pts',(0.687212695546969,1.39546370826298,3.16805602876893));
#71965=CARTESIAN_POINT('Ctrl Pts',(0.63524803400905,1.42105432371016,3.17219237390058));
#71966=CARTESIAN_POINT('Ctrl Pts',(0.581864863608335,1.44373210896724,3.17632871903223));
#71967=CARTESIAN_POINT('Ctrl Pts',(0.527423546018679,1.46335390562402,3.18046506416387));
#71968=CARTESIAN_POINT('Ctrl Pts',(0.472959795544747,1.48298378756443,3.18460311370231));
#71969=CARTESIAN_POINT('Ctrl Pts',(0.417437528561135,1.49955501995419,3.18874116324076));
#71970=CARTESIAN_POINT('Ctrl Pts',(0.361232374303376,1.51297436255713,3.1928792127792));
#71971=CARTESIAN_POINT('Ctrl Pts',(0.304917273782369,1.52641995553859,3.19702535700379));
#71972=CARTESIAN_POINT('Ctrl Pts',(0.247917130813764,1.53670124337833,3.20117150122839));
#71973=CARTESIAN_POINT('Ctrl Pts',(0.190616973613277,1.54377635017852,3.20531764545298));
#71974=CARTESIAN_POINT('Ctrl Pts',(0.135934027218097,1.55052829824982,3.20927441264974));
#71975=CARTESIAN_POINT('Ctrl Pts',(0.0809782871612533,1.55436064168982,
3.21323117984651));
#71976=CARTESIAN_POINT('Ctrl Pts',(0.0260839355377171,1.55528128591161,
3.21718794704327));
#71977=CARTESIAN_POINT('Ctrl Pts',(-0.0314578466786569,1.55624633072482,
3.22133554018506));
#71978=CARTESIAN_POINT('Ctrl Pts',(-0.0891743656713,1.55401572701735,3.22548313332686));
#71979=CARTESIAN_POINT('Ctrl Pts',(-0.146681119937474,1.54856866139474,
3.22963072646865));
#71980=CARTESIAN_POINT('Ctrl Pts',(-0.204085433340574,1.54313129901674,
3.23377093120839));
#71981=CARTESIAN_POINT('Ctrl Pts',(-0.261280209372237,1.53448889598676,
3.23791113594813));
#71982=CARTESIAN_POINT('Ctrl Pts',(-0.317880965569942,1.52267263117465,
3.24205134068788));
#71983=CARTESIAN_POINT('Ctrl Pts',(-0.374425302614842,1.51086814471489,
3.24618741850672));
#71984=CARTESIAN_POINT('Ctrl Pts',(-0.430376285603987,1.49589617047065,
3.25032349632556));
#71985=CARTESIAN_POINT('Ctrl Pts',(-0.485356331049852,1.47783946418744,
3.2544595741444));
#71986=CARTESIAN_POINT('Ctrl Pts',(-0.540302722180867,1.45979381075211,
3.2585931201926));
#71987=CARTESIAN_POINT('Ctrl Pts',(-0.594278859959502,1.43866733041535,
3.26272666624079));
#71988=CARTESIAN_POINT('Ctrl Pts',(-0.646921272169161,1.41459291586486,
3.26686021228899));
#71989=CARTESIAN_POINT('Ctrl Pts',(-0.699551710046281,1.39052397741307,
3.27099281809807));
#71990=CARTESIAN_POINT('Ctrl Pts',(-0.750848551095643,1.36350865247988,
3.27512542390715));
#71991=CARTESIAN_POINT('Ctrl Pts',(-0.800469364159435,1.33372750104442,
3.27925802971623));
#71992=CARTESIAN_POINT('Ctrl Pts',(-0.850135075827078,1.30391940260753,
3.28339437484798));
#71993=CARTESIAN_POINT('Ctrl Pts',(-0.898121280457421,1.27134074407872,
3.28753071997973));
#71994=CARTESIAN_POINT('Ctrl Pts',(-0.944112392095885,1.23621682608311,
3.29166706511148));
#71995=CARTESIAN_POINT('Ctrl Pts',(-0.990122454658598,1.20107843505813,
3.29580511465003));
#71996=CARTESIAN_POINT('Ctrl Pts',(-1.03413538790551,1.16339303229937,3.29994316418858));
#71997=CARTESIAN_POINT('Ctrl Pts',(-1.07586928763052,1.12342579903321,3.30408121372713));
#71998=CARTESIAN_POINT('Ctrl Pts',(-1.11768482553238,1.08338038347209,3.30822735795182));
#71999=CARTESIAN_POINT('Ctrl Pts',(-1.15721206300446,1.04104459865491,3.31237350217652));
#72000=CARTESIAN_POINT('Ctrl Pts',(-1.19420717299843,0.996719357672504,
3.31651964640121));
#72001=CARTESIAN_POINT('Ctrl Pts',(-1.22951251446752,0.954418692291638,
3.32047641359712));
#72002=CARTESIAN_POINT('Ctrl Pts',(-1.26251183707756,0.910306733284846,
3.32443318079302));
#72003=CARTESIAN_POINT('Ctrl Pts',(-1.29303070491053,0.864668633731202,
3.32838994798892));
#72004=CARTESIAN_POINT('Ctrl Pts',(-1.32557770694717,0.815997650022029,
3.33260966251727));
#72005=CARTESIAN_POINT('Ctrl Pts',(-1.35543705041063,0.765390969309646,
3.33682937704562));
#72006=CARTESIAN_POINT('Ctrl Pts',(-1.38237733416478,0.713171196829676,
3.34104909157397));
#72007=CARTESIAN_POINT('Ctrl Pts',(-1.41057883180484,0.658506746974681,
3.34546635274312));
#72008=CARTESIAN_POINT('Ctrl Pts',(-1.43558082164121,0.602074834659629,
3.34988361391226));
#72009=CARTESIAN_POINT('Ctrl Pts',(-1.45716801087107,0.544280844871521,
3.3543008750814));
#72010=CARTESIAN_POINT('Ctrl Pts',(-1.4777184304184,0.489262531703761,3.35850598809123));
#72011=CARTESIAN_POINT('Ctrl Pts',(-1.49517431711702,0.433010500479543,
3.36271110110106));
#72012=CARTESIAN_POINT('Ctrl Pts',(-1.50939742874429,0.375898459826751,
3.36691621411088));
#72013=CARTESIAN_POINT('Ctrl Pts',(-1.52360699435621,0.318840812375658,
3.3711173221936));
#72014=CARTESIAN_POINT('Ctrl Pts',(-1.53458977591059,0.26092526186512,3.37531843027631));
#72015=CARTESIAN_POINT('Ctrl Pts',(-1.5422572513629,0.202540910974892,3.37951953835902));
#72016=CARTESIAN_POINT('Ctrl Pts',(-1.54991969604829,0.14419486709509,3.38371789002005));
#72017=CARTESIAN_POINT('Ctrl Pts',(-1.55427109154466,0.0853811260470057,
3.38791624168107));
#72018=CARTESIAN_POINT('Ctrl Pts',(-1.55527429853346,0.0264972889417979,
3.3921145933421));
#72019=CARTESIAN_POINT('Ctrl Pts',(-1.55542895121716,0.0174198567301612,
3.39276180409596));
#72020=CARTESIAN_POINT('Ctrl Pts',(-1.5555041352991,0.00834076823806055,
3.39340901484983));
#72021=CARTESIAN_POINT('Ctrl Pts',(-1.55549982468662,-0.000738511954293953,
3.3940562256037));
#72022=CARTESIAN_POINT('',(-1.55549947476597,0.00127828118742131,3.25533856168564));
#72023=CARTESIAN_POINT('Ctrl Pts',(-1.55549999398642,0.000136778059410365,
2.55740452554354));
#72024=CARTESIAN_POINT('Ctrl Pts',(-1.55550066677956,-0.00751452008594075,
2.55795452808491));
#72025=CARTESIAN_POINT('Ctrl Pts',(-1.55544488600269,-0.0151659363071791,
2.55850137101385));
#72026=CARTESIAN_POINT('Ctrl Pts',(-1.55512972380064,-0.0366492764225271,
2.56002866939962));
#72027=CARTESIAN_POINT('Ctrl Pts',(-1.55474227162549,-0.0504790145162955,
2.5610024208821));
#72028=CARTESIAN_POINT('Ctrl Pts',(-1.5507605366209,-0.14671644808943,2.5677243704524));
#72029=CARTESIAN_POINT('Ctrl Pts',(-1.54080024390489,-0.228740829829826,
2.5731811021714));
#72030=CARTESIAN_POINT('Ctrl Pts',(-1.50221506830842,-0.418724185891338,
2.58595363659456));
#72031=CARTESIAN_POINT('Ctrl Pts',(-1.4684010507505,-0.525142967947681,
2.59323359772228));
#72032=CARTESIAN_POINT('Ctrl Pts',(-1.41401818085348,-0.648604910160357,
2.60251882338264));
#72033=CARTESIAN_POINT('Ctrl Pts',(-1.40402879760403,-0.669954311443345,
2.60415556407635));
#72034=CARTESIAN_POINT('Ctrl Pts',(-1.38752070105268,-0.703243386997612,
2.60676216209202));
#72035=CARTESIAN_POINT('Ctrl Pts',(-1.38132357394818,-0.715339164546512,
2.60772089505095));
#72036=CARTESIAN_POINT('Ctrl Pts',(-1.36943494295856,-0.737813154368939,
2.60952497419714));
#72037=CARTESIAN_POINT('Ctrl Pts',(-1.36378189974084,-0.748210685224179,
2.61036891130377));
#72038=CARTESIAN_POINT('Ctrl Pts',(-1.35079292373463,-0.771464718384139,
2.61227796885413));
#72039=CARTESIAN_POINT('Ctrl Pts',(-1.34339110705816,-0.784282882557667,
2.61334539532601));
#72040=CARTESIAN_POINT('Ctrl Pts',(-1.32017086496893,-0.823201387824557,
2.61663409906608));
#72041=CARTESIAN_POINT('Ctrl Pts',(-1.30376717518654,-0.848942017646318,
2.61887631537352));
#72042=CARTESIAN_POINT('Ctrl Pts',(-1.26316368376271,-0.908702099935163,
2.62424698580593));
#72043=CARTESIAN_POINT('Ctrl Pts',(-1.23833144776733,-0.942261479662191,
2.62739632774339));
#72044=CARTESIAN_POINT('Ctrl Pts',(-1.17192749556495,-1.02483776366739,
2.63548418697364));
#72045=CARTESIAN_POINT('Ctrl Pts',(-1.12861297157979,-1.07235179214764,
2.64046610377546));
#72046=CARTESIAN_POINT('Ctrl Pts',(-1.03031144500876,-1.16761191090088,
2.65107908546627));
#72047=CARTESIAN_POINT('Ctrl Pts',(-0.974650843652776,-1.21446161680688,
2.65669755866666));
#72048=CARTESIAN_POINT('Ctrl Pts',(-0.902685969855538,-1.26688836512334,
2.66334302505764));
#72049=CARTESIAN_POINT('Ctrl Pts',(-0.889306135304163,-1.27631608304539,
2.66455406797432));
#72050=CARTESIAN_POINT('Ctrl Pts',(-0.869032337807875,-1.29012778230562,
2.66634991564225));
#72051=CARTESIAN_POINT('Ctrl Pts',(-0.862249079867954,-1.29467116717456,
2.666944339601));
#72052=CARTESIAN_POINT('Ctrl Pts',(-0.85040903911395,-1.30246721974515,
2.66797035125066));
#72053=CARTESIAN_POINT('Ctrl Pts',(-0.845368866448033,-1.30574418438921,
2.66840349604331));
#72054=CARTESIAN_POINT('Ctrl Pts',(-0.833298791917207,-1.31349258802845,
2.66943225002405));
#72055=CARTESIAN_POINT('Ctrl Pts',(-0.826251799324381,-1.31793688314205,
2.67002609142558));
#72056=CARTESIAN_POINT('Ctrl Pts',(-0.804514817460219,-1.33140276606742,
2.67183823325247));
#72057=CARTESIAN_POINT('Ctrl Pts',(-0.789709712342323,-1.34023731161851,
2.67304527615289));
#72058=CARTESIAN_POINT('Ctrl Pts',(-0.754108225941177,-1.36068668109432,
2.67589132368899));
#72059=CARTESIAN_POINT('Ctrl Pts',(-0.733185544818253,-1.3720738120714,
2.67751909735938));
#72060=CARTESIAN_POINT('Ctrl Pts',(-0.649251437632802,-1.41528625398166,
2.68390676129007));
#72061=CARTESIAN_POINT('Ctrl Pts',(-0.584363617661553,-1.44328899831511,
2.68853614528891));
#72062=CARTESIAN_POINT('Ctrl Pts',(-0.430403580540948,-1.49763876101227,
2.6992837319135));
#72063=CARTESIAN_POINT('Ctrl Pts',(-0.340440968283687,-1.52061378958834,
2.7054006977874));
#72064=CARTESIAN_POINT('Ctrl Pts',(-0.225074329439661,-1.53932063899589,
2.71343753695664));
#72065=CARTESIAN_POINT('Ctrl Pts',(-0.201088200458417,-1.54263732278657,
2.71511779170382));
#72066=CARTESIAN_POINT('Ctrl Pts',(-0.163396438537252,-1.54695517694606,
2.71777805227307));
#72067=CARTESIAN_POINT('Ctrl Pts',(-0.149737681512893,-1.54833695325033,
2.71874613601522));
#72068=CARTESIAN_POINT('Ctrl Pts',(-0.124285577097147,-1.55057186802312,
2.72055854671853));
#72069=CARTESIAN_POINT('Ctrl Pts',(-0.112497248359295,-1.55147168118908,
2.72140134261587));
#72070=CARTESIAN_POINT('Ctrl Pts',(-0.0861154641478392,-1.55318317776514,
2.72329557210615));
#72071=CARTESIAN_POINT('Ctrl Pts',(-0.0715186968300371,-1.55392371298778,
2.72434915684566));
#72072=CARTESIAN_POINT('Ctrl Pts',(-0.0274368483683089,-1.55553770231681,
2.7275487263976));
#72073=CARTESIAN_POINT('Ctrl Pts',(0.00206316530907804,-1.55577821332288,
2.72971401967982));
#72074=CARTESIAN_POINT('Ctrl Pts',(0.103148066050718,-1.55372747290761,
2.73722096485802));
#72075=CARTESIAN_POINT('Ctrl Pts',(0.174550679077534,-1.54733261192267,
2.74267898537828));
#72076=CARTESIAN_POINT('Ctrl Pts',(0.334405274658064,-1.52180962946239,
2.75517629248939));
#72077=CARTESIAN_POINT('Ctrl Pts',(0.42215254603717,-1.49983981473869,2.76223737825773));
#72078=CARTESIAN_POINT('Ctrl Pts',(0.534978008388259,-1.46089826797665,
2.77129447765354));
#72079=CARTESIAN_POINT('Ctrl Pts',(0.562186723515036,-1.45064522697536,
2.77347568542298));
#72080=CARTESIAN_POINT('Ctrl Pts',(0.598745281613202,-1.43568557815522,
2.77638827694897));
#72081=CARTESIAN_POINT('Ctrl Pts',(0.608356855410751,-1.43163925064063,
2.77715227513264));
#72082=CARTESIAN_POINT('Ctrl Pts',(0.623655573244839,-1.42501681985392,
2.77836471086829));
#72083=CARTESIAN_POINT('Ctrl Pts',(0.629368953979372,-1.42250270103646,
2.77881668628916));
#72084=CARTESIAN_POINT('Ctrl Pts',(0.641545977332521,-1.41705659021329,
2.77977800648085));
#72085=CARTESIAN_POINT('Ctrl Pts',(0.648005038399275,-1.41411459808982,
2.7802867179991));
#72086=CARTESIAN_POINT('Ctrl Pts',(0.66464901454116,-1.40639556368957,2.7815950521461));
#72087=CARTESIAN_POINT('Ctrl Pts',(0.674802871338014,-1.4015519606559,2.78239074623073));
#72088=CARTESIAN_POINT('Ctrl Pts',(0.720607227504908,-1.379089117413,2.78597294660997));
#72089=CARTESIAN_POINT('Ctrl Pts',(0.755629815717988,-1.36021534078926,
2.78869212282522));
#72090=CARTESIAN_POINT('Ctrl Pts',(0.868272761519911,-1.29381627328179,
2.79749913649785));
#72091=CARTESIAN_POINT('Ctrl Pts',(0.942451140986418,-1.24082467600295,
2.80340733545588));
#72092=CARTESIAN_POINT('Ctrl Pts',(1.06849598321466,-1.13292145742947,2.81438416256689));
#72093=CARTESIAN_POINT('Ctrl Pts',(1.12181490289742,-1.08014994603771,2.81940104834758));
#72094=CARTESIAN_POINT('Ctrl Pts',(1.18433486489243,-1.00862992407715,2.8259756026149));
#72095=CARTESIAN_POINT('Ctrl Pts',(1.19725496627948,-0.993259219626242,
2.82737621466455));
#72096=CARTESIAN_POINT('Ctrl Pts',(1.2178782538717,-0.967737061446407,2.82968498058656));
#72097=CARTESIAN_POINT('Ctrl Pts',(1.22576087397562,-0.957733117215039,
2.83058585250302));
#72098=CARTESIAN_POINT('Ctrl Pts',(1.2408651223291,-0.938072161336295,2.83234918312583));
#72099=CARTESIAN_POINT('Ctrl Pts',(1.24809907014167,-0.928425725467489,
2.83321107102667));
#72100=CARTESIAN_POINT('Ctrl Pts',(1.26499258002281,-0.905344030031443,
2.83526628443137));
#72101=CARTESIAN_POINT('Ctrl Pts',(1.27455115790333,-0.891837062931261,
2.83646338717477));
#72102=CARTESIAN_POINT('Ctrl Pts',(1.30730244554708,-0.843954978902197,
2.8406894778553));
#72103=CARTESIAN_POINT('Ctrl Pts',(1.32933265301186,-0.808810113314039,
2.84376073671328));
#72104=CARTESIAN_POINT('Ctrl Pts',(1.38272092575624,-0.715554839641528,
2.85183698587778));
#72105=CARTESIAN_POINT('Ctrl Pts',(1.41182924184471,-0.656256404518643,
2.85690516928635));
#72106=CARTESIAN_POINT('Ctrl Pts',(1.47492623802638,-0.503935962714824,
2.86966857722658));
#72107=CARTESIAN_POINT('Ctrl Pts',(1.50397528371496,-0.40917017445148,2.87739430262341));
#72108=CARTESIAN_POINT('Ctrl Pts',(1.52684922231614,-0.297552931621444,
2.88588148259573));
#72109=CARTESIAN_POINT('Ctrl Pts',(1.52965405030364,-0.28278052526185,2.88699236380233));
#72110=CARTESIAN_POINT('Ctrl Pts',(1.53362113569536,-0.260096771705943,
2.8886769669872));
#72111=CARTESIAN_POINT('Ctrl Pts',(1.5349372466382,-0.252213748510286,2.88925849472302));
#72112=CARTESIAN_POINT('Ctrl Pts',(1.53724467080977,-0.237705571874942,
2.89032116725107));
#72113=CARTESIAN_POINT('Ctrl Pts',(1.53825399282406,-0.231083909729386,
2.89080323568961));
#72114=CARTESIAN_POINT('Ctrl Pts',(1.5405097763891,-0.21561470491729,2.89192275849157));
#72115=CARTESIAN_POINT('Ctrl Pts',(1.54172283011084,-0.206762659752222,
2.89255836727252));
#72116=CARTESIAN_POINT('Ctrl Pts',(1.54548509465893,-0.177431507639867,
2.89464932927137));
#72117=CARTESIAN_POINT('Ctrl Pts',(1.5477031746557,-0.156911142221963,2.89608784830627));
#72118=CARTESIAN_POINT('Ctrl Pts',(1.55218843318401,-0.105940194308941,
2.89961446193309));
#72119=CARTESIAN_POINT('Ctrl Pts',(1.5539688142981,-0.0754547455868742,
2.90168275320559));
#72120=CARTESIAN_POINT('Ctrl Pts',(1.55849862962008,0.0812875922889848,
2.91219620116184));
#72121=CARTESIAN_POINT('Ctrl Pts',(1.54676377354634,0.207483869094535,2.92029866090758));
#72122=CARTESIAN_POINT('Ctrl Pts',(1.51125711902438,0.370585557176765,2.93157176474556));
#72123=CARTESIAN_POINT('Ctrl Pts',(1.50106063534625,0.409936877928736,2.9343517461041));
#72124=CARTESIAN_POINT('Ctrl Pts',(1.48448020982984,0.464953700068905,2.93835155572542));
#72125=CARTESIAN_POINT('Ctrl Pts',(1.4793634549305,0.480985619414882,2.93953089575813));
#72126=CARTESIAN_POINT('Ctrl Pts',(1.47015904366596,0.508287587206274,2.94156473538278));
#72127=CARTESIAN_POINT('Ctrl Pts',(1.46619927875229,0.519599408557588,2.94241497815045));
#72128=CARTESIAN_POINT('Ctrl Pts',(1.45780303707786,0.542724392656266,2.94416936406522));
#72129=CARTESIAN_POINT('Ctrl Pts',(1.45335274509936,0.554531552081247,2.94507391356647));
#72130=CARTESIAN_POINT('Ctrl Pts',(1.44165981417089,0.584446356844289,2.94738887558736));
#72131=CARTESIAN_POINT('Ctrl Pts',(1.43421956947114,0.60247383859173,2.94880581323711));
#72132=CARTESIAN_POINT('Ctrl Pts',(1.39785350793337,0.686093739276635,2.95548442006801));
#72133=CARTESIAN_POINT('Ctrl Pts',(1.364758656916,0.7497666850119,2.96088506695034));
#72134=CARTESIAN_POINT('Ctrl Pts',(1.31268204102985,0.835010683626217,2.96854818384035));
#72135=CARTESIAN_POINT('Ctrl Pts',(1.29731434304312,0.85869225689098,2.9707264005899));
#72136=CARTESIAN_POINT('Ctrl Pts',(1.22462154754005,0.96430249328216,2.98064993055986));
#72137=CARTESIAN_POINT('Ctrl Pts',(1.16011906811862,1.04101106038503,2.98846446751961));
#72138=CARTESIAN_POINT('Ctrl Pts',(1.07803053308083,1.12145145076103,2.99702410884487));
#72139=CARTESIAN_POINT('Ctrl Pts',(1.06721572046666,1.1317481327949,2.99812715855436));
#72140=CARTESIAN_POINT('Ctrl Pts',(1.05040326888894,1.14729975980074,2.99980240142664));
#72141=CARTESIAN_POINT('Ctrl Pts',(1.04451105612193,1.1526666592142,3.00038227438098));
#72142=CARTESIAN_POINT('Ctrl Pts',(1.03358898230614,1.16246246041332,3.00144348733738));
#72143=CARTESIAN_POINT('Ctrl Pts',(1.0285715728754,1.16690431422159,3.00192573017348));
#72144=CARTESIAN_POINT('Ctrl Pts',(1.0167734474811,1.17721383083758,3.00304767886981));
#72145=CARTESIAN_POINT('Ctrl Pts',(1.00997048562823,1.18305548285214,3.00368551109597));
#72146=CARTESIAN_POINT('Ctrl Pts',(0.987197401696555,1.20227094226485,3.00579216531965));
#72147=CARTESIAN_POINT('Ctrl Pts',(0.971008416489164,1.21538343417404,3.00724380511885));
#72148=CARTESIAN_POINT('Ctrl Pts',(0.930136327124901,1.24715015686346,3.01081050752392));
#72149=CARTESIAN_POINT('Ctrl Pts',(0.905150316694884,1.26540122104497,3.01290517853364));
#72150=CARTESIAN_POINT('Ctrl Pts',(0.770903718344337,1.35744922297951,3.02381341498146));
#72151=CARTESIAN_POINT('Ctrl Pts',(0.653137773882393,1.4178765751256,3.03226054165568));
#72152=CARTESIAN_POINT('Ctrl Pts',(0.49511419470183,1.47504332771572,3.04365665765363));
#72153=CARTESIAN_POINT('Ctrl Pts',(0.460653535675166,1.48616582802963,3.04614157739441));
#72154=CARTESIAN_POINT('Ctrl Pts',(0.411885177842958,1.5000471042921,3.04967630261994));
#72155=CARTESIAN_POINT('Ctrl Pts',(0.397877545711802,1.50382317729253,3.0506935762601));
#72156=CARTESIAN_POINT('Ctrl Pts',(0.37214058149244,1.51037640310508,3.05256748583295));
#72157=CARTESIAN_POINT('Ctrl Pts',(0.360427753703246,1.51321423168955,3.05342210538286));
#72158=CARTESIAN_POINT('Ctrl Pts',(0.336490771335413,1.51872009825405,3.05517294093227));
#72159=CARTESIAN_POINT('Ctrl Pts',(0.324265064788769,1.52137731246451,3.05606943414939));
#72160=CARTESIAN_POINT('Ctrl Pts',(0.293420348508984,1.52769262964377,3.05833758590178));
#72161=CARTESIAN_POINT('Ctrl Pts',(0.274764457423025,1.53115796225464,3.05971524869403));
#72162=CARTESIAN_POINT('Ctrl Pts',(0.192727491827976,1.54484881348478,3.06580150307484));
#72163=CARTESIAN_POINT('Ctrl Pts',(0.128819709276032,1.55148483181308,3.070619759824));
#72164=CARTESIAN_POINT('Ctrl Pts',(-0.0340268311751895,1.55826338465152,
3.08307355389477));
#72165=CARTESIAN_POINT('Ctrl Pts',(-0.132905830901143,1.5529574776016,3.09081017326475));
#72166=CARTESIAN_POINT('Ctrl Pts',(-0.273817259753969,1.53183327443442,
3.10174400677911));
#72167=CARTESIAN_POINT('Ctrl Pts',(-0.316736965535675,1.52353783377184,
3.10505845832463));
#72168=CARTESIAN_POINT('Ctrl Pts',(-0.370831151647846,1.51069721702341,
3.10917265223417));
#72169=CARTESIAN_POINT('Ctrl Pts',(-0.382376537511689,1.5078163121503,3.1100469970095));
#72170=CARTESIAN_POINT('Ctrl Pts',(-0.40088967848638,1.5029704239286,3.11144175913816));
#72171=CARTESIAN_POINT('Ctrl Pts',(-0.407878485003016,1.50108886370351,
3.11196661411289));
#72172=CARTESIAN_POINT('Ctrl Pts',(-0.421571009292349,1.49729980497505,
3.11299128119691));
#72173=CARTESIAN_POINT('Ctrl Pts',(-0.428275460830389,1.49539591908275,
3.1134912599735));
#72174=CARTESIAN_POINT('Ctrl Pts',(-0.445179855151272,1.49047250773447,
3.11474800438157));
#72175=CARTESIAN_POINT('Ctrl Pts',(-0.455362292910664,1.48739322258794,
3.11550142380806));
#72176=CARTESIAN_POINT('Ctrl Pts',(-0.497334160288804,1.4742290187605,3.11859526534472));
#72177=CARTESIAN_POINT('Ctrl Pts',(-0.528829243104645,1.46322673847797,
3.12088889189161));
#72178=CARTESIAN_POINT('Ctrl Pts',(-0.619990830119003,1.42805230071179,
3.12751249065167));
#72179=CARTESIAN_POINT('Ctrl Pts',(-0.678541556288328,1.40117969116268,
3.13174881750846));
#72180=CARTESIAN_POINT('Ctrl Pts',(-0.824199000176661,1.32305015840969,
3.14262881113184));
#72181=CARTESIAN_POINT('Ctrl Pts',(-0.908271736794991,1.26680903863619,
3.14926055087571));
#72182=CARTESIAN_POINT('Ctrl Pts',(-1.00506785920549,1.18743750937835,3.15786773475718));
#72183=CARTESIAN_POINT('Ctrl Pts',(-1.02347086873527,1.17161278202752,3.15955183429557));
#72184=CARTESIAN_POINT('Ctrl Pts',(-1.05170116182092,1.14616478498989,3.1622168343793));
#72185=CARTESIAN_POINT('Ctrl Pts',(-1.06178433133578,1.13683026888804,3.16318574119065));
#72186=CARTESIAN_POINT('Ctrl Pts',(-1.08031010434405,1.11921851318366,3.16499890037722));
#72187=CARTESIAN_POINT('Ctrl Pts',(-1.08878461570736,1.11097616907149,3.16584161104774));
#72188=CARTESIAN_POINT('Ctrl Pts',(-1.10690567057418,1.09294507688949,3.16767318785373));
#72189=CARTESIAN_POINT('Ctrl Pts',(-1.11651801054958,1.08312354524126,3.16866346606241));
#72190=CARTESIAN_POINT('Ctrl Pts',(-1.14476824736488,1.05348281297292,3.17163127472119));
#72191=CARTESIAN_POINT('Ctrl Pts',(-1.16301677298507,1.03330159741598,3.17362504240296));
#72192=CARTESIAN_POINT('Ctrl Pts',(-1.20425022545421,0.985224537130244,
3.17831646419471));
#72193=CARTESIAN_POINT('Ctrl Pts',(-1.22681002964438,0.956986303982907,
3.18102900277771));
#72194=CARTESIAN_POINT('Ctrl Pts',(-1.30975983730283,0.845399322573014,
3.19158183578564));
#72195=CARTESIAN_POINT('Ctrl Pts',(-1.36280402610939,0.756923228062467,
3.19962943570454));
#72196=CARTESIAN_POINT('Ctrl Pts',(-1.4286109880124,0.617480513162525,3.21150716946423));
#72197=CARTESIAN_POINT('Ctrl Pts',(-1.44819793151959,0.570031066384954,
3.21541704128836));
#72198=CARTESIAN_POINT('Ctrl Pts',(-1.46954440868428,0.510070346638533,
3.22013153937928));
#72199=CARTESIAN_POINT('Ctrl Pts',(-1.47354481131869,0.498395668327471,
3.22103906356265));
#72200=CARTESIAN_POINT('Ctrl Pts',(-1.47970023587389,0.479709527938183,
3.2224737523592));
#72201=CARTESIAN_POINT('Ctrl Pts',(-1.481945244217,0.472728588445855,3.22300579498135));
#72202=CARTESIAN_POINT('Ctrl Pts',(-1.48620882975001,0.459141882683332,
3.22403330146045));
#72203=CARTESIAN_POINT('Ctrl Pts',(-1.48823290217871,0.452538159151741,
3.22452904114376));
#72204=CARTESIAN_POINT('Ctrl Pts',(-1.49317118369247,0.436035033926161,
3.22575926801548));
#72205=CARTESIAN_POINT('Ctrl Pts',(-1.49603106785679,0.426119459694168,
3.22649070193102));
#72206=CARTESIAN_POINT('Ctrl Pts',(-1.50204147877787,0.404473903453057,
3.22807215182909));
#72207=CARTESIAN_POINT('Ctrl Pts',(-1.50515375825844,0.392733915449799,
3.22892020866478));
#72208=CARTESIAN_POINT('Ctrl Pts',(-1.53948062599013,0.256841540014063,
3.23863820370184));
#72209=CARTESIAN_POINT('Ctrl Pts',(-1.55539425379136,0.129318318352997,
3.24684545811903));
#72210=CARTESIAN_POINT('Ctrl Pts',(-1.55549947476597,0.00127828118742131,
3.25533856168564));
#72211=CARTESIAN_POINT('Ctrl Pts',(-1.55549947598823,0.00127679299616906,
3.25533866039979));
#72212=CARTESIAN_POINT('Ctrl Pts',(-1.55549982533167,0.000851192647130529,
3.25536689116748));
#72213=CARTESIAN_POINT('Ctrl Pts',(-1.55550000000001,0.000425594936828899,
3.25539512411182));
#72214=CARTESIAN_POINT('Ctrl Pts',(-1.5555,-2.78355693781297E-11,3.25542335925836));
#72215=CARTESIAN_POINT('Origin',(0.,0.,-1.2940562256037));
#72216=CARTESIAN_POINT('',(-1.5555,3.27936543916168E-11,4.09298010292487));
#72217=CARTESIAN_POINT('',(-1.55549973205853,-0.000912999512362819,3.95473109552063));
#72218=CARTESIAN_POINT('',(-1.5555,-1.46451138874614E-13,-1.2940562256037));
#72219=CARTESIAN_POINT('Ctrl Pts',(-1.5555,3.27936543916168E-11,4.09298010292487));
#72220=CARTESIAN_POINT('Ctrl Pts',(-1.55549999999797,0.0961723718999923,
4.0865093943148));
#72221=CARTESIAN_POINT('Ctrl Pts',(-1.54658104654986,0.19214252460412,4.08027899656591));
#72222=CARTESIAN_POINT('Ctrl Pts',(-1.5160184056625,0.355132423876049,4.0692864656076));
#72223=CARTESIAN_POINT('Ctrl Pts',(-1.4986013139837,0.422638307704138,4.06460887058734));
#72224=CARTESIAN_POINT('Ctrl Pts',(-1.47058125802744,0.507299717203055,
4.05843293558878));
#72225=CARTESIAN_POINT('Ctrl Pts',(-1.46409136710595,0.525736291991427,
4.05706892840103));
#72226=CARTESIAN_POINT('Ctrl Pts',(-1.45291589980749,0.555670429162924,
4.05482015705476));
#72227=CARTESIAN_POINT('Ctrl Pts',(-1.44843687620198,0.567243190624775,
4.05394229765395));
#72228=CARTESIAN_POINT('Ctrl Pts',(-1.43945027808374,0.589661829440032,
4.05222449354026));
#72229=CARTESIAN_POINT('Ctrl Pts',(-1.43495736839511,0.600512708519122,
4.05138509259346));
#72230=CARTESIAN_POINT('Ctrl Pts',(-1.42401722826071,0.626110371663382,
4.04938538850006));
#72231=CARTESIAN_POINT('Ctrl Pts',(-1.41746325999352,0.640809748848823,
4.04822151416309));
#72232=CARTESIAN_POINT('Ctrl Pts',(-1.39382744592283,0.691683129952188,
4.04413732687073));
#72233=CARTESIAN_POINT('Ctrl Pts',(-1.37558060494067,0.727294966522605,
4.04117766697035));
#72234=CARTESIAN_POINT('Ctrl Pts',(-1.32527484197728,0.816795404353789,
4.03347186927593));
#72235=CARTESIAN_POINT('Ctrl Pts',(-1.29129572384702,0.869518282893116,
4.02866908328488));
#72236=CARTESIAN_POINT('Ctrl Pts',(-1.19446380387038,1.00152268546568,4.016007762852));
#72237=CARTESIAN_POINT('Ctrl Pts',(-1.12689419921254,1.07698813317372,4.00809764905098));
#72238=CARTESIAN_POINT('Ctrl Pts',(-1.03977283005922,1.15704383364694,3.99925028601655));
#72239=CARTESIAN_POINT('Ctrl Pts',(-1.02687358290104,1.16850703075635,3.99797142028373));
#72240=CARTESIAN_POINT('Ctrl Pts',(-1.00747199783853,1.18517919299813,3.99609662136178));
#72241=CARTESIAN_POINT('Ctrl Pts',(-1.00111477980536,1.19055396855765,3.99548985595854));
#72242=CARTESIAN_POINT('Ctrl Pts',(-0.989716231450383,1.2000351241053,3.99441572401816));
#72243=CARTESIAN_POINT('Ctrl Pts',(-0.984691950335508,1.20416123738632,
3.99394699498987));
#72244=CARTESIAN_POINT('Ctrl Pts',(-0.973384553336077,1.2133291595659,3.99290261887856));
#72245=CARTESIAN_POINT('Ctrl Pts',(-0.967087977612545,1.21835380301992,
3.99232816884416));
#72246=CARTESIAN_POINT('Ctrl Pts',(-0.947823887904936,1.23348302408408,
3.99059116742359));
#72247=CARTESIAN_POINT('Ctrl Pts',(-0.934734483940863,1.24343153977477,
3.98943882914256));
#72248=CARTESIAN_POINT('Ctrl Pts',(-0.90338067449584,1.26648680592147,3.98673721904535));
#72249=CARTESIAN_POINT('Ctrl Pts',(-0.884984700595165,1.27940910719654,
3.98519788141716));
#72250=CARTESIAN_POINT('Ctrl Pts',(-0.813195164333619,1.32754820574574,
3.9793368882468));
#72251=CARTESIAN_POINT('Ctrl Pts',(-0.757926064274728,1.35986023703415,
3.9751261010072));
#72252=CARTESIAN_POINT('Ctrl Pts',(-0.609082211501665,1.43497685278604,
3.96415378350199));
#72253=CARTESIAN_POINT('Ctrl Pts',(-0.51299250989561,1.47206496064522,3.95740658000145));
#72254=CARTESIAN_POINT('Ctrl Pts',(-0.390988362417942,1.5057476387048,3.94869955841954));
#72255=CARTESIAN_POINT('Ctrl Pts',(-0.367881609119759,1.51155908518508,
3.94704571324467));
#72256=CARTESIAN_POINT('Ctrl Pts',(-0.331551877907083,1.51981382502132,
3.94443288756169));
#72257=CARTESIAN_POINT('Ctrl Pts',(-0.318414589652544,1.52262038582644,
3.94348553286073));
#72258=CARTESIAN_POINT('Ctrl Pts',(-0.293953463955743,1.52751568510971,
3.94171606521265));
#72259=CARTESIAN_POINT('Ctrl Pts',(-0.282639519677632,1.5296495337313,3.94089545744011));
#72260=CARTESIAN_POINT('Ctrl Pts',(-0.257370779052741,1.53412539738197,
3.93905732226748));
#72261=CARTESIAN_POINT('Ctrl Pts',(-0.243405773758763,1.53640296064816,
3.93803782005983));
#72262=CARTESIAN_POINT('Ctrl Pts',(-0.201535766674934,1.54264641164664,
3.93496926788953));
#72263=CARTESIAN_POINT('Ctrl Pts',(-0.173553444326004,1.54604451009725,
3.93290268568777));
#72264=CARTESIAN_POINT('Ctrl Pts',(-0.081877620771733,1.55465729680042,
3.92607635915011));
#72265=CARTESIAN_POINT('Ctrl Pts',(-0.0179593145520292,1.55670771324327,
3.9212262033976));
#72266=CARTESIAN_POINT('Ctrl Pts',(0.153773987858308,1.55163828903036,3.90800325951898));
#72267=CARTESIAN_POINT('Ctrl Pts',(0.261025946268553,1.53723582719364,3.89952528091339));
#72268=CARTESIAN_POINT('Ctrl Pts',(0.388697071536212,1.50633456344946,3.88961783538915));
#72269=CARTESIAN_POINT('Ctrl Pts',(0.411344012874213,1.50030846299012,3.88786887178004));
#72270=CARTESIAN_POINT('Ctrl Pts',(0.442947721905521,1.49112955932365,3.88544791612991));
#72271=CARTESIAN_POINT('Ctrl Pts',(0.452023776008327,1.48840336102673,3.88475497358671));
#72272=CARTESIAN_POINT('Ctrl Pts',(0.467404321649869,1.48362979684451,3.88358528893068));
#72273=CARTESIAN_POINT('Ctrl Pts',(0.473721567440397,1.48162480328825,3.88310620216603));
#72274=CARTESIAN_POINT('Ctrl Pts',(0.487006278791073,1.47731478885378,3.88210174829763));
#72275=CARTESIAN_POINT('Ctrl Pts',(0.493970510288702,1.47500075994025,3.88157690080123));
#72276=CARTESIAN_POINT('Ctrl Pts',(0.513139613029507,1.46848038105032,3.88013631415919));
#72277=CARTESIAN_POINT('Ctrl Pts',(0.525309235761293,1.46417114009887,3.87922631281039));
#72278=CARTESIAN_POINT('Ctrl Pts',(0.618344789530839,1.42991807285091,3.87229424768459));
#72279=CARTESIAN_POINT('Ctrl Pts',(0.696660204834102,1.39344353793524,3.86659896100625));
#72280=CARTESIAN_POINT('Ctrl Pts',(0.866552692998655,1.29639329700604,3.85371511181484));
#72281=CARTESIAN_POINT('Ctrl Pts',(0.955547501503209,1.2322641084535,3.84655613748701));
#72282=CARTESIAN_POINT('Ctrl Pts',(1.05460928615685,1.14364896646002,3.83740891282686));
#72283=CARTESIAN_POINT('Ctrl Pts',(1.07178429223863,1.12756908207228,3.83577528834192));
#72284=CARTESIAN_POINT('Ctrl Pts',(1.09813740297661,1.10175008206707,3.83318739791945));
#72285=CARTESIAN_POINT('Ctrl Pts',(1.10756619464419,1.09227107609621,3.8322443892467));
#72286=CARTESIAN_POINT('Ctrl Pts',(1.12488796282642,1.07440214851652,3.83047890211347));
#72287=CARTESIAN_POINT('Ctrl Pts',(1.13281225259552,1.06604375749793,3.82965787421626));
#72288=CARTESIAN_POINT('Ctrl Pts',(1.15031788975076,1.04716354730411,3.82781339240678));
#72289=CARTESIAN_POINT('Ctrl Pts',(1.15984902449567,1.03659681536245,3.8267878980819));
#72290=CARTESIAN_POINT('Ctrl Pts',(1.18810701985886,1.00439079118751,3.82368154684059));
#72291=CARTESIAN_POINT('Ctrl Pts',(1.20638206321886,0.982365140601841,3.82158250544671));
#72292=CARTESIAN_POINT('Ctrl Pts',(1.26979367882918,0.90150011391547,3.81396027197312));
#72293=CARTESIAN_POINT('Ctrl Pts',(1.31131227227638,0.839961813950697,3.80830771229271));
#72294=CARTESIAN_POINT('Ctrl Pts',(1.39421044262462,0.695873714600873,3.79546804290782));
#72295=CARTESIAN_POINT('Ctrl Pts',(1.43296018313743,0.612118553094414,3.78826184291176));
#72296=CARTESIAN_POINT('Ctrl Pts',(1.47322287196129,0.499928416234718,3.77923481401478));
#72297=CARTESIAN_POINT('Ctrl Pts',(1.48170618626917,0.474195162606534,3.77720576194676));
#72298=CARTESIAN_POINT('Ctrl Pts',(1.4923986817236,0.438664630753659,3.77447208963765));
#72299=CARTESIAN_POINT('Ctrl Pts',(1.49519124327984,0.429049698406976,3.77373905151848));
#72300=CARTESIAN_POINT('Ctrl Pts',(1.49968567723108,0.412998098588867,3.77252719548992));
#72301=CARTESIAN_POINT('Ctrl Pts',(1.50143938020525,0.406576381749281,3.77204552893751));
#72302=CARTESIAN_POINT('Ctrl Pts',(1.5049826460929,0.393265984719415,3.77105394955424));
#72303=CARTESIAN_POINT('Ctrl Pts',(1.50676624714113,0.386375958996842,3.77054437219304));
#72304=CARTESIAN_POINT('Ctrl Pts',(1.5114006023796,0.367953244210156,3.7691911215732));
#72305=CARTESIAN_POINT('Ctrl Pts',(1.51416670922835,0.356399453117021,3.76835208934191));
#72306=CARTESIAN_POINT('Ctrl Pts',(1.52820287487348,0.294655961635023,3.76391400858891));
#72307=CARTESIAN_POINT('Ctrl Pts',(1.53711176539667,0.243956558049187,3.76042969817292));
#72308=CARTESIAN_POINT('Ctrl Pts',(1.55156672203716,0.128297067216008,3.75265086713397));
#72309=CARTESIAN_POINT('Ctrl Pts',(1.55557706746083,0.0632454462312255,
3.74839324341717));
#72310=CARTESIAN_POINT('Ctrl Pts',(1.5553939680873,-0.0892340033225456,
3.7383422055366));
#72311=CARTESIAN_POINT('Ctrl Pts',(1.54792911191298,-0.176424694897936,
3.73253316740635));
#72312=CARTESIAN_POINT('Ctrl Pts',(1.52976132969099,-0.282528868339989,
3.72508698312319));
#72313=CARTESIAN_POINT('Ctrl Pts',(1.52594436201107,-0.302466568221327,
3.7236716840226));
#72314=CARTESIAN_POINT('Ctrl Pts',(1.51913467717288,-0.334616171589868,
3.72136026318372));
#72315=CARTESIAN_POINT('Ctrl Pts',(1.51638205671683,-0.346876910515645,
3.7204718252204));
#72316=CARTESIAN_POINT('Ctrl Pts',(1.5107854714666,-0.370464392339823,3.71874850480573));
#72317=CARTESIAN_POINT('Ctrl Pts',(1.50796189180211,-0.381795136085018,
3.7179143316572));
#72318=CARTESIAN_POINT('Ctrl Pts',(1.50105165052053,-0.408251971148112,
3.7159511343197));
#72319=CARTESIAN_POINT('Ctrl Pts',(1.49686355076355,-0.423349981027338,
3.71481889572626));
#72320=CARTESIAN_POINT('Ctrl Pts',(1.48198735243904,-0.47399524870437,3.71097918483647));
#72321=CARTESIAN_POINT('Ctrl Pts',(1.47025596021202,-0.509219983615412,
3.70823845436778));
#72322=CARTESIAN_POINT('Ctrl Pts',(1.43776457389458,-0.59626027222761,3.70128436723927));
#72323=CARTESIAN_POINT('Ctrl Pts',(1.41545576459332,-0.647438920799612,
3.6970279551877));
#72324=CARTESIAN_POINT('Ctrl Pts',(1.36693300922773,-0.744194934353254,
3.6886823755887));
#72325=CARTESIAN_POINT('Ctrl Pts',(1.34106097370961,-0.789865320960806,
3.68460383020917));
#72326=CARTESIAN_POINT('Ctrl Pts',(1.27683647936504,-0.890954306381601,
3.67533029822414));
#72327=CARTESIAN_POINT('Ctrl Pts',(1.23708697992361,-0.945372331420556,
3.67015448970654));
#72328=CARTESIAN_POINT('Ctrl Pts',(1.18582446423293,-1.00675746025347,3.66422551982853));
#72329=CARTESIAN_POINT('Ctrl Pts',(1.17759828734018,-1.01636732770417,3.66329461198794));
#72330=CARTESIAN_POINT('Ctrl Pts',(1.16445239868656,-1.03135052185687,3.66184026763188));
#72331=CARTESIAN_POINT('Ctrl Pts',(1.15961082610881,-1.03679121597966,3.66131154579171));
#72332=CARTESIAN_POINT('Ctrl Pts',(1.15027532746898,-1.04713473230588,3.66030551328904));
#72333=CARTESIAN_POINT('Ctrl Pts',(1.14578794270035,-1.05204299760754,3.65982778763336));
#72334=CARTESIAN_POINT('Ctrl Pts',(1.13473903634854,-1.06397365162221,3.65866535382958));
#72335=CARTESIAN_POINT('Ctrl Pts',(1.12814350943214,-1.0709644469436,3.65798316239319));
#72336=CARTESIAN_POINT('Ctrl Pts',(1.10341992854202,-1.09668783710814,3.65546691670175));
#72337=CARTESIAN_POINT('Ctrl Pts',(1.08488554087559,-1.11502615000068,3.65366096864965));
#72338=CARTESIAN_POINT('Ctrl Pts',(1.03438481289924,-1.16254051382225,3.64891931005681));
#72339=CARTESIAN_POINT('Ctrl Pts',(1.00164628811219,-1.19086423959588,3.64602609538907));
#72340=CARTESIAN_POINT('Ctrl Pts',(0.863663916002498,-1.30051783274062,
3.63434428573772));
#72341=CARTESIAN_POINT('Ctrl Pts',(0.749392523045323,-1.36955130673227,
3.62576409737399));
#72342=CARTESIAN_POINT('Ctrl Pts',(0.606238571196468,-1.43269224747661,
3.61499587623665));
#72343=CARTESIAN_POINT('Ctrl Pts',(0.584530395116345,-1.44168526306604,
3.61336430152426));
#72344=CARTESIAN_POINT('Ctrl Pts',(0.550169381495906,-1.45501631517865,
3.61077893934143));
#72345=CARTESIAN_POINT('Ctrl Pts',(0.537649522632959,-1.45968893832079,
3.60983637207233));
#72346=CARTESIAN_POINT('Ctrl Pts',(0.514229308578519,-1.46808757742567,
3.60807128554323));
#72347=CARTESIAN_POINT('Ctrl Pts',(0.503344685431386,-1.47185496273268,
3.60725021127794));
#72348=CARTESIAN_POINT('Ctrl Pts',(0.478913398223881,-1.48000842503088,
3.60540506670967));
#72349=CARTESIAN_POINT('Ctrl Pts',(0.465346486850612,-1.4843300183086,3.60437894917613));
#72350=CARTESIAN_POINT('Ctrl Pts',(0.424296143791934,-1.49678806814361,
3.60126864939008));
#72351=CARTESIAN_POINT('Ctrl Pts',(0.396646704143519,-1.50435133183752,
3.59916621384345));
#72352=CARTESIAN_POINT('Ctrl Pts',(0.296009361989527,-1.5289125775164,3.59148212640709));
#72353=CARTESIAN_POINT('Ctrl Pts',(0.222034226977328,-1.54139327201333,
3.58576790247432));
#72354=CARTESIAN_POINT('Ctrl Pts',(0.0543470526105254,-1.5573614745651,
3.57275426770513));
#72355=CARTESIAN_POINT('Ctrl Pts',(-0.0393752239906029,-1.55781230544449,
3.5654353864327));
#72356=CARTESIAN_POINT('Ctrl Pts',(-0.157805989479645,-1.54768178052438,
3.55645039637803));
#72357=CARTESIAN_POINT('Ctrl Pts',(-0.18298460958476,-1.5449072601812,3.55455643455861));
#72358=CARTESIAN_POINT('Ctrl Pts',(-0.217776743347928,-1.5402107525119,
3.55197154456373));
#72359=CARTESIAN_POINT('Ctrl Pts',(-0.227455295180025,-1.53881122106602,
3.55125595487535));
#72360=CARTESIAN_POINT('Ctrl Pts',(-0.243656874047524,-1.53631224708758,
3.55006462847682));
#72361=CARTESIAN_POINT('Ctrl Pts',(-0.250187139087899,-1.53526232129158,
3.54958624326111));
#72362=CARTESIAN_POINT('Ctrl Pts',(-0.263808173778837,-1.53298313119613,
3.54859240233945));
#72363=CARTESIAN_POINT('Ctrl Pts',(-0.2708974121799,-1.53174626840134,3.54807737001296));
#72364=CARTESIAN_POINT('Ctrl Pts',(-0.290026757988819,-1.52827179890672,
3.54669300923794));
#72365=CARTESIAN_POINT('Ctrl Pts',(-0.302049748108351,-1.52594108211685,
3.54582870159898));
#72366=CARTESIAN_POINT('Ctrl Pts',(-0.371852740508876,-1.51155204681196,
3.54083768130732));
#72367=CARTESIAN_POINT('Ctrl Pts',(-0.428943380458982,-1.49635335222618,
3.53686271390149));
#72368=CARTESIAN_POINT('Ctrl Pts',(-0.610687498550401,-1.43670776867674,
3.52415530077221));
#72369=CARTESIAN_POINT('Ctrl Pts',(-0.730556903895627,-1.37962097910419,
3.51564119168497));
#72370=CARTESIAN_POINT('Ctrl Pts',(-0.862351647997895,-1.2948086667663,
3.5049014408981));
#72371=CARTESIAN_POINT('Ctrl Pts',(-0.882626353682912,-1.28107394683488,
3.50320820619611));
#72372=CARTESIAN_POINT('Ctrl Pts',(-0.91466378750058,-1.25824917737933,
3.50045959811465));
#72373=CARTESIAN_POINT('Ctrl Pts',(-0.926635598489587,-1.2494587936889,
3.49941550962772));
#72374=CARTESIAN_POINT('Ctrl Pts',(-0.947706641671402,-1.23351783341402,
3.49754616460189));
#72375=CARTESIAN_POINT('Ctrl Pts',(-0.9568555263783,-1.22643451208446,3.49672358265607));
#72376=CARTESIAN_POINT('Ctrl Pts',(-0.97607960686687,-1.21120465154065,
3.49497123847157));
#72377=CARTESIAN_POINT('Ctrl Pts',(-0.986133688616471,-1.20303301540983,
3.49404051140951));
#72378=CARTESIAN_POINT('Ctrl Pts',(-1.01311425080504,-1.18053859725922,
3.49150305238647));
#72379=CARTESIAN_POINT('Ctrl Pts',(-1.02983786772414,-1.16597844612327,
3.4898867413495));
#72380=CARTESIAN_POINT('Ctrl Pts',(-1.06645428953764,-1.13269652526368,
3.48624707481798));
#72381=CARTESIAN_POINT('Ctrl Pts',(-1.08617625269331,-1.11379852410176,
3.48421683990996));
#72382=CARTESIAN_POINT('Ctrl Pts',(-1.14947531658844,-1.04986338233452,
3.47746426964904));
#72383=CARTESIAN_POINT('Ctrl Pts',(-1.19082585791133,-1.00271578881269,
3.47266244576171));
#72384=CARTESIAN_POINT('Ctrl Pts',(-1.29111794189993,-0.873383294073018,
3.46000500492474));
#72385=CARTESIAN_POINT('Ctrl Pts',(-1.34509916989565,-0.787714822142316,
3.45209782458507));
#72386=CARTESIAN_POINT('Ctrl Pts',(-1.39814664451044,-0.681956878310091,
3.44325004227776));
#72387=CARTESIAN_POINT('Ctrl Pts',(-1.40564122936845,-0.666372285728577,
3.44196843057678));
#72388=CARTESIAN_POINT('Ctrl Pts',(-1.41635984390617,-0.643097548266357,
3.44009040630299));
#72389=CARTESIAN_POINT('Ctrl Pts',(-1.41978416174851,-0.635501854075211,
3.43948311047828));
#72390=CARTESIAN_POINT('Ctrl Pts',(-1.42577175900896,-0.621930391532003,
3.43840842944615));
#72391=CARTESIAN_POINT('Ctrl Pts',(-1.42835879869708,-0.615965638412577,
3.4379396755894));
#72392=CARTESIAN_POINT('Ctrl Pts',(-1.43406490147965,-0.602580197367621,
3.43689571987182));
#72393=CARTESIAN_POINT('Ctrl Pts',(-1.43716385493171,-0.59515132330036,
3.43632170944422));
#72394=CARTESIAN_POINT('Ctrl Pts',(-1.44640359618374,-0.572508552946962,
3.43458745949149));
#72395=CARTESIAN_POINT('Ctrl Pts',(-1.45236172086018,-0.557220687073791,
3.43343738592663));
#72396=CARTESIAN_POINT('Ctrl Pts',(-1.48205480727729,-0.477317467350164,
3.42751968035562));
#72397=CARTESIAN_POINT('Ctrl Pts',(-1.50172605748703,-0.411265767278821,
3.42293994475575));
#72398=CARTESIAN_POINT('Ctrl Pts',(-1.54252708223655,-0.231406233733472,
3.41076701841973));
#72399=CARTESIAN_POINT('Ctrl Pts',(-1.5554514956748,-0.116208668896937,
3.40325199989059));
#72400=CARTESIAN_POINT('Ctrl Pts',(-1.55549986374249,-0.000651073801188791,
3.39533201070811));
#72401=CARTESIAN_POINT('Ctrl Pts',(-1.5555,-2.78355693781297E-11,3.25542335925836));
#72402=CARTESIAN_POINT('Ctrl Pts',(-1.55549999999891,-0.0607860708812731,
3.25945607524617));
#72403=CARTESIAN_POINT('Ctrl Pts',(-1.55193697213556,-0.121515943941803,
3.26353655937556));
#72404=CARTESIAN_POINT('Ctrl Pts',(-1.54284580338691,-0.198733706385335,
3.26889097315067));
#72405=CARTESIAN_POINT('Ctrl Pts',(-1.54058583546237,-0.215553949602213,
3.27006729424422));
#72406=CARTESIAN_POINT('Ctrl Pts',(-1.53622297308072,-0.244436185471864,
3.27210645413131));
#72407=CARTESIAN_POINT('Ctrl Pts',(-1.53425200647297,-0.256516739104691,
3.27296521076461));
#72408=CARTESIAN_POINT('Ctrl Pts',(-1.53022115015054,-0.279511764896393,
3.27461171291426));
#72409=CARTESIAN_POINT('Ctrl Pts',(-1.5281865185639,-0.290429936450797,
3.27539862007994));
#72410=CARTESIAN_POINT('Ctrl Pts',(-1.52369387412355,-0.313182547425268,
3.27704972294765));
#72411=CARTESIAN_POINT('Ctrl Pts',(-1.52121449704045,-0.325011951823233,
3.27791454974933));
#72412=CARTESIAN_POINT('Ctrl Pts',(-1.5154255758991,-0.351112770075724,
3.27983746802952));
#72413=CARTESIAN_POINT('Ctrl Pts',(-1.51205179272346,-0.365368584095339,
3.28089754711258));
#72414=CARTESIAN_POINT('Ctrl Pts',(-1.49956986812762,-0.414973379702481,
3.28462173942229));
#72415=CARTESIAN_POINT('Ctrl Pts',(-1.48941990867522,-0.450045136977735,
3.2873185771476));
#72416=CARTESIAN_POINT('Ctrl Pts',(-1.4386366890612,-0.604895778239368,
3.2995197546192));
#72417=CARTESIAN_POINT('Ctrl Pts',(-1.38472089335823,-0.719801133176935,
3.30942524276129));
#72418=CARTESIAN_POINT('Ctrl Pts',(-1.29124933733976,-0.868732283639018,
3.32295827192875));
#72419=CARTESIAN_POINT('Ctrl Pts',(-1.26300733993977,-0.909304196565685,
3.32671924801125));
#72420=CARTESIAN_POINT('Ctrl Pts',(-1.22542628259493,-0.958154514751454,
3.33128341996175));
#72421=CARTESIAN_POINT('Ctrl Pts',(-1.21785914857268,-0.967754497448563,
3.33218213374262));
#72422=CARTESIAN_POINT('Ctrl Pts',(-1.20558831904237,-0.982949873518572,
3.33360622512833));
#72423=CARTESIAN_POINT('Ctrl Pts',(-1.20095717706635,-0.988602808821515,
3.33413636232796));
#72424=CARTESIAN_POINT('Ctrl Pts',(-1.19191418881416,-0.999483669430574,
3.33515711940426));
#72425=CARTESIAN_POINT('Ctrl Pts',(-1.18750743581047,-1.00471544800308,
3.33564804897284));
#72426=CARTESIAN_POINT('Ctrl Pts',(-1.17636009579729,-1.01777397417979,
3.33687420330828));
#72427=CARTESIAN_POINT('Ctrl Pts',(-1.16957562827719,-1.02556316362537,
3.33760631658791));
#72428=CARTESIAN_POINT('Ctrl Pts',(-1.14389903790712,-1.05445600736992,
3.34032734573549));
#72429=CARTESIAN_POINT('Ctrl Pts',(-1.12450801161479,-1.07511137160182,
3.34228349171483));
#72430=CARTESIAN_POINT('Ctrl Pts',(-1.04057578437535,-1.15975898687436,
3.35040658346888));
#72431=CARTESIAN_POINT('Ctrl Pts',(-0.971051608072913,-1.21856497727376,
3.35632563994744));
#72432=CARTESIAN_POINT('Ctrl Pts',(-0.837968091971192,-1.31246767562476,
3.36706354742693));
#72433=CARTESIAN_POINT('Ctrl Pts',(-0.776347310742355,-1.34983157507516,
3.37184074195209));
#72434=CARTESIAN_POINT('Ctrl Pts',(-0.686150698456772,-1.39629761831886,
3.37877486756192));
#72435=CARTESIAN_POINT('Ctrl Pts',(-0.659559173426035,-1.40905334368822,
3.38081170985634));
#72436=CARTESIAN_POINT('Ctrl Pts',(-0.619272052132952,-1.4269884151098,
3.38389648679915));
#72437=CARTESIAN_POINT('Ctrl Pts',(-0.605838826215595,-1.43274320876832,
3.38492485435898));
#72438=CARTESIAN_POINT('Ctrl Pts',(-0.58139516340195,-1.44280964942013,
3.38679684844014));
#72439=CARTESIAN_POINT('Ctrl Pts',(-0.570412732423084,-1.44718669184952,
3.38763818861054));
#72440=CARTESIAN_POINT('Ctrl Pts',(-0.546570760135594,-1.45637534750301,
3.38946580551102));
#72441=CARTESIAN_POINT('Ctrl Pts',(-0.533695360963547,-1.46114269936617,
3.39045348242595));
#72442=CARTESIAN_POINT('Ctrl Pts',(-0.497938469113249,-1.47384668153679,
3.39319924249326));
#72443=CARTESIAN_POINT('Ctrl Pts',(-0.474933044732482,-1.48142000821229,
3.3949690538451));
#72444=CARTESIAN_POINT('Ctrl Pts',(-0.364130450539393,-1.51504978086094,
3.40351321751441));
#72445=CARTESIAN_POINT('Ctrl Pts',(-0.274336258379674,-1.53385179761166,
3.4105124170346));
#72446=CARTESIAN_POINT('Ctrl Pts',(-0.112505898868495,-1.55306891692159,
3.42312866137376));
#72447=CARTESIAN_POINT('Ctrl Pts',(-0.0410895024410422,-1.55659658445065,
3.42869220018023));
#72448=CARTESIAN_POINT('Ctrl Pts',(0.0542747113740685,-1.55473747928889,
3.43596661321126));
#72449=CARTESIAN_POINT('Ctrl Pts',(0.0782184428484231,-1.55371695573676,
3.43777950301424));
#72450=CARTESIAN_POINT('Ctrl Pts',(0.119408719021244,-1.55100665489163,
3.44086523003329));
#72451=CARTESIAN_POINT('Ctrl Pts',(0.136667897161868,-1.54958124582316,
3.44214816058904));
#72452=CARTESIAN_POINT('Ctrl Pts',(0.162205181816856,-1.54704213807897,
3.44402819226639));
#72453=CARTESIAN_POINT('Ctrl Pts',(0.170503248063316,-1.54614958814523,
3.44463622413106));
#72454=CARTESIAN_POINT('Ctrl Pts',(0.18476670296111,-1.54449916365417,3.44567597910792));
#72455=CARTESIAN_POINT('Ctrl Pts',(0.190735330327972,-1.5437734414532,3.4461094174091));
#72456=CARTESIAN_POINT('Ctrl Pts',(0.204785124664938,-1.54198240429226,
3.44712582511819));
#72457=CARTESIAN_POINT('Ctrl Pts',(0.212862319282244,-1.54088816056889,
3.44770718398428));
#72458=CARTESIAN_POINT('Ctrl Pts',(0.237063211504203,-1.53741565536871,
3.44944115072805));
#72459=CARTESIAN_POINT('Ctrl Pts',(0.253159105872497,-1.53484734930616,
3.45058386281324));
#72460=CARTESIAN_POINT('Ctrl Pts',(0.34785296670199,-1.51820744736787,3.45726026693833));
#72461=CARTESIAN_POINT('Ctrl Pts',(0.425323236034948,-1.49835207651838,
3.4625371778767));
#72462=CARTESIAN_POINT('Ctrl Pts',(0.573085353210863,-1.44808893689026,
3.47281806006367));
#72463=CARTESIAN_POINT('Ctrl Pts',(0.643331526199665,-1.41827788145873,
3.47781075825616));
#72464=CARTESIAN_POINT('Ctrl Pts',(0.7527509524352,-1.36203471361566,3.48608225237901));
#72465=CARTESIAN_POINT('Ctrl Pts',(0.793402484442948,-1.33876225616569,
3.48927378454031));
#72466=CARTESIAN_POINT('Ctrl Pts',(0.847507031028264,-1.30445758564444,
3.49372954065074));
#72467=CARTESIAN_POINT('Ctrl Pts',(0.861919034635415,-1.29498003712624,
3.49493752954185));
#72468=CARTESIAN_POINT('Ctrl Pts',(0.886232945305602,-1.27840515456497,
3.49701371329313));
#72469=CARTESIAN_POINT('Ctrl Pts',(0.896214738556411,-1.27142742602964,
3.49787736163097));
#72470=CARTESIAN_POINT('Ctrl Pts',(0.915100626648279,-1.25789242418635,
3.49953372879897));
#72471=CARTESIAN_POINT('Ctrl Pts',(0.924018783896665,-1.25135597775206,
3.50032560859368));
#72472=CARTESIAN_POINT('Ctrl Pts',(0.944827186580309,-1.23576100308039,
3.50219675450528));
#72473=CARTESIAN_POINT('Ctrl Pts',(0.956657850512842,-1.22662520653967,
3.50327899760884));
#72474=CARTESIAN_POINT('Ctrl Pts',(0.998908138827007,-1.19301593207937,
3.50721237466657));
#72475=CARTESIAN_POINT('Ctrl Pts',(1.0285330681755,-1.1675717188049,3.51010155075974));
#72476=CARTESIAN_POINT('Ctrl Pts',(1.15121702971096,-1.05390590887231,3.52265216421355));
#72477=CARTESIAN_POINT('Ctrl Pts',(1.23412544244741,-0.955481174912032,
3.53271408168902));
#72478=CARTESIAN_POINT('Ctrl Pts',(1.32072768779213,-0.822313467803962,
3.54491123362982));
#72479=CARTESIAN_POINT('Ctrl Pts',(1.33668667053844,-0.796109315406132,
3.54724824359846));
#72480=CARTESIAN_POINT('Ctrl Pts',(1.36210342901551,-0.751454066336237,
3.55110816399502));
#72481=CARTESIAN_POINT('Ctrl Pts',(1.37198599152631,-0.733255420732715,
3.55264839672875));
#72482=CARTESIAN_POINT('Ctrl Pts',(1.38561405705907,-0.706918639022424,
3.55482539992706));
#72483=CARTESIAN_POINT('Ctrl Pts',(1.38965681095889,-0.698937933885297,
3.55547837807798));
#72484=CARTESIAN_POINT('Ctrl Pts',(1.39660623815778,-0.684920538374741,
3.5566130301217));
#72485=CARTESIAN_POINT('Ctrl Pts',(1.39954308625618,-0.678899318384618,
3.55709648640158));
#72486=CARTESIAN_POINT('Ctrl Pts',(1.40589466997023,-0.665660700793265,
3.55815075710846));
#72487=CARTESIAN_POINT('Ctrl Pts',(1.40929284983607,-0.658435769465999,
3.55872057981965));
#72488=CARTESIAN_POINT('Ctrl Pts',(1.4189137830434,-0.637564780612528,3.56035167931683));
#72489=CARTESIAN_POINT('Ctrl Pts',(1.42499521590975,-0.62385403039611,3.56140490790846));
#72490=CARTESIAN_POINT('Ctrl Pts',(1.46981602417088,-0.518727601458954,
3.56935818113446));
#72491=CARTESIAN_POINT('Ctrl Pts',(1.4999267326764,-0.423866626399561,3.57584564312699));
#72492=CARTESIAN_POINT('Ctrl Pts',(1.53460624281731,-0.262468337359891,
3.58671343910008));
#72493=CARTESIAN_POINT('Ctrl Pts',(1.5443299749483,-0.197357595802677,3.5910522198203));
#72494=CARTESIAN_POINT('Ctrl Pts',(1.55341046346989,-0.0906003373645394,
3.59828803159756));
#72495=CARTESIAN_POINT('Ctrl Pts',(1.55527054292207,-0.0492497805970797,
3.60111929965253));
#72496=CARTESIAN_POINT('Ctrl Pts',(1.55556378546693,0.00865730581965027,
3.60515258545369));
#72497=CARTESIAN_POINT('Ctrl Pts',(1.55538387593836,0.0251912934767595,
3.60631190726155));
#72498=CARTESIAN_POINT('Ctrl Pts',(1.55461711938295,0.0537698425695558,
3.60833073347586));
#72499=CARTESIAN_POINT('Ctrl Pts',(1.55415371220992,0.0658164706205951,
3.6091863235393));
#72500=CARTESIAN_POINT('Ctrl Pts',(1.55291266181557,0.0905805154546697,
3.61095522025259));
#72501=CARTESIAN_POINT('Ctrl Pts',(1.55211869723514,0.103296160748277,3.61186897426871));
#72502=CARTESIAN_POINT('Ctrl Pts',(1.54966983852326,0.136042573045771,3.61423698789709));
#72503=CARTESIAN_POINT('Ctrl Pts',(1.54778279293913,0.156053022352627,3.61569837921906));
#72504=CARTESIAN_POINT('Ctrl Pts',(1.53696557978105,0.251031171078054,3.62270656400717));
#72505=CARTESIAN_POINT('Ctrl Pts',(1.52297436257048,0.32530869355889,3.62840792686284));
#72506=CARTESIAN_POINT('Ctrl Pts',(1.48047849683495,0.48575091670956,3.64116681057139));
#72507=CARTESIAN_POINT('Ctrl Pts',(1.44971730180168,0.571042823307886,3.64824790371171));
#72508=CARTESIAN_POINT('Ctrl Pts',(1.39505828000717,0.689177979869859,3.65820734170105));
#72509=CARTESIAN_POINT('Ctrl Pts',(1.3770278473173,0.724533509919141,3.66120683221527));
#72510=CARTESIAN_POINT('Ctrl Pts',(1.35217737854268,0.768975256494281,3.66496895312808));
#72511=CARTESIAN_POINT('Ctrl Pts',(1.34658482737159,0.778727121975855,3.66579392654287));
#72512=CARTESIAN_POINT('Ctrl Pts',(1.33729043893774,0.794534377858817,3.66712922826534));
#72513=CARTESIAN_POINT('Ctrl Pts',(1.33365213614556,0.800626367832799,3.66764336658298));
#72514=CARTESIAN_POINT('Ctrl Pts',(1.32673447595282,0.812031314815556,3.66860469112551));
#72515=CARTESIAN_POINT('Ctrl Pts',(1.32346459254547,0.81734980386155,3.66905248844869));
#72516=CARTESIAN_POINT('Ctrl Pts',(1.31464416675451,0.831504568502812,3.6702433393182));
#72517=CARTESIAN_POINT('Ctrl Pts',(1.30903646123255,0.840305118141006,3.67098276162416));
#72518=CARTESIAN_POINT('Ctrl Pts',(1.28744571292995,0.873448197808177,3.67376643751292));
#72519=CARTESIAN_POINT('Ctrl Pts',(1.27086771106949,0.897398321508173,3.67577594679725));
#72520=CARTESIAN_POINT('Ctrl Pts',(1.20020472960121,0.99359525315292,3.68390172411251));
#72521=CARTESIAN_POINT('Ctrl Pts',(1.14055223864123,1.06153960941272,3.68977907762025));
#72522=CARTESIAN_POINT('Ctrl Pts',(1.02361707230754,1.17341916484714,3.70044913488262));
#72523=CARTESIAN_POINT('Ctrl Pts',(0.968544708676698,1.2192719618557,3.70520059978927));
#72524=CARTESIAN_POINT('Ctrl Pts',(0.886598805241418,1.27843376908419,3.71210790562896));
#72525=CARTESIAN_POINT('Ctrl Pts',(0.862198093567136,1.2950152892425,3.71414534474061));
#72526=CARTESIAN_POINT('Ctrl Pts',(0.825024984598602,1.31875988489306,3.71723084399427));
#72527=CARTESIAN_POINT('Ctrl Pts',(0.812598039994556,1.32645326295926,3.71825932300566));
#72528=CARTESIAN_POINT('Ctrl Pts',(0.789926083913295,1.34005104553896,3.72013143419495));
#72529=CARTESIAN_POINT('Ctrl Pts',(0.779718534316432,1.34601597903946,3.72097277865108));
#72530=CARTESIAN_POINT('Ctrl Pts',(0.757513231743672,1.35865463514754,3.7228003065987));
#72531=CARTESIAN_POINT('Ctrl Pts',(0.745493219111438,1.36528698511159,3.72378788916717));
#72532=CARTESIAN_POINT('Ctrl Pts',(0.712035335391271,1.38317466461226,3.72653311690271));
#72533=CARTESIAN_POINT('Ctrl Pts',(0.690420884575803,1.39408943468898,3.72830248283838));
#72534=CARTESIAN_POINT('Ctrl Pts',(0.584838874199675,1.44434813142377,3.73693069837145));
#72535=CARTESIAN_POINT('Ctrl Pts',(0.497734093839646,1.4766291095255,3.74402075881413));
#72536=CARTESIAN_POINT('Ctrl Pts',(0.340205353866142,1.51947980109964,3.75666163577891));
#72537=CARTESIAN_POINT('Ctrl Pts',(0.270939086164993,1.53334640972864,3.76215675698973));
#72538=CARTESIAN_POINT('Ctrl Pts',(0.17735770129943,1.54553920806934,3.76935283956779));
#72539=CARTESIAN_POINT('Ctrl Pts',(0.153677707322813,1.54807315321948,3.77115404507967));
#72540=CARTESIAN_POINT('Ctrl Pts',(0.112772285398751,1.5515024094248,3.77422215753199));
#72541=CARTESIAN_POINT('Ctrl Pts',(0.0955732645950326,1.55265679751913,
3.77549901539143));
#72542=CARTESIAN_POINT('Ctrl Pts',(0.0700378400900962,1.55394476963077,
3.77737195661427));
#72543=CARTESIAN_POINT('Ctrl Pts',(0.0617144909625686,1.55429758289432,
3.77797885715571));
#72544=CARTESIAN_POINT('Ctrl Pts',(0.047380211490857,1.55478985948599,3.77901741770781));
#72545=CARTESIAN_POINT('Ctrl Pts',(0.0413708629452457,1.55496136510556,
3.77945078012098));
#72546=CARTESIAN_POINT('Ctrl Pts',(0.0271980468000013,1.55528363118929,
3.78046807750647));
#72547=CARTESIAN_POINT('Ctrl Pts',(0.0190341925520919,1.55540496806032,
3.78105038955749));
#72548=CARTESIAN_POINT('Ctrl Pts',(-0.00549853325664263,1.55557640196247,
3.78279025334399));
#72549=CARTESIAN_POINT('Ctrl Pts',(-0.0218682241375157,1.55543241980869,
3.78393780957672));
#72550=CARTESIAN_POINT('Ctrl Pts',(-0.111198544749674,1.55323606069066,
3.79014205518946));
#72551=CARTESIAN_POINT('Ctrl Pts',(-0.183956303259965,1.54630853016511,
3.79498634205472));
#72552=CARTESIAN_POINT('Ctrl Pts',(-0.32046191274894,1.52353532527263,3.80411338942916));
#72553=CARTESIAN_POINT('Ctrl Pts',(-0.384213540820087,1.50871980034343,
3.80839311112881));
#72554=CARTESIAN_POINT('Ctrl Pts',(-0.486029259238781,1.47818452842605,
3.81547230877433));
#72555=CARTESIAN_POINT('Ctrl Pts',(-0.524734320829272,1.46489162121172,
3.8182226094687));
#72556=CARTESIAN_POINT('Ctrl Pts',(-0.590915582161795,1.43920262194015,
3.82307105588552));
#72557=CARTESIAN_POINT('Ctrl Pts',(-0.618639226485134,1.42750506735872,
3.82514806300027));
#72558=CARTESIAN_POINT('Ctrl Pts',(-0.659398207977537,1.4088970950988,3.82828141712173));
#72559=CARTESIAN_POINT('Ctrl Pts',(-0.672703696651877,1.40259286017864,
3.82931724115352));
#72560=CARTESIAN_POINT('Ctrl Pts',(-0.696534381742325,1.39088462388856,
3.83119711285093));
#72561=CARTESIAN_POINT('Ctrl Pts',(-0.707091339055635,1.38554754736967,
3.83203878252375));
#72562=CARTESIAN_POINT('Ctrl Pts',(-0.729694229951577,1.37379504373212,
3.83386065822316));
#72563=CARTESIAN_POINT('Ctrl Pts',(-0.741718575976136,1.36734049286904,
3.83484219197334));
#72564=CARTESIAN_POINT('Ctrl Pts',(-0.774503763128134,1.349182020093,3.83755336856953));
#72565=CARTESIAN_POINT('Ctrl Pts',(-0.795082187738909,1.33715833051186,
3.83929426122792));
#72566=CARTESIAN_POINT('Ctrl Pts',(-0.907056260347639,1.26823469007577,
3.84899121052981));
#72567=CARTESIAN_POINT('Ctrl Pts',(-0.992615230169811,1.20244641552962,
3.85727124457528));
#72568=CARTESIAN_POINT('Ctrl Pts',(-1.11422359903628,1.08705501331505,3.87027076716141));
#72569=CARTESIAN_POINT('Ctrl Pts',(-1.15533794183563,1.04325345832949,3.87492800745078));
#72570=CARTESIAN_POINT('Ctrl Pts',(-1.21436578555386,0.972585819178756,
3.88193121779223));
#72571=CARTESIAN_POINT('Ctrl Pts',(-1.23414858373607,0.94735688093723,3.88434067756427));
#72572=CARTESIAN_POINT('Ctrl Pts',(-1.25935734167289,0.913076940659836,
3.88747873809432));
#72573=CARTESIAN_POINT('Ctrl Pts',(-1.2654899594665,0.90455823046206,3.88824783097148));
#72574=CARTESIAN_POINT('Ctrl Pts',(-1.27553416094645,0.890303898549334,
3.88951619744513));
#72575=CARTESIAN_POINT('Ctrl Pts',(-1.27949434271589,0.88460310974975,3.89001860838951));
#72576=CARTESIAN_POINT('Ctrl Pts',(-1.28701911004849,0.873614742561962,
3.89097747143102));
#72577=CARTESIAN_POINT('Ctrl Pts',(-1.29058953553784,0.868331482058339,
3.89143434315744));
#72578=CARTESIAN_POINT('Ctrl Pts',(-1.30031456586995,0.853748578907524,
3.89268448026577));
#72579=CARTESIAN_POINT('Ctrl Pts',(-1.30640196328723,0.84440424888625,3.89347343034902));
#72580=CARTESIAN_POINT('Ctrl Pts',(-1.33129693310522,0.805276017497543,
3.896730705872));
#72581=CARTESIAN_POINT('Ctrl Pts',(-1.34919210545048,0.774920704266457,
3.8991473029384));
#72582=CARTESIAN_POINT('Ctrl Pts',(-1.40695071097731,0.668868691062298,
3.90731246306713));
#72583=CARTESIAN_POINT('Ctrl Pts',(-1.44159678355945,0.590505159647553,
3.91288389473558));
#72584=CARTESIAN_POINT('Ctrl Pts',(-1.49523176312639,0.435854322458862,
3.92368256333216));
#72585=CARTESIAN_POINT('Ctrl Pts',(-1.51523471972271,0.360206433021615,
3.9288826851764));
#72586=CARTESIAN_POINT('Ctrl Pts',(-1.53380238538461,0.259992883848979,
3.93589797543827));
#72587=CARTESIAN_POINT('Ctrl Pts',(-1.53759858512539,0.236509077635695,
3.93755012244972));
#72588=CARTESIAN_POINT('Ctrl Pts',(-1.54270321353632,0.199572961961079,
3.94016653464031));
#72589=CARTESIAN_POINT('Ctrl Pts',(-1.54437744070055,0.186174306275306,
3.94111928775718));
#72590=CARTESIAN_POINT('Ctrl Pts',(-1.54719252055082,0.160984043077589,
3.94291821874048));
#72591=CARTESIAN_POINT('Ctrl Pts',(-1.54837351793495,0.149197830003592,
3.94376306673269));
#72592=CARTESIAN_POINT('Ctrl Pts',(-1.55073858002753,0.122527630868944,
3.94568250085911));
#72593=CARTESIAN_POINT('Ctrl Pts',(-1.55184316274791,0.107637973202424,
3.94675950004294));
#72594=CARTESIAN_POINT('Ctrl Pts',(-1.55459560178378,0.0615518718819224,
3.95011086755889));
#72595=CARTESIAN_POINT('Ctrl Pts',(-1.55551806522174,0.0303217476106547,
3.95240736132449));
#72596=CARTESIAN_POINT('Ctrl Pts',(-1.55549973205925,-0.000912997037756428,
3.95473109533655));
#72597=CARTESIAN_POINT('Origin',(0.,0.,-1.2940562256037));
#72598=CARTESIAN_POINT('',(-1.5555,1.04251457910392E-10,4.79368285916456));
#72599=CARTESIAN_POINT('',(-1.55731034188284,-0.00109208591688013,4.65637838558307));
#72600=CARTESIAN_POINT('',(-1.5555,-1.46451138874614E-13,-1.2940562256037));
#72601=CARTESIAN_POINT('',(-1.55549960461727,0.00128691399081897,4.79358337162685));
#72602=CARTESIAN_POINT('Ctrl Pts',(-1.5555,1.04251457910392E-10,4.79368285916456));
#72603=CARTESIAN_POINT('Ctrl Pts',(-1.55549999999997,0.000428530864078361,
4.79364965059424));
#72604=CARTESIAN_POINT('Ctrl Pts',(-1.55549982291353,0.000857065800172565,
4.79361644270702));
#72605=CARTESIAN_POINT('Ctrl Pts',(-1.55549946873031,0.00128560480406378,
4.79358323553491));
#72606=CARTESIAN_POINT('Ctrl Pts',(-1.55549946766297,0.00128689557921172,
4.7935831355137));
#72607=CARTESIAN_POINT('Ctrl Pts',(-1.55544058013389,0.0724655689735681,
4.78806755282632));
#72608=CARTESIAN_POINT('Ctrl Pts',(-1.55049609564374,0.143566382762285,
4.78258209313387));
#72609=CARTESIAN_POINT('Ctrl Pts',(-1.53939498818184,0.223456484097864,
4.77659888361676));
#72610=CARTESIAN_POINT('Ctrl Pts',(-1.53800759084097,0.232814070963751,
4.77590096791649));
#72611=CARTESIAN_POINT('Ctrl Pts',(-1.53548389434461,0.248827319965951,
4.77471227496371));
#72612=CARTESIAN_POINT('Ctrl Pts',(-1.53438948968821,0.255489184388934,
4.77421942557452));
#72613=CARTESIAN_POINT('Ctrl Pts',(-1.53213016146775,0.26870375559159,4.77324540404521));
#72614=CARTESIAN_POINT('Ctrl Pts',(-1.53096647814555,0.275256589324356,
4.77276417957794));
#72615=CARTESIAN_POINT('Ctrl Pts',(-1.52844340448471,0.288953078417005,
4.77176228213858));
#72616=CARTESIAN_POINT('Ctrl Pts',(-1.52707593262449,0.296094957746632,
4.77124205807168));
#72617=CARTESIAN_POINT('Ctrl Pts',(-1.52320297555013,0.315581368821034,
4.76982801046675));
#72618=CARTESIAN_POINT('Ctrl Pts',(-1.52059748709042,0.327905800653344,
4.76893958132191));
#72619=CARTESIAN_POINT('Ctrl Pts',(-1.50395760161377,0.402147108094241,
4.7636159120303));
#72620=CARTESIAN_POINT('Ctrl Pts',(-1.48629126669349,0.463196606322958,
4.75935575163557));
#72621=CARTESIAN_POINT('Ctrl Pts',(-1.43308249456964,0.612235503630998,
4.74886735773477));
#72622=CARTESIAN_POINT('Ctrl Pts',(-1.39313960679404,0.698369260059456,
4.74271505038869));
#72623=CARTESIAN_POINT('Ctrl Pts',(-1.33317855207121,0.801766215674174,
4.73470040271835));
#72624=CARTESIAN_POINT('Ctrl Pts',(-1.32023942043558,0.822898474586927,
4.73302743517984));
#72625=CARTESIAN_POINT('Ctrl Pts',(-1.28955429604292,0.870425795424214,
4.72917218819553));
#72626=CARTESIAN_POINT('Ctrl Pts',(-1.27149303922234,0.896602789783632,
4.72698082756456));
#72627=CARTESIAN_POINT('Ctrl Pts',(-1.24379738766127,0.934222100918189,
4.72371720037957));
#72628=CARTESIAN_POINT('Ctrl Pts',(-1.23477927421008,0.946109397475254,
4.72266843820484));
#72629=CARTESIAN_POINT('Ctrl Pts',(-1.21846219984213,0.966987159740279,
4.72079390816695));
#72630=CARTESIAN_POINT('Ctrl Pts',(-1.21123112563465,0.976029429162663,
4.71997087095333));
#72631=CARTESIAN_POINT('Ctrl Pts',(-1.19572019104251,0.994987606549854,
4.71822090312841));
#72632=CARTESIAN_POINT('Ctrl Pts',(-1.18741643820315,1.004882727508,4.71729304286907));
#72633=CARTESIAN_POINT('Ctrl Pts',(-1.16464814530916,1.03133815095531,4.71477206780274));
#72634=CARTESIAN_POINT('Ctrl Pts',(-1.14995464003247,1.04769648180703,4.7131695860798));
#72635=CARTESIAN_POINT('Ctrl Pts',(-1.04893129507252,1.15548008142694,4.70230640276321));
#72636=CARTESIAN_POINT('Ctrl Pts',(-0.952150796382376,1.23644148308719,
4.69257832216735));
#72637=CARTESIAN_POINT('Ctrl Pts',(-0.790028110168338,1.34164144803684,
4.67759851604862));
#72638=CARTESIAN_POINT('Ctrl Pts',(-0.731002016487151,1.37469416185448,
4.67238443315003));
#72639=CARTESIAN_POINT('Ctrl Pts',(-0.655318630388377,1.41081631425189,
4.66612549217126));
#72640=CARTESIAN_POINT('Ctrl Pts',(-0.640519365806971,1.4175966201511,4.66492108803867));
#72641=CARTESIAN_POINT('Ctrl Pts',(-0.618269149151414,1.42737097327888,
4.66314200798544));
#72642=CARTESIAN_POINT('Ctrl Pts',(-0.610897575785989,1.43054143444812,
4.66255771762055));
#72643=CARTESIAN_POINT('Ctrl Pts',(-0.598108061055424,1.43592522165312,
4.66155322531566));
#72644=CARTESIAN_POINT('Ctrl Pts',(-0.592701828646886,1.43816516449059,
4.6611314770918));
#72645=CARTESIAN_POINT('Ctrl Pts',(-0.579865363989483,1.44339896564495,
4.66013680362941));
#72646=CARTESIAN_POINT('Ctrl Pts',(-0.57242448301163,1.44636600940417,4.65956547380703));
#72647=CARTESIAN_POINT('Ctrl Pts',(-0.549862417074104,1.4551612194953,4.65784794487773));
#72648=CARTESIAN_POINT('Ctrl Pts',(-0.534672203317368,1.46081091918562,
4.65671162754101));
#72649=CARTESIAN_POINT('Ctrl Pts',(-0.447708121886464,1.49161713745868,
4.65030435190047));
#72650=CARTESIAN_POINT('Ctrl Pts',(-0.37424517945838,1.51172342252536,4.64526639207819));
#72651=CARTESIAN_POINT('Ctrl Pts',(-0.220104360418011,1.54197826773324,
4.63491506005674));
#72652=CARTESIAN_POINT('Ctrl Pts',(-0.139517540184281,1.55134681465798,
4.62961813671609));
#72653=CARTESIAN_POINT('Ctrl Pts',(-0.0271220723330674,1.55558188772191,
4.62205426207034));
#72654=CARTESIAN_POINT('Ctrl Pts',(0.00435269819245649,1.55581215854594,
4.61991805171286));
#72655=CARTESIAN_POINT('Ctrl Pts',(0.0604927116598626,1.55451933947443,
4.61605794081641));
#72656=CARTESIAN_POINT('Ctrl Pts',(0.0851558335524943,1.55336348381762,
4.61434497984134));
#72657=CARTESIAN_POINT('Ctrl Pts',(0.123216183101447,1.55067064853022,4.61166933840946));
#72658=CARTESIAN_POINT('Ctrl Pts',(0.136639181108704,1.54954554685792,4.61071950996269));
#72659=CARTESIAN_POINT('Ctrl Pts',(0.161503126375638,1.54713590230741,4.60894774831573));
#72660=CARTESIAN_POINT('Ctrl Pts',(0.172947775880819,1.54589838403586,4.60812735120939));
#72661=CARTESIAN_POINT('Ctrl Pts',(0.198382823785304,1.54286209801361,4.60629268879579));
#72662=CARTESIAN_POINT('Ctrl Pts',(0.21236445512609,1.54099984168584,4.60527648483814));
#72663=CARTESIAN_POINT('Ctrl Pts',(0.247946578775081,1.53576711720121,4.60266983205447));
#72664=CARTESIAN_POINT('Ctrl Pts',(0.269504219739021,1.53213104201285,4.60107119621729));
#72665=CARTESIAN_POINT('Ctrl Pts',(0.384624600074086,1.5102092668917,4.59242626857688));
#72666=CARTESIAN_POINT('Ctrl Pts',(0.476418858607355,1.48380843137654,4.58512993525905));
#72667=CARTESIAN_POINT('Ctrl Pts',(0.629771040168057,1.42399843674715,4.57237747368261));
#72668=CARTESIAN_POINT('Ctrl Pts',(0.692583859762,1.39452909629116,4.56698137543402));
#72669=CARTESIAN_POINT('Ctrl Pts',(0.783492461604464,1.34421599173406,4.55906142809076));
#72670=CARTESIAN_POINT('Ctrl Pts',(0.813196589775267,1.32645723849003,4.55645551301168));
#72671=CARTESIAN_POINT('Ctrl Pts',(0.851199896223808,1.30197980126336,4.55311995814195));
#72672=CARTESIAN_POINT('Ctrl Pts',(0.860055029746958,1.29614737924565,4.55234264328249));
#72673=CARTESIAN_POINT('Ctrl Pts',(0.874525238338738,1.2864029963958,4.55107314443031));
#72674=CARTESIAN_POINT('Ctrl Pts',(0.880175222084871,1.2825438183348,4.55057764340932));
#72675=CARTESIAN_POINT('Ctrl Pts',(0.891530391551703,1.2746773757119,4.54958246338089));
#72676=CARTESIAN_POINT('Ctrl Pts',(0.897234444896402,1.27066880312863,4.54908288430815));
#72677=CARTESIAN_POINT('Ctrl Pts',(0.912037844099199,1.26011619911593,4.54778666563331));
#72678=CARTESIAN_POINT('Ctrl Pts',(0.921093954489292,1.25351179118699,4.54699400090288));
#72679=CARTESIAN_POINT('Ctrl Pts',(0.960279530654349,1.22428066806721,4.54356164736946));
#72680=CARTESIAN_POINT('Ctrl Pts',(0.989655198539604,1.20065942562923,4.54098191101041));
#72681=CARTESIAN_POINT('Ctrl Pts',(1.0816614319476,1.12100259481197,4.53277290929936));
#72682=CARTESIAN_POINT('Ctrl Pts',(1.14062080283282,1.06095439050667,4.52730148108551));
#72683=CARTESIAN_POINT('Ctrl Pts',(1.23895514859959,0.943079208231,4.51717441324297));
#72684=CARTESIAN_POINT('Ctrl Pts',(1.27983646298868,0.886806317016336,4.51255384436832));
#72685=CARTESIAN_POINT('Ctrl Pts',(1.33193256132645,0.803954133982975,4.50585710819311));
#72686=CARTESIAN_POINT('Ctrl Pts',(1.34638593216738,0.779507117765701,4.50389383504533));
#72687=CARTESIAN_POINT('Ctrl Pts',(1.36704546296176,0.74227237509779,4.50091362883222));
#72688=CARTESIAN_POINT('Ctrl Pts',(1.37375920408996,0.729772020652281,4.49991479091137));
#72689=CARTESIAN_POINT('Ctrl Pts',(1.38561010704412,0.706963566862782,4.49809427326667));
#72690=CARTESIAN_POINT('Ctrl Pts',(1.39080563561327,0.696686819519434,4.49727472650226));
#72691=CARTESIAN_POINT('Ctrl Pts',(1.40179992371849,0.67432694805489,4.49549259676014));
#72692=CARTESIAN_POINT('Ctrl Pts',(1.40755753466916,0.662224753922708,4.49452865776503));
#72693=CARTESIAN_POINT('Ctrl Pts',(1.42305210973537,0.628540759900732,4.49184663449693));
#72694=CARTESIAN_POINT('Ctrl Pts',(1.43245342776712,0.606809572133582,4.49011729399258));
#72695=CARTESIAN_POINT('Ctrl Pts',(1.48150617338333,0.485924592730933,4.48049739876968));
#72696=CARTESIAN_POINT('Ctrl Pts',(1.51135484391414,0.383121395576644,4.47228752974989));
#72697=CARTESIAN_POINT('Ctrl Pts',(1.54138264068597,0.217868225321859,4.45926116323008));
#72698=CARTESIAN_POINT('Ctrl Pts',(1.54876205009271,0.157047278119586,4.45450889172274));
#72699=CARTESIAN_POINT('Ctrl Pts',(1.55452907558365,0.0637299916082448,
4.44739621538762));
#72700=CARTESIAN_POINT('Ctrl Pts',(1.55551697158987,0.0314558088291498,
4.44496921151467));
#72701=CARTESIAN_POINT('Ctrl Pts',(1.55549426158034,-0.0111900230157694,
4.44182436116208));
#72702=CARTESIAN_POINT('Ctrl Pts',(1.55538520993825,-0.021551769590433,
4.44106510407128));
#72703=CARTESIAN_POINT('Ctrl Pts',(1.55503327193343,-0.0387028079584424,
4.4398172237534));
#72704=CARTESIAN_POINT('Ctrl Pts',(1.55484944367305,-0.0454928359895294,
4.43932549492275));
#72705=CARTESIAN_POINT('Ctrl Pts',(1.5544137180105,-0.0584493484662753,
4.43839185321851));
#72706=CARTESIAN_POINT('Ctrl Pts',(1.55416959387067,-0.0646158659789873,
4.43794949511199));
#72707=CARTESIAN_POINT('Ctrl Pts',(1.55340479991883,-0.0814057703177556,
4.43675010586722));
#72708=CARTESIAN_POINT('Ctrl Pts',(1.55281185106637,-0.092025777352445,
4.43599696481035));
#72709=CARTESIAN_POINT('Ctrl Pts',(1.54999796374082,-0.134577359051323,
4.43299835537197));
#72710=CARTESIAN_POINT('Ctrl Pts',(1.54690045637132,-0.166445423374152,
4.43079557698552));
#72711=CARTESIAN_POINT('Ctrl Pts',(1.53019177512169,-0.296510002970112,
4.4218981528355));
#72712=CARTESIAN_POINT('Ctrl Pts',(1.50819324691509,-0.39339711772293,4.41547621216647));
#72713=CARTESIAN_POINT('Ctrl Pts',(1.45779045323088,-0.546105395332603,
4.4048429632506));
#72714=CARTESIAN_POINT('Ctrl Pts',(1.43499523353654,-0.603466388729109,
4.40072591498259));
#72715=CARTESIAN_POINT('Ctrl Pts',(1.39694279477168,-0.684778199914722,
4.39458096007229));
#72716=CARTESIAN_POINT('Ctrl Pts',(1.38434129430823,-0.709907999815673,
4.39263705199916));
#72717=CARTESIAN_POINT('Ctrl Pts',(1.36439039510398,-0.747140482757923,
4.38968031979611));
#72718=CARTESIAN_POINT('Ctrl Pts',(1.35754490063065,-0.759507650105684,
4.38868515507894));
#72719=CARTESIAN_POINT('Ctrl Pts',(1.34481986832163,-0.781775104078759,
4.38686846884788));
#72720=CARTESIAN_POINT('Ctrl Pts',(1.33899707302187,-0.791706774612295,
4.38604903619909));
#72721=CARTESIAN_POINT('Ctrl Pts',(1.32613625893716,-0.813095100785673,
4.38426383911097));
#72722=CARTESIAN_POINT('Ctrl Pts',(1.31905891396428,-0.824526882871743,
4.38329668194154));
#72723=CARTESIAN_POINT('Ctrl Pts',(1.29900310482698,-0.85600313413033,4.38059652387313));
#72724=CARTESIAN_POINT('Ctrl Pts',(1.28571043326944,-0.875841878720963,
4.37885201729909));
#72725=CARTESIAN_POINT('Ctrl Pts',(1.21411933108679,-0.977545027687594,
4.36967825076646));
#72726=CARTESIAN_POINT('Ctrl Pts',(1.14845354541913,-1.05391075698835,4.36197062707782));
#72727=CARTESIAN_POINT('Ctrl Pts',(1.02854554932362,-1.16874846038424,4.34909950599572));
#72728=CARTESIAN_POINT('Ctrl Pts',(0.978372659379748,-1.21106010396637,
4.34400092813692));
#72729=CARTESIAN_POINT('Ctrl Pts',(0.90736814428987,-1.26363853549167,4.3372720926326));
#72730=CARTESIAN_POINT('Ctrl Pts',(0.888762152577831,-1.27679334611285,
4.33555075944941));
#72731=CARTESIAN_POINT('Ctrl Pts',(0.856107167031115,-1.2988211927873,4.33260934071207));
#72732=CARTESIAN_POINT('Ctrl Pts',(0.842192887064523,-1.307886528707,4.33138011845895));
#72733=CARTESIAN_POINT('Ctrl Pts',(0.821289749962543,-1.32103323057204,
4.32957195685271));
#72734=CARTESIAN_POINT('Ctrl Pts',(0.814410437454078,-1.32528536429933,
4.32898295788945));
#72735=CARTESIAN_POINT('Ctrl Pts',(0.802494214796415,-1.33252300570012,
4.32797354011803));
#72736=CARTESIAN_POINT('Ctrl Pts',(0.7974732780799,-1.33553393802237,4.32755152293823));
#72737=CARTESIAN_POINT('Ctrl Pts',(0.785593818980809,-1.34256687368055,
4.32656077942254));
#72738=CARTESIAN_POINT('Ctrl Pts',(0.778721310588699,-1.34656473536779,
4.32599359626356));
#72739=CARTESIAN_POINT('Ctrl Pts',(0.758016350942587,-1.35839764856804,
4.32430174549617));
#72740=CARTESIAN_POINT('Ctrl Pts',(0.744093639891219,-1.36607381438885,
4.32318653094773));
#72741=CARTESIAN_POINT('Ctrl Pts',(0.628759153273436,-1.4273758440877,4.3141102729709));
#72742=CARTESIAN_POINT('Ctrl Pts',(0.521803467995819,-1.46985329939973,
4.30669296867691));
#72743=CARTESIAN_POINT('Ctrl Pts',(0.345193773878057,-1.51825438254038,
4.29460866749738));
#72744=CARTESIAN_POINT('Ctrl Pts',(0.278138769947949,-1.53195709685333,
4.29005945003893));
#72745=CARTESIAN_POINT('Ctrl Pts',(0.182313848869221,-1.54503905716723,
4.28344145935312));
#72746=CARTESIAN_POINT('Ctrl Pts',(0.154125464502821,-1.54810503427325,
4.28148123655028));
#72747=CARTESIAN_POINT('Ctrl Pts',(0.111736487475051,-1.55154642016391,
4.27850472686826));
#72748=CARTESIAN_POINT('Ctrl Pts',(0.0975878925415331,-1.55250053659826,
4.27750646615948));
#72749=CARTESIAN_POINT('Ctrl Pts',(0.0719302910522939,-1.55387865569258,
4.27568655213387));
#72750=CARTESIAN_POINT('Ctrl Pts',(0.0604257337587508,-1.55436854092594,
4.2748670248509));
#72751=CARTESIAN_POINT('Ctrl Pts',(0.03551516501753,-1.55515231153641,4.27308442068608));
#72752=CARTESIAN_POINT('Ctrl Pts',(0.0221087659811843,-1.555400662389,4.27211998207671));
#72753=CARTESIAN_POINT('Ctrl Pts',(-0.0150056485346113,-1.55560827761934,
4.26943514643759));
#72754=CARTESIAN_POINT('Ctrl Pts',(-0.0387111595504639,-1.55519889861018,
4.26770345465379));
#72755=CARTESIAN_POINT('Ctrl Pts',(-0.168413921750909,-1.54999184722815,
4.258131150699));
#72756=CARTESIAN_POINT('Ctrl Pts',(-0.273698966111196,-1.53490038864118,
4.24997585058189));
#72757=CARTESIAN_POINT('Ctrl Pts',(-0.436441819911803,-1.49428966386498,
4.23696737218199));
#72758=CARTESIAN_POINT('Ctrl Pts',(-0.495336049373005,-1.47581366986062,
4.23217882310577));
#72759=CARTESIAN_POINT('Ctrl Pts',(-0.583279118989948,-1.44236491499426,
4.22502009047497));
#72760=CARTESIAN_POINT('Ctrl Pts',(-0.613213100195878,-1.4298954977857,
4.22258245028437));
#72761=CARTESIAN_POINT('Ctrl Pts',(-0.652187203406116,-1.41221095269598,
4.21942620939261));
#72762=CARTESIAN_POINT('Ctrl Pts',(-0.661593718060217,-1.40782871512499,
4.21866583671004));
#72763=CARTESIAN_POINT('Ctrl Pts',(-0.677086589934567,-1.40042142764064,
4.21741662378376));
#72764=CARTESIAN_POINT('Ctrl Pts',(-0.683198102406986,-1.39745010091746,
4.21692466493895));
#72765=CARTESIAN_POINT('Ctrl Pts',(-0.695592116388903,-1.3913235699585,
4.21592894259169));
#72766=CARTESIAN_POINT('Ctrl Pts',(-0.701873045912329,-1.38816566064146,
4.21542535232761));
#72767=CARTESIAN_POINT('Ctrl Pts',(-0.718351764157794,-1.37974009422637,
4.2141062276919));
#72768=CARTESIAN_POINT('Ctrl Pts',(-0.728513267443662,-1.37440184242834,
4.21329493117076));
#72769=CARTESIAN_POINT('Ctrl Pts',(-0.774146676596818,-1.34978042252123,
4.20965694410608));
#72770=CARTESIAN_POINT('Ctrl Pts',(-0.808921954787956,-1.3292314248599,
4.20689931511098));
#72771=CARTESIAN_POINT('Ctrl Pts',(-0.969469307350372,-1.22572500949163,
4.19404694897266));
#72772=CARTESIAN_POINT('Ctrl Pts',(-1.08354755812998,-1.12614435499403,
4.18446716649846));
#72773=CARTESIAN_POINT('Ctrl Pts',(-1.19992863481184,-0.990227971589131,
4.17222188996328));
#72774=CARTESIAN_POINT('Ctrl Pts',(-1.2177335920345,-0.968248363096394,
4.1702662623625));
#72775=CARTESIAN_POINT('Ctrl Pts',(-1.24354309853171,-0.934548841333982,
4.16729532207042));
#72776=CARTESIAN_POINT('Ctrl Pts',(-1.25200322627368,-0.923184094619307,
4.1662979318824));
#72777=CARTESIAN_POINT('Ctrl Pts',(-1.2670554074814,-0.90237654151281,4.16447892712253));
#72778=CARTESIAN_POINT('Ctrl Pts',(-1.27370015415414,-0.892972974138926,
4.16365942813738));
#72779=CARTESIAN_POINT('Ctrl Pts',(-1.28786133414336,-0.872452575355153,
4.16187610317046));
#72780=CARTESIAN_POINT('Ctrl Pts',(-1.29533947603909,-0.861310590357592,
4.1609109068083));
#72781=CARTESIAN_POINT('Ctrl Pts',(-1.3156542762789,-0.830179722488268,
4.15822180361493));
#72782=CARTESIAN_POINT('Ctrl Pts',(-1.32817810994251,-0.80999218461234,
4.15648654346149));
#72783=CARTESIAN_POINT('Ctrl Pts',(-1.39348787786544,-0.69912782452935,
4.14699739623331));
#72784=CARTESIAN_POINT('Ctrl Pts',(-1.4374497295426,-0.603588467139476,
4.13893673535704));
#72785=CARTESIAN_POINT('Ctrl Pts',(-1.49171395958147,-0.445277598252304,
4.12595855220623));
#72786=CARTESIAN_POINT('Ctrl Pts',(-1.50839238102825,-0.385014066723115,
4.12110617965291));
#72787=CARTESIAN_POINT('Ctrl Pts',(-1.52820213981031,-0.291967360627213,
4.11386659099218));
#72788=CARTESIAN_POINT('Ctrl Pts',(-1.53399545860567,-0.259817285894605,
4.11141040467801));
#72789=CARTESIAN_POINT('Ctrl Pts',(-1.54029408603605,-0.21721553247269,
4.10823431896477));
#72790=CARTESIAN_POINT('Ctrl Pts',(-1.54171231715226,-0.206909656570853,
4.10747201412035));
#72791=CARTESIAN_POINT('Ctrl Pts',(-1.54388657416256,-0.189843995991795,
4.10622049218401));
#72792=CARTESIAN_POINT('Ctrl Pts',(-1.54470182658022,-0.183092244570194,
4.10572813396047));
#72793=CARTESIAN_POINT('Ctrl Pts',(-1.54626892851389,-0.169357525464194,
4.10473250011569));
#72794=CARTESIAN_POINT('Ctrl Pts',(-1.54701781528832,-0.162374428846498,
4.10422938914682));
#72795=CARTESIAN_POINT('Ctrl Pts',(-1.5488627337859,-0.143998189223383,
4.10291299864447));
#72796=CARTESIAN_POINT('Ctrl Pts',(-1.54988038597653,-0.132597346281921,
4.10210392525345));
#72797=CARTESIAN_POINT('Ctrl Pts',(-1.55389503583024,-0.081223310025769,
4.09848818386706));
#72798=CARTESIAN_POINT('Ctrl Pts',(-1.55547235254112,-0.0411509399644201,
4.09574958078276));
#72799=CARTESIAN_POINT('Ctrl Pts',(-1.55549987993421,-0.000705786165981674,
4.09302759314932));
#72800=CARTESIAN_POINT('Ctrl Pts',(-1.55550000000001,-0.000352891711195591,
4.09300384633061));
#72801=CARTESIAN_POINT('Ctrl Pts',(-1.5555,3.27936543916168E-11,4.09298010292487));
#72802=CARTESIAN_POINT('Ctrl Pts',(-1.55549973205925,-0.000912997037756428,
3.95473109533655));
#72803=CARTESIAN_POINT('Ctrl Pts',(-1.55547442119289,-0.0440358596668717,
3.95793925547094));
#72804=CARTESIAN_POINT('Ctrl Pts',(-1.55365590759048,-0.087135391172154,
3.96119733324091));
#72805=CARTESIAN_POINT('Ctrl Pts',(-1.54478301234824,-0.192849268283468,
3.96930457206507));
#72806=CARTESIAN_POINT('Ctrl Pts',(-1.53571114152528,-0.255217351088432,
3.97419014007038));
#72807=CARTESIAN_POINT('Ctrl Pts',(-1.50717787626475,-0.392353145500239,
3.98504927277714));
#72808=CARTESIAN_POINT('Ctrl Pts',(-1.48587679832324,-0.466582170598623,
3.9910076496691));
#72809=CARTESIAN_POINT('Ctrl Pts',(-1.4546499626027,-0.551128654226623,
3.99769308726693));
#72810=CARTESIAN_POINT('Ctrl Pts',(-1.44999215891354,-0.563269097227302,
3.99865040418915));
#72811=CARTESIAN_POINT('Ctrl Pts',(-1.44241760503056,-0.582295095615148,
4.00014489916246));
#72812=CARTESIAN_POINT('Ctrl Pts',(-1.43960263872068,-0.589220140984957,
4.00068764464964));
#72813=CARTESIAN_POINT('Ctrl Pts',(-1.43411876921503,-0.602436974585278,
4.00172080312903));
#72814=CARTESIAN_POINT('Ctrl Pts',(-1.4314581810049,-0.60873182160191,4.00221164564211));
#72815=CARTESIAN_POINT('Ctrl Pts',(-1.4248338683996,-0.624121070490411,
4.00340903529682));
#72816=CARTESIAN_POINT('Ctrl Pts',(-1.42082437689268,-0.633195678206351,
4.00411288801435));
#72817=CARTESIAN_POINT('Ctrl Pts',(-1.4054614535129,-0.667085455942641,
4.00673544167841));
#72818=CARTESIAN_POINT('Ctrl Pts',(-1.39354176396732,-0.691640428234245,
4.00862341613449));
#72819=CARTESIAN_POINT('Ctrl Pts',(-1.35975329036538,-0.756821526832915,
4.01363590687048));
#72820=CARTESIAN_POINT('Ctrl Pts',(-1.33671277383052,-0.796810771144227,
4.01671241455552));
#72821=CARTESIAN_POINT('Ctrl Pts',(-1.24957538040695,-0.933600627281844,
4.02744477658827));
#72822=CARTESIAN_POINT('Ctrl Pts',(-1.17647042366368,-1.02418967787595,
4.03496773987277));
#72823=CARTESIAN_POINT('Ctrl Pts',(-1.07177626557557,-1.1277636087137,4.04501285872777));
#72824=CARTESIAN_POINT('Ctrl Pts',(-1.04892516950108,-1.14904781663746,
4.04716622957676));
#72825=CARTESIAN_POINT('Ctrl Pts',(-1.01422593641133,-1.17946972413543,
4.05039175445449));
#72826=CARTESIAN_POINT('Ctrl Pts',(-1.00286076803103,-1.18914815425578,
4.0514415069433));
#72827=CARTESIAN_POINT('Ctrl Pts',(-0.982230770878005,-1.20621029048426,
4.05333630916446));
#72828=CARTESIAN_POINT('Ctrl Pts',(-0.973017437502269,-1.21365464785958,
4.05417880994716));
#72829=CARTESIAN_POINT('Ctrl Pts',(-0.953119805087376,-1.22935969491474,
4.05599102146509));
#72830=CARTESIAN_POINT('Ctrl Pts',(-0.942411209170514,-1.23758786105403,
4.05696193286735));
#72831=CARTESIAN_POINT('Ctrl Pts',(-0.912540963779694,-1.2599267762182,
4.0596590159752));
#72832=CARTESIAN_POINT('Ctrl Pts',(-0.893161301883402,-1.2737383031633,
4.06139651028508));
#72833=CARTESIAN_POINT('Ctrl Pts',(-0.808751925347577,-1.33102164782062,
4.06891642171485));
#72834=CARTESIAN_POINT('Ctrl Pts',(-0.740819507006789,-1.36999321474931,
4.07485769615849));
#72835=CARTESIAN_POINT('Ctrl Pts',(-0.592947371564184,-1.44060151612279,
4.08749747394751));
#72836=CARTESIAN_POINT('Ctrl Pts',(-0.512722798417722,-1.47106592767015,
4.09419388516707));
#72837=CARTESIAN_POINT('Ctrl Pts',(-0.396722666041979,-1.50446647500579,
4.10340229228826));
#72838=CARTESIAN_POINT('Ctrl Pts',(-0.362726844111519,-1.51302277637698,
4.10604456354845));
#72839=CARTESIAN_POINT('Ctrl Pts',(-0.317585429133268,-1.52277500187325,
4.10945595349642));
#72840=CARTESIAN_POINT('Ctrl Pts',(-0.306677355981792,-1.52500925557806,
4.11027288813249));
#72841=CARTESIAN_POINT('Ctrl Pts',(-0.289489116800832,-1.52833795861851,
4.11154757935786));
#72842=CARTESIAN_POINT('Ctrl Pts',(-0.28322487481074,-1.52951120908663,
4.11200952367222));
#72843=CARTESIAN_POINT('Ctrl Pts',(-0.270120136652234,-1.53188236645063,
4.11297020012463));
#72844=CARTESIAN_POINT('Ctrl Pts',(-0.263278532149541,-1.53307302185879,
4.11346847554919));
#72845=CARTESIAN_POINT('Ctrl Pts',(-0.246061259271781,-1.53595071564451,
4.11471472160873));
#72846=CARTESIAN_POINT('Ctrl Pts',(-0.235675778250731,-1.53757851437402,
4.11545946244713));
#72847=CARTESIAN_POINT('Ctrl Pts',(-0.193421924532214,-1.54376310138674,
4.1184640700009));
#72848=CARTESIAN_POINT('Ctrl Pts',(-0.161429806091551,-1.54743572610124,
4.12068046200815));
#72849=CARTESIAN_POINT('Ctrl Pts',(-0.069073154729982,-1.55514212575297,
4.12697080183731));
#72850=CARTESIAN_POINT('Ctrl Pts',(-0.0085557153238808,-1.55665216966412,
4.13096182223911));
#72851=CARTESIAN_POINT('Ctrl Pts',(0.158779093940321,-1.55106588844895,
4.14198712026154));
#72852=CARTESIAN_POINT('Ctrl Pts',(0.264993374155987,-1.53648674054823,
4.14899373602919));
#72853=CARTESIAN_POINT('Ctrl Pts',(0.392058327885954,-1.50547015195689,
4.15799212555762));
#72854=CARTESIAN_POINT('Ctrl Pts',(0.415114644260933,-1.49927643812977,
4.15964935281536));
#72855=CARTESIAN_POINT('Ctrl Pts',(0.4511213048867,-1.48870960690779,4.16228122017885));
#72856=CARTESIAN_POINT('Ctrl Pts',(0.464172724791209,-1.4846920171426,4.16324436338655));
#72857=CARTESIAN_POINT('Ctrl Pts',(0.488427397740782,-1.47687468681791,
4.1650523315718));
#72858=CARTESIAN_POINT('Ctrl Pts',(0.499643550448358,-1.47311794223613,
4.16589568967408));
#72859=CARTESIAN_POINT('Ctrl Pts',(0.52471110318168,-1.46440258683413,4.16779755271291));
#72860=CARTESIAN_POINT('Ctrl Pts',(0.538537019503519,-1.45937470484351,
4.16885828885042));
#72861=CARTESIAN_POINT('Ctrl Pts',(0.580355041979949,-1.44349215315319,
4.17210369872703));
#72862=CARTESIAN_POINT('Ctrl Pts',(0.608104564417459,-1.43202310729415,
4.17430851122494));
#72863=CARTESIAN_POINT('Ctrl Pts',(0.672733860572164,-1.40309416822269,
4.1795691170087));
#72864=CARTESIAN_POINT('Ctrl Pts',(0.709291584777175,-1.38497257839226,
4.18264462470429));
#72865=CARTESIAN_POINT('Ctrl Pts',(0.80296895081271,-1.33385465506529,4.19078279856107));
#72866=CARTESIAN_POINT('Ctrl Pts',(0.858775778246576,-1.29862640751106,
4.19589598309198));
#72867=CARTESIAN_POINT('Ctrl Pts',(0.971039553426938,-1.21735100782933,
4.20664157984781));
#72868=CARTESIAN_POINT('Ctrl Pts',(1.02685050203534,-1.17065852205525,4.2122611747609));
#72869=CARTESIAN_POINT('Ctrl Pts',(1.09098249133582,-1.10887569058425,4.21890769995172));
#72870=CARTESIAN_POINT('Ctrl Pts',(1.10258950023114,-1.09733520121345,4.22011875144394));
#72871=CARTESIAN_POINT('Ctrl Pts',(1.11971053036842,-1.07976628367956,4.22191460917113));
#72872=CARTESIAN_POINT('Ctrl Pts',(1.12536232322705,-1.07387454977935,4.22250903476636));
#72873=CARTESIAN_POINT('Ctrl Pts',(1.13509510611368,-1.06356734266233,4.22353504796563));
#72874=CARTESIAN_POINT('Ctrl Pts',(1.1391971415892,-1.05917244488544,4.22396819269118));
#72875=CARTESIAN_POINT('Ctrl Pts',(1.14892289373412,-1.04863045886817,4.22499694490678));
#72876=CARTESIAN_POINT('Ctrl Pts',(1.15452284517919,-1.0424618282644,4.22559078463061));
#72877=CARTESIAN_POINT('Ctrl Pts',(1.17155707289206,-1.02339212305458,4.22740291580726));
#72878=CARTESIAN_POINT('Ctrl Pts',(1.1828271290968,-1.01034521796368,4.22860994992658));
#72879=CARTESIAN_POINT('Ctrl Pts',(1.20914514724829,-0.978833725395201,
4.2314559725448));
#72880=CARTESIAN_POINT('Ctrl Pts',(1.22399079902061,-0.960205239184679,
4.23308373034422));
#72881=CARTESIAN_POINT('Ctrl Pts',(1.28111466809978,-0.885046678936661,
4.23947128777618));
#72882=CARTESIAN_POINT('Ctrl Pts',(1.31995416291179,-0.826005317666755,
4.24410058554386));
#72883=CARTESIAN_POINT('Ctrl Pts',(1.40020215534977,-0.683815300086653,
4.25484820172164));
#72884=CARTESIAN_POINT('Ctrl Pts',(1.43844394090004,-0.599204237829116,
4.26096528282764));
#72885=CARTESIAN_POINT('Ctrl Pts',(1.47689132675248,-0.488833807938492,
4.2690022473666));
#72886=CARTESIAN_POINT('Ctrl Pts',(1.48432087280456,-0.46578741930575,4.27068250128885));
#72887=CARTESIAN_POINT('Ctrl Pts',(1.49511524256221,-0.429417194574645,
4.27334276084799));
#72888=CARTESIAN_POINT('Ctrl Pts',(1.4988467587665,-0.41620558349433,4.27431084442048));
#72889=CARTESIAN_POINT('Ctrl Pts',(1.50546540379897,-0.391527700873713,
4.27612325498091));
#72890=CARTESIAN_POINT('Ctrl Pts',(1.50839762775139,-0.380074472994539,
4.27696605090734));
#72891=CARTESIAN_POINT('Ctrl Pts',(1.51466216248913,-0.354390167030362,
4.27886028069304));
#72892=CARTESIAN_POINT('Ctrl Pts',(1.51792497970881,-0.34014347834996,4.27991386570177));
#72893=CARTESIAN_POINT('Ctrl Pts',(1.52716564254308,-0.29701081687955,4.28311343693397));
#72894=CARTESIAN_POINT('Ctrl Pts',(1.53252274268747,-0.268000279806779,
4.28527873165686));
#72895=CARTESIAN_POINT('Ctrl Pts',(1.54804801909595,-0.168094572402591,
4.2927856115967));
#72896=CARTESIAN_POINT('Ctrl Pts',(1.55414335791219,-0.0966666733046356,
4.29824356176868));
#72897=CARTESIAN_POINT('Ctrl Pts',(1.55675352456443,0.0651892654033261,
4.31074068532827));
#72898=CARTESIAN_POINT('Ctrl Pts',(1.55034760134611,0.155416528568425,4.31780165767729));
#72899=CARTESIAN_POINT('Ctrl Pts',(1.53158038601086,0.273288939038589,4.32685879977827));
#72900=CARTESIAN_POINT('Ctrl Pts',(1.52620525445035,0.301866050016731,4.32904014538075));
#72901=CARTESIAN_POINT('Ctrl Pts',(1.51781764021891,0.340468218081552,4.33195288822122));
#72902=CARTESIAN_POINT('Ctrl Pts',(1.51550093803742,0.350636448783077,4.33271690403882));
#72903=CARTESIAN_POINT('Ctrl Pts',(1.51163432371025,0.366852671802875,4.3339293603915));
#72904=CARTESIAN_POINT('Ctrl Pts',(1.51015001318952,0.372915745006729,4.33438133900417));
#72905=CARTESIAN_POINT('Ctrl Pts',(1.506900106992,0.385853194321856,4.33534265808603));
#72906=CARTESIAN_POINT('Ctrl Pts',(1.50512386907097,0.392724794476646,4.33585136537074));
#72907=CARTESIAN_POINT('Ctrl Pts',(1.5004109437553,0.410455585273452,4.33715967514111));
#72908=CARTESIAN_POINT('Ctrl Pts',(1.4974033203625,0.421295743245762,4.33795534936006));
#72909=CARTESIAN_POINT('Ctrl Pts',(1.48323262790042,0.470300194912241,4.34153729535848));
#72910=CARTESIAN_POINT('Ctrl Pts',(1.4707253201229,0.508063929082514,4.34425624880874));
#72911=CARTESIAN_POINT('Ctrl Pts',(1.4248933097274,0.630503034587347,4.35306190865689));
#72912=CARTESIAN_POINT('Ctrl Pts',(1.38559037034461,0.712738548353561,4.35896903796059));
#72913=CARTESIAN_POINT('Ctrl Pts',(1.30120666760964,0.855604378996572,4.3699459590959));
#72914=CARTESIAN_POINT('Ctrl Pts',(1.25848062635195,0.917290599815871,4.37496410860436));
#72915=CARTESIAN_POINT('Ctrl Pts',(1.19888497557155,0.991291197923033,4.381540065551));
#72916=CARTESIAN_POINT('Ctrl Pts',(1.18598966112629,1.00668360627153,4.38294072463355));
#72917=CARTESIAN_POINT('Ctrl Pts',(1.16443389142406,1.03142434404389,4.38524954791367));
#72918=CARTESIAN_POINT('Ctrl Pts',(1.15594986849713,1.04092379602623,4.38615042943682));
#72919=CARTESIAN_POINT('Ctrl Pts',(1.13920890034059,1.05921136294441,4.38791376441057));
#72920=CARTESIAN_POINT('Ctrl Pts',(1.13096451243298,1.06800977829544,4.38877564689549));
#72921=CARTESIAN_POINT('Ctrl Pts',(1.11116567889158,1.08865277302545,4.39083082366904));
#72922=CARTESIAN_POINT('Ctrl Pts',(1.09952309498047,1.10041035549216,4.39202789482905));
#72923=CARTESIAN_POINT('Ctrl Pts',(1.05805487789144,1.14097296796636,4.39625372929405));
#72924=CARTESIAN_POINT('Ctrl Pts',(1.02726956244842,1.16876691246246,4.39932475660458));
#72925=CARTESIAN_POINT('Ctrl Pts',(0.944705135715565,1.23752456501332,4.40740016034365));
#72926=CARTESIAN_POINT('Ctrl Pts',(0.891365997969124,1.27647949066352,4.4124677122007));
#72927=CARTESIAN_POINT('Ctrl Pts',(0.752305845475298,1.36506321244349,4.42523157422567));
#72928=CARTESIAN_POINT('Ctrl Pts',(0.664008124868332,1.41012690672247,4.43295844324156));
#72929=CARTESIAN_POINT('Ctrl Pts',(0.558043028650829,1.45203107233191,4.44144656322845));
#72930=CARTESIAN_POINT('Ctrl Pts',(0.54398282983077,1.45735684784334,4.44255734910481));
#72931=CARTESIAN_POINT('Ctrl Pts',(0.522333352922855,1.46520032167599,4.44424183838768));
#72932=CARTESIAN_POINT('Ctrl Pts',(0.514798661286699,1.4678645918828,4.4448233460133));
#72933=CARTESIAN_POINT('Ctrl Pts',(0.500911398612565,1.47265504719746,4.44588600072083));
#72934=CARTESIAN_POINT('Ctrl Pts',(0.494565390129854,1.47479835744498,4.44636807119652));
#72935=CARTESIAN_POINT('Ctrl Pts',(0.479722101696619,1.47970496524575,4.44748762311549));
#72936=CARTESIAN_POINT('Ctrl Pts',(0.471214587151072,1.48243613761681,4.44812325863881));
#72937=CARTESIAN_POINT('Ctrl Pts',(0.442979032400118,1.49123297648234,4.45021440882616));
#72938=CARTESIAN_POINT('Ctrl Pts',(0.423152862096039,1.49697961719711,4.45165308515535));
#72939=CARTESIAN_POINT('Ctrl Pts',(0.373727058224117,1.51024522437844,4.45518017835617));
#72940=CARTESIAN_POINT('Ctrl Pts',(0.344008552218119,1.51729064633663,4.45724878492633));
#72941=CARTESIAN_POINT('Ctrl Pts',(0.190364084958346,1.54896843078223,4.4677667523882));
#72942=CARTESIAN_POINT('Ctrl Pts',(0.0639816913856013,1.5593107781163,4.47587314684393));
#72943=CARTESIAN_POINT('Ctrl Pts',(-0.102821639041292,1.552628589251,4.48714780763645));
#72944=CARTESIAN_POINT('Ctrl Pts',(-0.143297143133573,1.54941708255568,
4.4899246066898));
#72945=CARTESIAN_POINT('Ctrl Pts',(-0.200299113857424,1.5426416882319,4.49392047399656));
#72946=CARTESIAN_POINT('Ctrl Pts',(-0.216966198733222,1.54038590724449,
4.4950991590511));
#72947=CARTESIAN_POINT('Ctrl Pts',(-0.245440147647349,1.53606086469989,
4.49713222950863));
#72948=CARTESIAN_POINT('Ctrl Pts',(-0.257265916661399,1.53412453199732,
4.49798236659563));
#72949=CARTESIAN_POINT('Ctrl Pts',(-0.281498341991835,1.52986869268484,
4.49973685859751));
#72950=CARTESIAN_POINT('Ctrl Pts',(-0.293901464741539,1.52753443334547,
4.50064162320406));
#72951=CARTESIAN_POINT('Ctrl Pts',(-0.325408081421934,1.52120698484425,
4.50295782937668));
#72952=CARTESIAN_POINT('Ctrl Pts',(-0.344466825296843,1.51700482930801,
4.50437581009712));
#72953=CARTESIAN_POINT('Ctrl Pts',(-0.433359299449749,1.49564396431863,
4.51107197157652));
#72954=CARTESIAN_POINT('Ctrl Pts',(-0.502018098146269,1.47401702174769,
4.51649006189344));
#72955=CARTESIAN_POINT('Ctrl Pts',(-0.594715876326606,1.43758863277048,
4.52413147056179));
#72956=CARTESIAN_POINT('Ctrl Pts',(-0.620229072318338,1.42676692814331,
4.52626971884226));
#72957=CARTESIAN_POINT('Ctrl Pts',(-0.736821710858317,1.37359443451321,
4.53618772662005));
#72958=CARTESIAN_POINT('Ctrl Pts',(-0.823959615080783,1.32316345517248,
4.54403862310551));
#72959=CARTESIAN_POINT('Ctrl Pts',(-0.917680608124188,1.25605023322117,
4.55262197176127));
#72960=CARTESIAN_POINT('Ctrl Pts',(-0.929606601008864,1.24724957277861,
4.55371664852113));
#72961=CARTESIAN_POINT('Ctrl Pts',(-0.9477310997487,1.23347036924187,4.55538187697321));
#72962=CARTESIAN_POINT('Ctrl Pts',(-0.954019894784616,1.22861281004857,
4.555959974721));
#72963=CARTESIAN_POINT('Ctrl Pts',(-0.965545846498206,1.21956812836718,
4.55701963727377));
#72964=CARTESIAN_POINT('Ctrl Pts',(-0.970793345706264,1.21539519668665,
4.55750208251466));
#72965=CARTESIAN_POINT('Ctrl Pts',(-0.983023141665749,1.20554003772583,
4.55862670177602));
#72966=CARTESIAN_POINT('Ctrl Pts',(-0.98998332669063,1.19983094764526,4.55926697142687));
#72967=CARTESIAN_POINT('Ctrl Pts',(-1.01304728036083,1.18057539794609,4.56139093715652));
#72968=CARTESIAN_POINT('Ctrl Pts',(-1.02892647665604,1.16676196356979,4.56285706281999));
#72969=CARTESIAN_POINT('Ctrl Pts',(-1.06777590622846,1.1315563269102,4.56646822650813));
#72970=CARTESIAN_POINT('Ctrl Pts',(-1.09038884359604,1.1097826501421,4.56859220948555));
#72971=CARTESIAN_POINT('Ctrl Pts',(-1.20929138036146,0.988147353447604,
4.57998540407079));
#72972=CARTESIAN_POINT('Ctrl Pts',(-1.29254875000947,0.876436207165882,
4.5888585352482));
#72973=CARTESIAN_POINT('Ctrl Pts',(-1.37524857426569,0.727510853602105,
4.60047252996697));
#72974=CARTESIAN_POINT('Ctrl Pts',(-1.38975613989361,0.699398543073187,
4.60265319254083));
#72975=CARTESIAN_POINT('Ctrl Pts',(-1.40986497311874,0.657332479271937,
4.6059115986384));
#72976=CARTESIAN_POINT('Ctrl Pts',(-1.41613769900417,0.643707402780434,
4.60696624968534));
#72977=CARTESIAN_POINT('Ctrl Pts',(-1.42701210073779,0.619158433751454,
4.60886636366504));
#72978=CARTESIAN_POINT('Ctrl Pts',(-1.43168786070544,0.608268490924934,
4.60970921753692));
#72979=CARTESIAN_POINT('Ctrl Pts',(-1.44140648519587,0.584900592698571,
4.6115183298303));
#72980=CARTESIAN_POINT('Ctrl Pts',(-1.44641272582161,0.572408564205819,
4.61248574655382));
#72981=CARTESIAN_POINT('Ctrl Pts',(-1.45973818233629,0.537866224302745,
4.61516247092041));
#72982=CARTESIAN_POINT('Ctrl Pts',(-1.46771902636209,0.515690200860258,
4.61688281918517));
#72983=CARTESIAN_POINT('Ctrl Pts',(-1.49945329818929,0.420798392316111,
4.6242563644812));
#72984=CARTESIAN_POINT('Ctrl Pts',(-1.51832622078728,0.346574386049884,
4.63006110627107));
#72985=CARTESIAN_POINT('Ctrl Pts',(-1.54756893934855,0.181464405618471,
4.64298626460136));
#72986=CARTESIAN_POINT('Ctrl Pts',(-1.5555449504945,0.0904333168781379,
4.65012314607825));
#72987=CARTESIAN_POINT('Ctrl Pts',(-1.55549980947038,-0.00076989453901936,
4.6570644451624));
#72988=CARTESIAN_POINT('Origin',(0.,0.,-1.2940562256037));
#72989=CARTESIAN_POINT('',(-1.55549996779056,0.00031654948737463,5.4955130075581));
#72990=CARTESIAN_POINT('',(-1.55596473934061,0.00138061827089576,5.3559437743963));
#72991=CARTESIAN_POINT('',(-1.5555,-1.46451138874614E-13,-1.2940562256037));
#72992=CARTESIAN_POINT('Ctrl Pts',(-1.55549996779057,0.000316549412329119,
5.49551300756351));
#72993=CARTESIAN_POINT('Ctrl Pts',(-1.55549621245051,0.0187700076134928,
5.49418400711457));
#72994=CARTESIAN_POINT('Ctrl Pts',(-1.55516407835502,0.0372211631028199,
5.4928448070229));
#72995=CARTESIAN_POINT('Ctrl Pts',(-1.55231211830025,0.116870410297289,
5.48701646529434));
#72996=CARTESIAN_POINT('Ctrl Pts',(-1.54650752544575,0.177888397832393,
5.4824276092901));
#72997=CARTESIAN_POINT('Ctrl Pts',(-1.52706475421104,0.30324956282706,5.47275179185585));
#72998=CARTESIAN_POINT('Ctrl Pts',(-1.51291330701088,0.367395427262038,
5.4676617846248));
#72999=CARTESIAN_POINT('Ctrl Pts',(-1.47445156825068,0.500954823256708,
5.45688328109391));
#73000=CARTESIAN_POINT('Ctrl Pts',(-1.4491836912554,0.569940246680635,5.45120764634296));
#73001=CARTESIAN_POINT('Ctrl Pts',(-1.41249987500531,0.651680267799144,
5.44452157937737));
#73002=CARTESIAN_POINT('Ctrl Pts',(-1.40563093601037,0.666366862158133,
5.44332208834666));
#73003=CARTESIAN_POINT('Ctrl Pts',(-1.39502610307436,0.688147227522723,
5.44154877323677));
#73004=CARTESIAN_POINT('Ctrl Pts',(-1.39146322032869,0.695323341379978,
5.44096542181317));
#73005=CARTESIAN_POINT('Ctrl Pts',(-1.38520221303316,0.707692958404927,
5.4399618773571));
#73006=CARTESIAN_POINT('Ctrl Pts',(-1.3825300678186,0.712899087572182,5.43954014868974));
#73007=CARTESIAN_POINT('Ctrl Pts',(-1.37612476855275,0.725207030025228,
5.43854461740483));
#73008=CARTESIAN_POINT('Ctrl Pts',(-1.37236597171916,0.732295201577709,
5.43797242084335));
#73009=CARTESIAN_POINT('Ctrl Pts',(-1.36081907373747,0.753668631593445,
5.43624949597365));
#73010=CARTESIAN_POINT('Ctrl Pts',(-1.35286124673461,0.767861614852756,
5.43510874071072));
#73011=CARTESIAN_POINT('Ctrl Pts',(-1.31074847083172,0.840282980699899,
5.42929135907679));
#73012=CARTESIAN_POINT('Ctrl Pts',(-1.27304824028396,0.896374579530541,
5.42479564204702));
#73013=CARTESIAN_POINT('Ctrl Pts',(-1.15498083671299,1.04949181271474,5.41202819290048));
#73014=CARTESIAN_POINT('Ctrl Pts',(-1.06634584047179,1.1394371540424,5.40385883240737));
#73015=CARTESIAN_POINT('Ctrl Pts',(-0.950648293228203,1.23139386139362,
5.39366161190992));
#73016=CARTESIAN_POINT('Ctrl Pts',(-0.933160564271279,1.24469847644713,
5.39213265906222));
#73017=CARTESIAN_POINT('Ctrl Pts',(-0.904956305404805,1.26522769368522,
5.38968212424182));
#73018=CARTESIAN_POINT('Ctrl Pts',(-0.894421019026142,1.27269715730894,
5.38877006668614));
#73019=CARTESIAN_POINT('Ctrl Pts',(-0.874266083563081,1.28661304576571,
5.38703067101911));
#73020=CARTESIAN_POINT('Ctrl Pts',(-0.864665026180948,1.29308495217789,
5.38620437966685));
#73021=CARTESIAN_POINT('Ctrl Pts',(-0.842523554910953,1.30765328138751,
5.38430349681577));
#73022=CARTESIAN_POINT('Ctrl Pts',(-0.829937237211112,1.31567746742314,
5.38322629977629));
#73023=CARTESIAN_POINT('Ctrl Pts',(-0.789562264691533,1.34060793889677,
5.37978019578898));
#73024=CARTESIAN_POINT('Ctrl Pts',(-0.761359599075222,1.35682330653378,
5.37738670203064));
#73025=CARTESIAN_POINT('Ctrl Pts',(-0.692140490535513,1.3937836664822,5.37154079301822));
#73026=CARTESIAN_POINT('Ctrl Pts',(-0.650674264042728,1.41361723551713,
5.36806145645192));
#73027=CARTESIAN_POINT('Ctrl Pts',(-0.553023130418471,1.45511696657497,
5.35993379132822));
#73028=CARTESIAN_POINT('Ctrl Pts',(-0.496335421825024,1.47541536721711,
5.35526255576933));
#73029=CARTESIAN_POINT('Ctrl Pts',(-0.36584968592708,1.51376577685326,5.34471810397349));
#73030=CARTESIAN_POINT('Ctrl Pts',(-0.291606432972014,1.5298042704696,5.33886102384214));
#73031=CARTESIAN_POINT('Ctrl Pts',(-0.203851725107997,1.54213728182862,
5.33228991746553));
#73032=CARTESIAN_POINT('Ctrl Pts',(-0.191199653998479,1.54375698936549,
5.33135108336637));
#73033=CARTESIAN_POINT('Ctrl Pts',(-0.171271555272678,1.54605940099818,
5.32988722770739));
#73034=CARTESIAN_POINT('Ctrl Pts',(-0.164008536434367,1.54684673542889,
5.32935681026712));
#73035=CARTESIAN_POINT('Ctrl Pts',(-0.150133032996969,1.54825205401307,
5.32834973849311));
#73036=CARTESIAN_POINT('Ctrl Pts',(-0.143521797418711,1.54887889967481,
5.32787264624057));
#73037=CARTESIAN_POINT('Ctrl Pts',(-0.127388919845725,1.5503043594596,5.32671475310773));
#73038=CARTESIAN_POINT('Ctrl Pts',(-0.117863350193136,1.55105763492817,
5.32603642079458));
#73039=CARTESIAN_POINT('Ctrl Pts',(-0.0827367371431863,1.55350994453142,
5.32355263178784));
#73040=CARTESIAN_POINT('Ctrl Pts',(-0.0571001636006358,1.55466339747332,
5.3217743490185));
#73041=CARTESIAN_POINT('Ctrl Pts',(0.0107791434335332,1.55603588151908,
5.3171290383019));
#73042=CARTESIAN_POINT('Ctrl Pts',(0.0530236251046945,1.55516972000688,
5.31430240506007));
#73043=CARTESIAN_POINT('Ctrl Pts',(0.230439225642614,1.54429302761647,5.30251288258265));
#73044=CARTESIAN_POINT('Ctrl Pts',(0.364019800968434,1.51836453370021,5.29377879978447));
#73045=CARTESIAN_POINT('Ctrl Pts',(0.514328775593441,1.46818709127913,5.282864645061));
#73046=CARTESIAN_POINT('Ctrl Pts',(0.535942891310052,1.46043573888513,5.28126930432832));
#73047=CARTESIAN_POINT('Ctrl Pts',(0.569745076543431,1.44746202452444,5.27872864895791));
#73048=CARTESIAN_POINT('Ctrl Pts',(0.582052037284146,1.44255716390761,5.27779390827196));
#73049=CARTESIAN_POINT('Ctrl Pts',(0.604948257612353,1.43309132911008,5.27603580476125));
#73050=CARTESIAN_POINT('Ctrl Pts',(0.615552436059126,1.42856863232373,5.27521378744696));
#73051=CARTESIAN_POINT('Ctrl Pts',(0.639281239314825,1.41813501582131,5.27335629689604));
#73052=CARTESIAN_POINT('Ctrl Pts',(0.652375894412909,1.41215901813877,5.27231865042575));
#73053=CARTESIAN_POINT('Ctrl Pts',(0.692054750666777,1.39338114832703,5.2691347001366));
#73054=CARTESIAN_POINT('Ctrl Pts',(0.718357864203998,1.38000455159089,5.26696883560596));
#73055=CARTESIAN_POINT('Ctrl Pts',(0.779442782059232,1.34671981587785,5.2618036613646));
#73056=CARTESIAN_POINT('Ctrl Pts',(0.813865891287156,1.32620026695378,5.25878522489259));
#73057=CARTESIAN_POINT('Ctrl Pts',(0.903887237328606,1.26771320455635,5.2506044261875));
#73058=CARTESIAN_POINT('Ctrl Pts',(0.957876222252802,1.22742859499133,5.2453853121892));
#73059=CARTESIAN_POINT('Ctrl Pts',(1.0649128999384,1.13618771307338,5.23447804211464));
#73060=CARTESIAN_POINT('Ctrl Pts',(1.11731116976713,1.08470265375015,5.22880303784704));
#73061=CARTESIAN_POINT('Ctrl Pts',(1.1766153376106,1.01755560735805,5.22211756418395));
#73062=CARTESIAN_POINT('Ctrl Pts',(1.18715702995261,1.00523694118504,5.22091807679578));
#73063=CARTESIAN_POINT('Ctrl Pts',(1.20261788269123,0.986587382388459,5.21914476596098));
#73064=CARTESIAN_POINT('Ctrl Pts',(1.20768345717725,0.980380084307348,5.21856141523433));
#73065=CARTESIAN_POINT('Ctrl Pts',(1.21636573365046,0.969571501423572,5.21755787145548));
#73066=CARTESIAN_POINT('Ctrl Pts',(1.22000465929557,0.964988667697563,5.21713614277651));
#73067=CARTESIAN_POINT('Ctrl Pts',(1.22857121224422,0.954074101744648,5.21614061081295));
#73068=CARTESIAN_POINT('Ctrl Pts',(1.23347582941661,0.94772464407345,5.2155684135923));
#73069=CARTESIAN_POINT('Ctrl Pts',(1.24817724427677,0.928384901951449,5.21384548461502));
#73070=CARTESIAN_POINT('Ctrl Pts',(1.25781993509795,0.915278113448224,5.21270472597334));
#73071=CARTESIAN_POINT('Ctrl Pts',(1.30640099030776,0.847026303321275,5.20688730824865));
#73072=CARTESIAN_POINT('Ctrl Pts',(1.34192965025754,0.789534095063161,5.20239156099648));
#73073=CARTESIAN_POINT('Ctrl Pts',(1.43265852025243,0.61879170371439,5.18962413218974));
#73074=CARTESIAN_POINT('Ctrl Pts',(1.47799723580522,0.500933588962382,5.18145481777101));
#73075=CARTESIAN_POINT('Ctrl Pts',(1.51399746982476,0.357595700974926,5.1712576435497));
#73076=CARTESIAN_POINT('Ctrl Pts',(1.5188973129164,0.336175390965826,5.16972868345068));
#73077=CARTESIAN_POINT('Ctrl Pts',(1.52595406549342,0.30201195694397,5.16727813975036));
#73078=CARTESIAN_POINT('Ctrl Pts',(1.52840881945412,0.289332844118817,5.16636608068866));
#73079=CARTESIAN_POINT('Ctrl Pts',(1.53276445440062,0.265230921318809,5.16462668386954));
#73080=CARTESIAN_POINT('Ctrl Pts',(1.53469621967475,0.253814527282955,5.16380039289171));
#73081=CARTESIAN_POINT('Ctrl Pts',(1.53882611997609,0.227633952170098,5.16189951337155));
#73082=CARTESIAN_POINT('Ctrl Pts',(1.54093951249221,0.212857777948125,5.16082231932134));
#73083=CARTESIAN_POINT('Ctrl Pts',(1.54698126620469,0.165792527845507,5.1573762357485));
#73084=CARTESIAN_POINT('Ctrl Pts',(1.55010943707154,0.133411551167825,5.15498275982972));
#73085=CARTESIAN_POINT('Ctrl Pts',(1.55520234428562,0.0551089108422377,
5.14913690547225));
#73086=CARTESIAN_POINT('Ctrl Pts',(1.55615129434233,0.00915378107127548,
5.14565760640941));
#73087=CARTESIAN_POINT('Ctrl Pts',(1.55364297917172,-0.0969202016699715,
5.13752994080372));
#73088=CARTESIAN_POINT('Ctrl Pts',(1.54873226451111,-0.156932446103068,
5.13285866494629));
#73089=CARTESIAN_POINT('Ctrl Pts',(1.5298019759392,-0.291614089909617,5.12231415018773));
#73090=CARTESIAN_POINT('Ctrl Pts',(1.51376466618073,-0.365857890844107,
5.11645704723095));
#73091=CARTESIAN_POINT('Ctrl Pts',(1.48877506129423,-0.450878851757248,
5.10988591886634));
#73092=CARTESIAN_POINT('Ctrl Pts',(1.48502789896872,-0.463071365392931,
5.10894708400576));
#73093=CARTESIAN_POINT('Ctrl Pts',(1.47889921198597,-0.482172933582224,
5.10748322743332));
#73094=CARTESIAN_POINT('Ctrl Pts',(1.47661835804157,-0.489113328030066,
5.10695280983035));
#73095=CARTESIAN_POINT('Ctrl Pts',(1.47217092464432,-0.5023316822306,5.10594573795506));
#73096=CARTESIAN_POINT('Ctrl Pts',(1.47001293215372,-0.508612162144354,
5.10546864576175));
#73097=CARTESIAN_POINT('Ctrl Pts',(1.46465206160209,-0.523894915229154,
5.10431075305752));
#73098=CARTESIAN_POINT('Ctrl Pts',(1.46140626641931,-0.532882051262191,
5.10363242110919));
#73099=CARTESIAN_POINT('Ctrl Pts',(1.44914058229796,-0.565888757788537,
5.10114863515081));
#73100=CARTESIAN_POINT('Ctrl Pts',(1.43960909547117,-0.589715489355327,
5.09937035497825));
#73101=CARTESIAN_POINT('Ctrl Pts',(1.41284045885494,-0.652108644465265,
5.0947250532553));
#73102=CARTESIAN_POINT('Ctrl Pts',(1.39461416297496,-0.690228723778092,
5.09189842621685));
#73103=CARTESIAN_POINT('Ctrl Pts',(1.31147476961905,-0.847335344281351,
5.08010889340678));
#73104=CARTESIAN_POINT('Ctrl Pts',(1.23271952853975,-0.958302614951366,
5.07137479604307));
#73105=CARTESIAN_POINT('Ctrl Pts',(1.1249724719531,-1.07449725890156,5.06046062751484));
#73106=CARTESIAN_POINT('Ctrl Pts',(1.1089905727636,-1.09098452661708,5.0588652902678));
#73107=CARTESIAN_POINT('Ctrl Pts',(1.08322106388461,-1.1164174358852,5.05632463919935));
#73108=CARTESIAN_POINT('Ctrl Pts',(1.07367356846478,-1.12560242240939,5.05538989926836));
#73109=CARTESIAN_POINT('Ctrl Pts',(1.05560081453365,-1.14254981175479,5.05363179641978));
#73110=CARTESIAN_POINT('Ctrl Pts',(1.04710426202992,-1.15034160285659,5.052809779003));
#73111=CARTESIAN_POINT('Ctrl Pts',(1.02780633183187,-1.16764787959965,5.05095228720443));
#73112=CARTESIAN_POINT('Ctrl Pts',(1.01695804938706,-1.17710820503355,5.04991463957633));
#73113=CARTESIAN_POINT('Ctrl Pts',(0.983476062849216,-1.20549808846037,
5.04673068183193));
#73114=CARTESIAN_POINT('Ctrl Pts',(0.96043490313042,-1.22393438768901,5.04456481086921));
#73115=CARTESIAN_POINT('Ctrl Pts',(0.904903587027513,-1.26583364785535,
5.03939961784058));
#73116=CARTESIAN_POINT('Ctrl Pts',(0.872004593677074,-1.28871751697013,
5.03638116881919));
#73117=CARTESIAN_POINT('Ctrl Pts',(0.781573956407065,-1.34657011074711,
5.02820035338002));
#73118=CARTESIAN_POINT('Ctrl Pts',(0.72259608596092,-1.37911664307269,5.02298123557274));
#73119=CARTESIAN_POINT('Ctrl Pts',(0.595309114351531,-1.4389471892505,5.01207398819018));
#73120=CARTESIAN_POINT('Ctrl Pts',(0.526786462914177,-1.46542146527923,
5.0063990104397));
#73121=CARTESIAN_POINT('Ctrl Pts',(0.441147791099174,-1.49172105070239,
4.99971356173075));
#73122=CARTESIAN_POINT('Ctrl Pts',(0.425576203886753,-1.4962379544405,4.99851407449644));
#73123=CARTESIAN_POINT('Ctrl Pts',(0.402207726986503,-1.50262216781296,
4.99674076384221));
#73124=CARTESIAN_POINT('Ctrl Pts',(0.394462975437901,-1.50467385284933,
4.99615741314501));
#73125=CARTESIAN_POINT('Ctrl Pts',(0.381034339373259,-1.50812046156477,
4.99515386939476));
#73126=CARTESIAN_POINT('Ctrl Pts',(0.375358087371483,-1.50954324341259,
4.9947321407153));
#73127=CARTESIAN_POINT('Ctrl Pts',(0.361880685239677,-1.51284070041495,
4.99373660872308));
#73128=CARTESIAN_POINT('Ctrl Pts',(0.354072888158268,-1.51468710056462,
4.99316441147458));
#73129=CARTESIAN_POINT('Ctrl Pts',(0.330389240424846,-1.52009470401718,
4.99144148232381));
#73130=CARTESIAN_POINT('Ctrl Pts',(0.314470885238262,-1.52346745173387,
4.99030072353941));
#73131=CARTESIAN_POINT('Ctrl Pts',(0.232251836461684,-1.53954415109864,
4.9844833042903));
#73132=CARTESIAN_POINT('Ctrl Pts',(0.165220682807613,-1.54817356979386,
4.97998755576158));
#73133=CARTESIAN_POINT('Ctrl Pts',(-0.0277477083768383,-1.56033447212346,
4.96722012781395));
#73134=CARTESIAN_POINT('Ctrl Pts',(-0.153811437169086,-1.55298175242768,
4.95905081534133));
#73135=CARTESIAN_POINT('Ctrl Pts',(-0.299228323718729,-1.52660585432991,
4.94885364307465));
#73136=CARTESIAN_POINT('Ctrl Pts',(-0.320761192389297,-1.52222705216107,
4.94732468266935));
#73137=CARTESIAN_POINT('Ctrl Pts',(-0.35479124275334,-1.51455280734043,
4.94487413859396));
#73138=CARTESIAN_POINT('Ctrl Pts',(-0.367353063342234,-1.51155507373973,
4.94396207946866));
#73139=CARTESIAN_POINT('Ctrl Pts',(-0.39110379635212,-1.50557368958552,
4.94222268260088));
#73140=CARTESIAN_POINT('Ctrl Pts',(-0.402299613152616,-1.50262081783683,
4.94139639163887));
#73141=CARTESIAN_POINT('Ctrl Pts',(-0.427850472564649,-1.49557581445297,
4.9394955122594));
#73142=CARTESIAN_POINT('Ctrl Pts',(-0.442181459458291,-1.49140154608117,
4.93841831833545));
#73143=CARTESIAN_POINT('Ctrl Pts',(-0.487543935555206,-1.47747727919295,
4.93497223562489));
#73144=CARTESIAN_POINT('Ctrl Pts',(-0.518328833659744,-1.4669605067727,
4.93257876045963));
#73145=CARTESIAN_POINT('Ctrl Pts',(-0.591751697810771,-1.43927803082343,
4.92673290841069));
#73146=CARTESIAN_POINT('Ctrl Pts',(-0.634000856416312,-1.42117330217063,
4.92325361093192));
#73147=CARTESIAN_POINT('Ctrl Pts',(-0.729593954772603,-1.37509795829541,
4.91512486394116));
#73148=CARTESIAN_POINT('Ctrl Pts',(-0.782240100439677,-1.34584603364123,
4.91045247516294));
#73149=CARTESIAN_POINT('Ctrl Pts',(-0.897076039036702,-1.2730206514751,
4.89990987672638));
#73150=CARTESIAN_POINT('Ctrl Pts',(-0.958049270255439,-1.22779118276984,
4.89405579280581));
#73151=CARTESIAN_POINT('Ctrl Pts',(-1.02515790167138,-1.1699549333394,4.88748633894162));
#73152=CARTESIAN_POINT('Ctrl Pts',(-1.03472701062877,-1.16150045675095,
4.88654648085501));
#73153=CARTESIAN_POINT('Ctrl Pts',(-1.04960812759939,-1.1480228386689,4.88508139679141));
#73154=CARTESIAN_POINT('Ctrl Pts',(-1.0549904290706,-1.14307867623974,4.88455076058673));
#73155=CARTESIAN_POINT('Ctrl Pts',(-1.06519577098285,-1.13357059947853,
4.88354355238179));
#73156=CARTESIAN_POINT('Ctrl Pts',(-1.07002468889417,-1.12901350811918,
4.88306653951879));
#73157=CARTESIAN_POINT('Ctrl Pts',(-1.07492232739759,-1.12433191648366,
4.88258214429944));
#73158=CARTESIAN_POINT('Ctrl Pts',(-1.07502026796231,-1.12423827182316,
4.88257245735426));
#73159=CARTESIAN_POINT('Ctrl Pts',(-1.07521532371274,-1.12405172288283,
4.88255316460205));
#73160=CARTESIAN_POINT('Ctrl Pts',(-1.07531243909564,-1.12395881881355,
4.88254355877959));
#73161=CARTESIAN_POINT('Ctrl Pts',(-1.07550595354348,-1.12377364789288,
4.88252441749432));
#73162=CARTESIAN_POINT('Ctrl Pts',(-1.07560235277528,-1.12368138122434,
4.88251488201851));
#73163=CARTESIAN_POINT('Ctrl Pts',(-1.07579453975672,-1.12349738576423,
4.88249587106382));
#73164=CARTESIAN_POINT('Ctrl Pts',(-1.07589032765145,-1.12340565712281,
4.88248639557356));
#73165=CARTESIAN_POINT('Ctrl Pts',(-1.07608139310954,-1.1232226416942,4.88246749458972));
#73166=CARTESIAN_POINT('Ctrl Pts',(-1.0761766707884,-1.12313135503462,4.88245806908718));
#73167=CARTESIAN_POINT('Ctrl Pts',(-1.07636681371685,-1.12294913045878,
4.88243925839793));
#73168=CARTESIAN_POINT('Ctrl Pts',(-1.07646167906463,-1.1228581926381,4.88242987320347));
#73169=CARTESIAN_POINT('Ctrl Pts',(-1.07665109246371,-1.12267657509134,
4.88241113372157));
#73170=CARTESIAN_POINT('Ctrl Pts',(-1.07674564058268,-1.12258589544336,
4.88240177942893));
#73171=CARTESIAN_POINT('Ctrl Pts',(-1.08327110384483,-1.11632584106427,
4.88175615396039));
#73172=CARTESIAN_POINT('Ctrl Pts',(-1.08964909522667,-1.11010113370812,
4.88112399837675));
#73173=CARTESIAN_POINT('Ctrl Pts',(-1.11411280972569,-1.08581135962823,
4.87869317585419));
#73174=CARTESIAN_POINT('Ctrl Pts',(-1.13180680853526,-1.06735523591599,
4.87692193039107));
#73175=CARTESIAN_POINT('Ctrl Pts',(-1.17774155068838,-1.01701444273853,
4.87226003217223));
#73176=CARTESIAN_POINT('Ctrl Pts',(-1.20514236162626,-0.984391153385109,
4.86941088766435));
#73177=CARTESIAN_POINT('Ctrl Pts',(-1.29537292150981,-0.867538975858345,
4.85962107782995));
#73178=CARTESIAN_POINT('Ctrl Pts',(-1.35098488812134,-0.778109473641279,
4.85281550816503));
#73179=CARTESIAN_POINT('Ctrl Pts',(-1.4158416855509,-0.645584115997787,
4.84286751383945));
#73180=CARTESIAN_POINT('Ctrl Pts',(-1.43294988245549,-0.606663533609501,
4.83996403278265));
#73181=CARTESIAN_POINT('Ctrl Pts',(-1.45460039012204,-0.551364926885388,
4.83583219011614));
#73182=CARTESIAN_POINT('Ctrl Pts',(-1.46050179484208,-0.535537156170969,
4.83464892534577));
#73183=CARTESIAN_POINT('Ctrl Pts',(-1.47007419320775,-0.508527807802072,
4.8326269372629));
#73184=CARTESIAN_POINT('Ctrl Pts',(-1.47387826629725,-0.497394719677229,
4.83179269406144));
#73185=CARTESIAN_POINT('Ctrl Pts',(-1.48135396658007,-0.474677088226673,
4.83008820453524));
#73186=CARTESIAN_POINT('Ctrl Pts',(-1.4850168475045,-0.463090552156438,
4.82921773704695));
#73187=CARTESIAN_POINT('Ctrl Pts',(-1.49384990129269,-0.433966577763472,
4.82702626617733));
#73188=CARTESIAN_POINT('Ctrl Pts',(-1.49884719410677,-0.416379098743493,
4.82569974291303));
#73189=CARTESIAN_POINT('Ctrl Pts',(-1.51110387703126,-0.370159020359163,
4.82220395706157));
#73190=CARTESIAN_POINT('Ctrl Pts',(-1.51785942608517,-0.341401780430383,
4.82001923083557));
#73191=CARTESIAN_POINT('Ctrl Pts',(-1.54488019058464,-0.209632836606872,
4.80996148349255));
#73192=CARTESIAN_POINT('Ctrl Pts',(-1.55550000000703,-0.104940599039015,
4.80181512781945));
#73193=CARTESIAN_POINT('Ctrl Pts',(-1.5555,1.042515379579E-10,4.79368285916456));
#73194=CARTESIAN_POINT('Ctrl Pts',(-1.55745457732731,-0.000856696892064714,
4.6559437743963));
#73195=CARTESIAN_POINT('Ctrl Pts',(-1.55778497931963,-0.0507117794212508,
4.65952722214655));
#73196=CARTESIAN_POINT('Ctrl Pts',(-1.53299973239953,-0.615518763747496,
4.70014792479876));
#73197=CARTESIAN_POINT('Ctrl Pts',(-0.843969773291502,-1.63319857630279,
4.77780588235294));
#73198=CARTESIAN_POINT('Ctrl Pts',(0.914045851976043,-1.59503691128215,
4.88891764705882));
#73199=CARTESIAN_POINT('Ctrl Pts',(1.83578508816481,-0.0975483364234787,
5.0000294117647));
#73200=CARTESIAN_POINT('Ctrl Pts',(1.07793273566426,1.48918890180207,5.11114117647059));
#73201=CARTESIAN_POINT('Ctrl Pts',(-0.666138955726334,1.7134414082573,5.22225294117646));
#73202=CARTESIAN_POINT('Ctrl Pts',(-1.49940020022205,0.726840308291178,
5.30385380715171));
#73203=CARTESIAN_POINT('Ctrl Pts',(-1.55693103699923,0.106352731462292,
5.34841741822499));
#73204=CARTESIAN_POINT('Ctrl Pts',(-1.55596473934061,0.00138061827089576,
5.3559437743963));
#73205=CARTESIAN_POINT('Origin',(0.,0.,-1.2940562256037));
#73206=CARTESIAN_POINT('',(-1.5555,8.75720568004264E-11,6.19393713463064));
#73207=CARTESIAN_POINT('',(-1.55549999442795,-0.000131661106665976,6.05447729365266));
#73208=CARTESIAN_POINT('',(-1.5555,-1.46451138874614E-13,-1.2940562256037));
#73209=CARTESIAN_POINT('Ctrl Pts',(-1.5555,8.75698298596905E-11,6.19393713463064));
#73210=CARTESIAN_POINT('Ctrl Pts',(-1.55549999999434,0.100505756995347,
6.18732362246232));
#73211=CARTESIAN_POINT('Ctrl Pts',(-1.54575960958544,0.200767590378707,
6.18070462680335));
#73212=CARTESIAN_POINT('Ctrl Pts',(-1.52327742079485,0.31539202784566,6.17265070533303));
#73213=CARTESIAN_POINT('Ctrl Pts',(-1.51988702902391,0.331345163515344,
6.17151910230652));
#73214=CARTESIAN_POINT('Ctrl Pts',(-1.51360209151602,0.358788638093367,
6.16955213806078));
#73215=CARTESIAN_POINT('Ctrl Pts',(-1.51082589452176,0.370304848823369,
6.16872050526237));
#73216=CARTESIAN_POINT('Ctrl Pts',(-1.5050012643872,0.393309942282735,6.16704602094438));
#73217=CARTESIAN_POINT('Ctrl Pts',(-1.50195213953966,0.404797817175777,
6.16620319790713));
#73218=CARTESIAN_POINT('Ctrl Pts',(-1.49589518743367,0.426606833623501,
6.16458990221574));
#73219=CARTESIAN_POINT('Ctrl Pts',(-1.49291141214447,0.436933984751265,
6.16382025540544));
#73220=CARTESIAN_POINT('Ctrl Pts',(-1.48487232212131,0.463714002399664,
6.16180909012442));
#73221=CARTESIAN_POINT('Ctrl Pts',(-1.47965066269369,0.480114945725162,
6.16056220488934));
#73222=CARTESIAN_POINT('Ctrl Pts',(-1.45985787120231,0.53889056821253,6.15603694656404));
#73223=CARTESIAN_POINT('Ctrl Pts',(-1.44373084518829,0.580713836248065,
6.15270857180386));
#73224=CARTESIAN_POINT('Ctrl Pts',(-1.38489859206161,0.715624052944825,
6.1416075381184));
#73225=CARTESIAN_POINT('Ctrl Pts',(-1.33481246918224,0.805191419101341,
6.13362748948238));
#73226=CARTESIAN_POINT('Ctrl Pts',(-1.25210065049771,0.923913659331325,
6.12243790179828));
#73227=CARTESIAN_POINT('Ctrl Pts',(-1.22649098458838,0.957649628971214,
6.11918284362215));
#73228=CARTESIAN_POINT('Ctrl Pts',(-1.18335880596058,1.00989494618722,6.11406214642334));
#73229=CARTESIAN_POINT('Ctrl Pts',(-1.16670342819835,1.02909142679247,6.11216224374716));
#73230=CARTESIAN_POINT('Ctrl Pts',(-1.14357274068401,1.05446728875482,6.10963482590579));
#73231=CARTESIAN_POINT('Ctrl Pts',(-1.13750463629241,1.06101040936331,6.10898165506301));
#73232=CARTESIAN_POINT('Ctrl Pts',(-1.13129023681397,1.06759667821647,6.1083229860029));
#73233=CARTESIAN_POINT('Ctrl Pts',(-1.1312000912299,1.06769219387,6.10831343356977));
#73234=CARTESIAN_POINT('Ctrl Pts',(-1.13101948973085,1.06788350544808,6.10829430016277));
#73235=CARTESIAN_POINT('Ctrl Pts',(-1.13092903373902,1.06797930130002,6.10828471919453));
#73236=CARTESIAN_POINT('Ctrl Pts',(-1.13074772098684,1.06817126856462,6.10826551918392));
#73237=CARTESIAN_POINT('Ctrl Pts',(-1.13065686412614,1.06826743988027,6.10825590014911));
#73238=CARTESIAN_POINT('Ctrl Pts',(-1.13047465653578,1.06846025598309,6.10823661420777));
#73239=CARTESIAN_POINT('Ctrl Pts',(-1.13038330568018,1.06855690064906,6.1082269473107));
#73240=CARTESIAN_POINT('Ctrl Pts',(-1.13020001392395,1.06875076441187,6.10820755554025));
#73241=CARTESIAN_POINT('Ctrl Pts',(-1.13010807286833,1.06884798336458,6.10819783067807));
#73242=CARTESIAN_POINT('Ctrl Pts',(-1.12992350101001,1.06904310017404,6.10817831251915));
#73243=CARTESIAN_POINT('Ctrl Pts',(-1.1298308700259,1.06914099785809,6.1081685192359));
#73244=CARTESIAN_POINT('Ctrl Pts',(-1.12964481460175,1.06933758061251,6.10814885337328));
#73245=CARTESIAN_POINT('Ctrl Pts',(-1.12955138994786,1.06943626548464,6.10813898080936));
#73246=CARTESIAN_POINT('Ctrl Pts',(-1.12489201240993,1.07435669475281,6.10764672131218));
#73247=CARTESIAN_POINT('Ctrl Pts',(-1.1202950966329,1.07914931813107,6.10716662024116));
#73248=CARTESIAN_POINT('Ctrl Pts',(-1.11057682678282,1.08915229893169,6.10616346098069));
#73249=CARTESIAN_POINT('Ctrl Pts',(-1.10544926680595,1.0943562229969,6.10564088787371));
#73250=CARTESIAN_POINT('Ctrl Pts',(-1.09126925583627,1.10854604979731,6.10421337044226));
#73251=CARTESIAN_POINT('Ctrl Pts',(-1.08214240508445,1.11745728155795,6.10331399368169));
#73252=CARTESIAN_POINT('Ctrl Pts',(-1.01802255185381,1.17853987420884,6.0971197439294));
#73253=CARTESIAN_POINT('Ctrl Pts',(-0.959382040211156,1.22674995535479,
6.09207670739811));
#73254=CARTESIAN_POINT('Ctrl Pts',(-0.848276510567133,1.30523255568569,
6.08310042958823));
#73255=CARTESIAN_POINT('Ctrl Pts',(-0.797126670099014,1.33708415917972,
6.07916043288644));
#73256=CARTESIAN_POINT('Ctrl Pts',(-0.703916199839546,1.38787358345946,
6.07211884124433));
#73257=CARTESIAN_POINT('Ctrl Pts',(-0.662621138862048,1.40805676137398,
6.06904380997088));
#73258=CARTESIAN_POINT('Ctrl Pts',(-0.590670333397883,1.43935634693151,
6.06369956486552));
#73259=CARTESIAN_POINT('Ctrl Pts',(-0.560447348213359,1.45139128213938,
6.06145883067095));
#73260=CARTESIAN_POINT('Ctrl Pts',(-0.515837640255012,1.46755394053074,
6.05814405449518));
#73261=CARTESIAN_POINT('Ctrl Pts',(-0.50173219337852,1.47243601497056,6.05709491713882));
#73262=CARTESIAN_POINT('Ctrl Pts',(-0.476563977497652,1.48074342453098,
6.05521996990831));
#73263=CARTESIAN_POINT('Ctrl Pts',(-0.4655289565391,1.48424967283571,6.05439689518635));
#73264=CARTESIAN_POINT('Ctrl Pts',(-0.442105066125174,1.49140542596913,
6.05264711334185));
#73265=CARTESIAN_POINT('Ctrl Pts',(-0.429707891126956,1.49502446258402,
6.05171947935995));
#73266=CARTESIAN_POINT('Ctrl Pts',(-0.39610023328814,1.50438281264368,6.04919980435372));
#73267=CARTESIAN_POINT('Ctrl Pts',(-0.374811584959257,1.50982754839254,
6.04759841306176));
#73268=CARTESIAN_POINT('Ctrl Pts',(-0.23086252915487,1.5434116603317,6.03672894072802));
#73269=CARTESIAN_POINT('Ctrl Pts',(-0.105314296951799,1.5570207221201,6.02699256671601));
#73270=CARTESIAN_POINT('Ctrl Pts',(0.0879702475561942,1.55447694891604,
6.01200997737115));
#73271=CARTESIAN_POINT('Ctrl Pts',(0.155348183048942,1.54919530245018,6.00680112561446));
#73272=CARTESIAN_POINT('Ctrl Pts',(0.238278572920402,1.53722746586338,6.00054764375608));
#73273=CARTESIAN_POINT('Ctrl Pts',(0.254345077891514,1.53465096909691,5.99934375009415));
#73274=CARTESIAN_POINT('Ctrl Pts',(0.278269692415118,1.53042823861274,5.99756526889735));
#73275=CARTESIAN_POINT('Ctrl Pts',(0.286159697282557,1.52897261274699,5.99698107598373));
#73276=CARTESIAN_POINT('Ctrl Pts',(0.299784681428891,1.52634977614278,5.99597668499117));
#73277=CARTESIAN_POINT('Ctrl Pts',(0.305524696174648,1.52521118456764,5.99555494170796));
#73278=CARTESIAN_POINT('Ctrl Pts',(0.319107981313133,1.52243703680532,5.99456018391639));
#73279=CARTESIAN_POINT('Ctrl Pts',(0.326945216680282,1.52077324660806,5.99398876593171));
#73280=CARTESIAN_POINT('Ctrl Pts',(0.350601178924871,1.51555992270552,5.99227068860269));
#73281=CARTESIAN_POINT('Ctrl Pts',(0.366378190402151,1.51182344928817,5.9911339202866));
#73282=CARTESIAN_POINT('Ctrl Pts',(0.453152783866419,1.4898343159594,5.98491714641951));
#73283=CARTESIAN_POINT('Ctrl Pts',(0.522858350126134,1.4668249869679,5.98005279422658));
#73284=CARTESIAN_POINT('Ctrl Pts',(0.652945980216558,1.41342525492405,5.97078097161365));
#73285=CARTESIAN_POINT('Ctrl Pts',(0.71347804039623,1.38385628121094,5.96637817449022));
#73286=CARTESIAN_POINT('Ctrl Pts',(0.806708636098383,1.33056699957885,5.95922156983969));
#73287=CARTESIAN_POINT('Ctrl Pts',(0.840728887961389,1.30933645186616,5.9565243551852));
#73288=CARTESIAN_POINT('Ctrl Pts',(0.898309517757776,1.27023290224372,5.95176793682155));
#73289=CARTESIAN_POINT('Ctrl Pts',(0.922251110259659,1.25295822473093,5.94972909416547));
#73290=CARTESIAN_POINT('Ctrl Pts',(0.957115568819714,1.22626150835033,5.94665743588395));
#73291=CARTESIAN_POINT('Ctrl Pts',(0.96842320594772,1.21735120997193,5.94564446474324));
#73292=CARTESIAN_POINT('Ctrl Pts',(0.988560351730942,1.2010252233923,5.94380899912389));
#73293=CARTESIAN_POINT('Ctrl Pts',(0.997434270784263,1.19366579016095,5.94298880688795));
#73294=CARTESIAN_POINT('Ctrl Pts',(1.01632691798641,1.17763972109679,5.94121746799815));
#73295=CARTESIAN_POINT('Ctrl Pts',(1.02631831432266,1.16894243418587,5.94026509877406));
#73296=CARTESIAN_POINT('Ctrl Pts',(1.05331511110293,1.14482938447257,5.93764791061511));
#73297=CARTESIAN_POINT('Ctrl Pts',(1.07009169098644,1.12916372215336,5.93597270723586));
#73298=CARTESIAN_POINT('Ctrl Pts',(1.18352889886552,1.01843916648673,5.92429545484538));
#73299=CARTESIAN_POINT('Ctrl Pts',(1.26773120836102,0.911483326915082,5.91374536081626));
#73300=CARTESIAN_POINT('Ctrl Pts',(1.35856837308699,0.758718994893285,5.90000153131931));
#73301=CARTESIAN_POINT('Ctrl Pts',(1.37866050227068,0.721566499344423,5.89675577322499));
#73302=CARTESIAN_POINT('Ctrl Pts',(1.40849053995322,0.660600171865966,5.89162599840744));
#73303=CARTESIAN_POINT('Ctrl Pts',(1.41919304505899,0.637282890891516,5.88970837246558));
#73304=CARTESIAN_POINT('Ctrl Pts',(1.43308407436719,0.604931039847843,5.88711775692739));
#73305=CARTESIAN_POINT('Ctrl Pts',(1.43677266131674,0.596117320092936,5.88641899245111));
#73306=CARTESIAN_POINT('Ctrl Pts',(1.44288699595086,0.581120867482679,5.88524254606759));
#73307=CARTESIAN_POINT('Ctrl Pts',(1.44535474224175,0.574955669600456,5.88476245338597));
#73308=CARTESIAN_POINT('Ctrl Pts',(1.45045438419841,0.561974822980848,5.88375928405301));
#73309=CARTESIAN_POINT('Ctrl Pts',(1.45307785374348,0.555156175417558,5.8832366927621));
#73310=CARTESIAN_POINT('Ctrl Pts',(1.46014977824049,0.536381943934191,5.88180907095295));
#73311=CARTESIAN_POINT('Ctrl Pts',(1.46449948511695,0.524389407318887,5.88090960934952));
#73312=CARTESIAN_POINT('Ctrl Pts',(1.49367994410934,0.44073982453446,5.87471288439105));
#73313=CARTESIAN_POINT('Ctrl Pts',(1.51339226117757,0.367394116034133,5.86966768527994));
#73314=CARTESIAN_POINT('Ctrl Pts',(1.53900290933919,0.233814050823407,5.86069256610842));
#73315=CARTESIAN_POINT('Ctrl Pts',(1.54689314861505,0.17412772902152,5.85675583996998));
#73316=CARTESIAN_POINT('Ctrl Pts',(1.5546787619804,0.0683066064660613,5.8497171105308));
#73317=CARTESIAN_POINT('Ctrl Pts',(1.55601787859658,0.0223544985036325,
5.84664155752925));
#73318=CARTESIAN_POINT('Ctrl Pts',(1.55482789562833,-0.0561124988750462,
5.84129650913789));
#73319=CARTESIAN_POINT('Ctrl Pts',(1.55331452006572,-0.0886123411355607,
5.83905550560502));
#73320=CARTESIAN_POINT('Ctrl Pts',(1.54962210075184,-0.135920582541938,
5.83574040626327));
#73321=CARTESIAN_POINT('Ctrl Pts',(1.54824648071701,-0.15078417498026,5.83469122220941));
#73322=CARTESIAN_POINT('Ctrl Pts',(1.54542434879024,-0.177138075808367,
5.83281622304226));
#73323=CARTESIAN_POINT('Ctrl Pts',(1.54406300689717,-0.188636510822875,
5.83199314364161));
#73324=CARTESIAN_POINT('Ctrl Pts',(1.5409120306448,-0.212925193861889,5.83024338489538));
#73325=CARTESIAN_POINT('Ctrl Pts',(1.53909122751143,-0.225710431933803,
5.82931577903717));
#73326=CARTESIAN_POINT('Ctrl Pts',(1.53374320312031,-0.260182145597517,
5.82679626560476));
#73327=CARTESIAN_POINT('Ctrl Pts',(1.52991547241985,-0.28181823502813,5.82519500983114));
#73328=CARTESIAN_POINT('Ctrl Pts',(1.50108539483435,-0.426805488715601,
5.81432475684774));
#73329=CARTESIAN_POINT('Ctrl Pts',(1.46165321004162,-0.546788576369168,
5.8045873531112));
#73330=CARTESIAN_POINT('Ctrl Pts',(1.37954828209111,-0.72179137571153,5.78960441794395));
#73331=CARTESIAN_POINT('Ctrl Pts',(1.34692905325015,-0.780973861132466,
5.7843962153277));
#73332=CARTESIAN_POINT('Ctrl Pts',(1.30180150011851,-0.85156196904706,5.77814341094369));
#73333=CARTESIAN_POINT('Ctrl Pts',(1.29282334705419,-0.865131655658124,
5.77693958065828));
#73334=CARTESIAN_POINT('Ctrl Pts',(1.27910223437042,-0.885179126897421,
5.77516117381309));
#73335=CARTESIAN_POINT('Ctrl Pts',(1.27451970134879,-0.89176462766739,5.77457699299982));
#73336=CARTESIAN_POINT('Ctrl Pts',(1.26650678670468,-0.903091940787994,
5.77357261458507));
#73337=CARTESIAN_POINT('Ctrl Pts',(1.26310039188334,-0.907850151435346,
5.77315087191335));
#73338=CARTESIAN_POINT('Ctrl Pts',(1.25496668431837,-0.919077286499646,
5.77215610364143));
#73339=CARTESIAN_POINT('Ctrl Pts',(1.25021614416999,-0.925529058269034,
5.77158467470252));
#73340=CARTESIAN_POINT('Ctrl Pts',(1.23570250920406,-0.944924547920943,
5.76986652922714));
#73341=CARTESIAN_POINT('Ctrl Pts',(1.22578634406955,-0.957753092118421,
5.76872970486963));
#73342=CARTESIAN_POINT('Ctrl Pts',(1.16985229575528,-1.02782280620752,5.76250323880995));
#73343=CARTESIAN_POINT('Ctrl Pts',(1.12002016712495,-1.08191109364863,5.75763010560487));
#73344=CARTESIAN_POINT('Ctrl Pts',(1.01787062365482,-1.17813036989517,5.74837773140616));
#73345=CARTESIAN_POINT('Ctrl Pts',(0.966290331923454,-1.220792566977,5.74400270556658));
#73346=CARTESIAN_POINT('Ctrl Pts',(0.879523827842564,-1.283603507024,5.7368651424418));
#73347=CARTESIAN_POINT('Ctrl Pts',(0.846020307262605,-1.30592856110802,
5.73415764346354));
#73348=CARTESIAN_POINT('Ctrl Pts',(0.786437303343166,-1.3423758694586,5.729385059918));
#73349=CARTESIAN_POINT('Ctrl Pts',(0.760749693953393,-1.35709849173012,
5.72734053823085));
#73350=CARTESIAN_POINT('Ctrl Pts',(0.721956173072818,-1.37788505546186,
5.72426201721646));
#73351=CARTESIAN_POINT('Ctrl Pts',(0.709159710732051,-1.38451450761659,
5.72324799699761));
#73352=CARTESIAN_POINT('Ctrl Pts',(0.68596328346975,-1.39612590986945,5.72141140967549));
#73353=CARTESIAN_POINT('Ctrl Pts',(0.675596410996834,-1.40117188767795,
5.72059115736507));
#73354=CARTESIAN_POINT('Ctrl Pts',(0.653210353646895,-1.41176190005422,
5.71882055979193));
#73355=CARTESIAN_POINT('Ctrl Pts',(0.641174658460541,-1.41726866393784,
5.71786900140752));
#73356=CARTESIAN_POINT('Ctrl Pts',(0.608125360827213,-1.4318827725488,5.71525633723756));
#73357=CARTESIAN_POINT('Ctrl Pts',(0.586979336012558,-1.44068035465576,
5.71358490667965));
#73358=CARTESIAN_POINT('Ctrl Pts',(0.439141500713128,-1.49839168348515,
5.70189485446018));
#73359=CARTESIAN_POINT('Ctrl Pts',(0.306732816311562,-1.53098761397395,
5.69132580902141));
#73360=CARTESIAN_POINT('Ctrl Pts',(0.129949078662473,-1.55063465352026,
5.67757159682885));
#73361=CARTESIAN_POINT('Ctrl Pts',(0.0879093842415107,-1.55358520396131,
5.67433328279631));
#73362=CARTESIAN_POINT('Ctrl Pts',(0.0201977969613845,-1.55557973304851,
5.66921369005209));
#73363=CARTESIAN_POINT('Ctrl Pts',(-0.00542038943477336,-1.55570147182633,
5.6672989480957));
#73364=CARTESIAN_POINT('Ctrl Pts',(-0.0405785454446391,-1.5549999390086,
5.66471152350156));
#73365=CARTESIAN_POINT('Ctrl Pts',(-0.0501237690313576,-1.55472153418934,
5.66401314503642));
#73366=CARTESIAN_POINT('Ctrl Pts',(-0.0663008480386664,-1.5541005539251,
5.66283714775373));
#73367=CARTESIAN_POINT('Ctrl Pts',(-0.0729340654963613,-1.55380338636156,
5.66235712254839));
#73368=CARTESIAN_POINT('Ctrl Pts',(-0.0868637001504683,-1.55308993652841,
5.66135387182954));
#73369=CARTESIAN_POINT('Ctrl Pts',(-0.094159368060113,-1.55266470063568,
5.66083113391641));
#73370=CARTESIAN_POINT('Ctrl Pts',(-0.11419068421685,-1.551355441475,5.65940267041467));
#73371=CARTESIAN_POINT('Ctrl Pts',(-0.126919213453564,-1.55036600814602,
5.6585025246396));
#73372=CARTESIAN_POINT('Ctrl Pts',(-0.215431747984915,-1.54238817555035,
5.65228648526826));
#73373=CARTESIAN_POINT('Ctrl Pts',(-0.290636371536021,-1.53000191274858,
5.64722443282021));
#73374=CARTESIAN_POINT('Ctrl Pts',(-0.423572867878734,-1.49794566675011,
5.63820156385544));
#73375=CARTESIAN_POINT('Ctrl Pts',(-0.481623098155619,-1.48030209370686,
5.63423446949909));
#73376=CARTESIAN_POINT('Ctrl Pts',(-0.581199236530258,-1.44355798320697,
5.6271914758283));
#73377=CARTESIAN_POINT('Ctrl Pts',(-0.623188238602572,-1.42593413207612,
5.62414380544839));
#73378=CARTESIAN_POINT('Ctrl Pts',(-0.693560475555203,-1.39269462171343,
5.61884171907256));
#73379=CARTESIAN_POINT('Ctrl Pts',(-0.722339986588968,-1.37798735070021,
5.61661514580918));
#73380=CARTESIAN_POINT('Ctrl Pts',(-0.763680617648392,-1.35520990202905,
5.61331736500265));
#73381=CARTESIAN_POINT('Ctrl Pts',(-0.77661792844527,-1.34783772403101,
5.61227068863502));
#73382=CARTESIAN_POINT('Ctrl Pts',(-0.799420127740366,-1.33440686437997,
5.61039847537237));
#73383=CARTESIAN_POINT('Ctrl Pts',(-0.809327097894377,-1.32842156551155,
5.6095756441021));
#73384=CARTESIAN_POINT('Ctrl Pts',(-0.83016171822836,-1.31551475612854,
5.60782462947459));
#73385=CARTESIAN_POINT('Ctrl Pts',(-0.841071617125858,-1.3085664171523,
5.6068955008717));
#73386=CARTESIAN_POINT('Ctrl Pts',(-0.870358421010073,-1.28939656899751,
5.60436723590744));
#73387=CARTESIAN_POINT('Ctrl Pts',(-0.888563304042817,-1.27691912625267,
5.60275863904885));
#73388=CARTESIAN_POINT('Ctrl Pts',(-1.00820448796809,-1.19112075176179,
5.59193098019633));
#73389=CARTESIAN_POINT('Ctrl Pts',(-1.10072003799945,-1.10618628701079,
5.58224967321679));
#73390=CARTESIAN_POINT('Ctrl Pts',(-1.22620854477788,-0.959483704961743,
5.56728549392952));
#73391=CARTESIAN_POINT('Ctrl Pts',(-1.266946940279,-0.905010297610914,5.5620418073036));
#73392=CARTESIAN_POINT('Ctrl Pts',(-1.31289016560192,-0.8343655282264,5.55575198432674));
#73393=CARTESIAN_POINT('Ctrl Pts',(-1.32156955765091,-0.820548829640439,
5.55454469990656));
#73394=CARTESIAN_POINT('Ctrl Pts',(-1.3341950595696,-0.799730140119969,
5.55276224138154));
#73395=CARTESIAN_POINT('Ctrl Pts',(-1.33830660058748,-0.792830501722975,
5.55217740161241));
#73396=CARTESIAN_POINT('Ctrl Pts',(-1.34532138193611,-0.780848818431469,
5.551172337649));
#73397=CARTESIAN_POINT('Ctrl Pts',(-1.34824957437302,-0.775781919307044,
5.55075056108574));
#73398=CARTESIAN_POINT('Ctrl Pts',(-1.35511454310304,-0.76374660388735,
5.54975636072694));
#73399=CARTESIAN_POINT('Ctrl Pts',(-1.35902622715029,-0.756764178135495,
5.54918552612413));
#73400=CARTESIAN_POINT('Ctrl Pts',(-1.37067696040424,-0.735585702465334,
5.54747107571725));
#73401=CARTESIAN_POINT('Ctrl Pts',(-1.37824902703871,-0.721298363200619,
5.5463372897936));
#73402=CARTESIAN_POINT('Ctrl Pts',(-1.42179095277394,-0.635951047907557,
5.53968277342803));
#73403=CARTESIAN_POINT('Ctrl Pts',(-1.45248739563885,-0.562322750641483,
5.53441881645385));
#73404=CARTESIAN_POINT('Ctrl Pts',(-1.50197208513788,-0.412095804786269,
5.52400209212123));
#73405=CARTESIAN_POINT('Ctrl Pts',(-1.52085201134606,-0.335784731675577,
5.51886206306377));
#73406=CARTESIAN_POINT('Ctrl Pts',(-1.54148635314156,-0.213286078280297,
5.51050282797458));
#73407=CARTESIAN_POINT('Ctrl Pts',(-1.5470891174386,-0.167886129574404,
5.50738338416856));
#73408=CARTESIAN_POINT('Ctrl Pts',(-1.5520094080886,-0.105504418935435,
5.50302932791489));
#73409=CARTESIAN_POINT('Ctrl Pts',(-1.55306153173296,-0.0886804653159927,
5.50184847303187));
#73410=CARTESIAN_POINT('Ctrl Pts',(-1.55438856351805,-0.0599791782285614,
5.49982100710866));
#73411=CARTESIAN_POINT('Ctrl Pts',(-1.55480120029659,-0.048109474691243,
5.49897876276333));
#73412=CARTESIAN_POINT('Ctrl Pts',(-1.55536174447704,-0.0240539016133195,
5.49726363135309));
#73413=CARTESIAN_POINT('Ctrl Pts',(-1.55550244753266,-0.0118687164362759,
5.49639057878115));
#73414=CARTESIAN_POINT('Ctrl Pts',(-1.55549996779057,0.000316549412329119,
5.49551300756351));
#73415=CARTESIAN_POINT('Ctrl Pts',(-1.55549937218933,0.00139754019306266,
5.35621122277575));
#73416=CARTESIAN_POINT('Ctrl Pts',(-1.55559462614257,-0.104622640978542,
5.36319747743842));
#73417=CARTESIAN_POINT('Ctrl Pts',(-1.54485106980132,-0.210368542457165,
5.37012627567963));
#73418=CARTESIAN_POINT('Ctrl Pts',(-1.51948565660077,-0.333355901469767,
5.378727583461));
#73419=CARTESIAN_POINT('Ctrl Pts',(-1.51517400246084,-0.352435106664556,
5.38007698449756));
#73420=CARTESIAN_POINT('Ctrl Pts',(-1.50638888331349,-0.388162038393061,
5.38263597283379));
#73421=CARTESIAN_POINT('Ctrl Pts',(-1.50199619653517,-0.404826654203786,
5.38384292500506));
#73422=CARTESIAN_POINT('Ctrl Pts',(-1.4940289863857,-0.433134959995016,
5.38591787781));
#73423=CARTESIAN_POINT('Ctrl Pts',(-1.49059285227339,-0.444816185850429,
5.38678134560506));
#73424=CARTESIAN_POINT('Ctrl Pts',(-1.48377456560763,-0.46702848731743,
5.38843774130807));
#73425=CARTESIAN_POINT('Ctrl Pts',(-1.48041651470706,-0.477566226628152,
5.38922983404945));
#73426=CARTESIAN_POINT('Ctrl Pts',(-1.47225276490055,-0.502270664768497,
5.39110206806758));
#73427=CARTESIAN_POINT('Ctrl Pts',(-1.46735458199097,-0.516405389317805,
5.39218519503222));
#73428=CARTESIAN_POINT('Ctrl Pts',(-1.44889147902196,-0.567299686470397,
5.39612975787505));
#73429=CARTESIAN_POINT('Ctrl Pts',(-1.43414378380739,-0.603611266726163,
5.39902954514188));
#73430=CARTESIAN_POINT('Ctrl Pts',(-1.3751667166187,-0.734424266385154,
5.40979894090119));
#73431=CARTESIAN_POINT('Ctrl Pts',(-1.32283747958938,-0.824959539373897,
5.41791083537331));
#73432=CARTESIAN_POINT('Ctrl Pts',(-1.23517119294205,-0.946580437038499,
5.42951665995351));
#73433=CARTESIAN_POINT('Ctrl Pts',(-1.20687152197627,-0.98240727084699,
5.43303223237939));
#73434=CARTESIAN_POINT('Ctrl Pts',(-1.15947048249572,-1.03727061677243,
5.43852045687238));
#73435=CARTESIAN_POINT('Ctrl Pts',(-1.14137989423181,-1.05714440225415,
5.44053202404411));
#73436=CARTESIAN_POINT('Ctrl Pts',(-1.11644087966305,-1.08315463597974,
5.44318592154724));
#73437=CARTESIAN_POINT('Ctrl Pts',(-1.11004104675936,-1.08971238800746,
5.44385690565517));
#73438=CARTESIAN_POINT('Ctrl Pts',(-1.10347969926421,-1.09631784851829,
5.44453434613287));
#73439=CARTESIAN_POINT('Ctrl Pts',(-1.10337594716636,-1.09642226850917,
5.4445450556046));
#73440=CARTESIAN_POINT('Ctrl Pts',(-1.10316828171242,-1.0966312114593,5.44456648591301));
#73441=CARTESIAN_POINT('Ctrl Pts',(-1.10306436831849,-1.09673573438144,
5.44457720674692));
#73442=CARTESIAN_POINT('Ctrl Pts',(-1.10285627344347,-1.09694499039339,
5.4445986707756));
#73443=CARTESIAN_POINT('Ctrl Pts',(-1.10275209189547,-1.09704972341412,
5.44460941396514));
#73444=CARTESIAN_POINT('Ctrl Pts',(-1.10254335135056,-1.09725950912321,
5.44463093394031));
#73445=CARTESIAN_POINT('Ctrl Pts',(-1.10243879225428,-1.0973645617121,5.44464171071842));
#73446=CARTESIAN_POINT('Ctrl Pts',(-1.10222918423786,-1.09757509883223,
5.44466330939392));
#73447=CARTESIAN_POINT('Ctrl Pts',(-1.10212413518729,-1.09768058322991,
5.44467413128117));
#73448=CARTESIAN_POINT('Ctrl Pts',(-1.10191343136236,-1.09789209952021,
5.44469583203788));
#73449=CARTESIAN_POINT('Ctrl Pts',(-1.10180777642052,-1.09799813124841,
5.44470671089493));
#73450=CARTESIAN_POINT('Ctrl Pts',(-1.10159574083055,-1.09821086157687,
5.44472853785013));
#73451=CARTESIAN_POINT('Ctrl Pts',(-1.10148935997882,-1.09831755997749,
5.4447394859332));
#73452=CARTESIAN_POINT('Ctrl Pts',(-1.10127574789631,-1.09853174744648,
5.44476146405641));
#73453=CARTESIAN_POINT('Ctrl Pts',(-1.10116851643139,-1.09863923627038,
5.44477249407785));
#73454=CARTESIAN_POINT('Ctrl Pts',(-1.10095307311749,-1.09885513342537,
5.44479464931521));
#73455=CARTESIAN_POINT('Ctrl Pts',(-1.10084486098597,-1.09896354148033,
5.44480577451021));
#73456=CARTESIAN_POINT('Ctrl Pts',(-1.10062732027645,-1.09918141168588,
5.44482813392619));
#73457=CARTESIAN_POINT('Ctrl Pts',(-1.10051799137245,-1.09929087351814,
5.44483936812301));
#73458=CARTESIAN_POINT('Ctrl Pts',(-1.100298074202,-1.09951099238802,5.44486196004768));
#73459=CARTESIAN_POINT('Ctrl Pts',(-1.10018748557034,-1.09962164905443,
5.44487331774715));
#73460=CARTESIAN_POINT('Ctrl Pts',(-1.09996489831589,-1.09984430605457,
5.4448961719414));
#73461=CARTESIAN_POINT('Ctrl Pts',(-1.09985289927611,-1.09995630596934,
5.44490766840417));
#73462=CARTESIAN_POINT('Ctrl Pts',(-1.09962733190117,-1.10018180621022,
5.44493081624437));
#73463=CARTESIAN_POINT('Ctrl Pts',(-1.0995137630907,-1.10029530606754,5.44494246758604));
#73464=CARTESIAN_POINT('Ctrl Pts',(-1.0993475870668,-1.10046132977795,5.44495951144099));
#73465=CARTESIAN_POINT('Ctrl Pts',(-1.0992949937133,-1.10051386739248,5.44496490500675));
#73466=CARTESIAN_POINT('Ctrl Pts',(-1.09918482523972,-1.10062390333105,
5.44497620161535));
#73467=CARTESIAN_POINT('Ctrl Pts',(-1.09912724937277,-1.10068140090909,
5.44498210460103));
#73468=CARTESIAN_POINT('Ctrl Pts',(-1.09900648866035,-1.10080197849289,
5.44499448393808));
#73469=CARTESIAN_POINT('Ctrl Pts',(-1.09894330289011,-1.10086505758171,
5.44500096021925));
#73470=CARTESIAN_POINT('Ctrl Pts',(-1.09881058684144,-1.10099752674318,
5.44501456102142));
#73471=CARTESIAN_POINT('Ctrl Pts',(-1.09874105542098,-1.10106691566946,
5.44502168545441));
#73472=CARTESIAN_POINT('Ctrl Pts',(-1.09859477930165,-1.1012128643647,5.44503667093697));
#73473=CARTESIAN_POINT('Ctrl Pts',(-1.09851803316126,-1.10128942270898,
5.44504453187735));
#73474=CARTESIAN_POINT('Ctrl Pts',(-1.09835629329758,-1.10145073306999,
5.44506109551254));
#73475=CARTESIAN_POINT('Ctrl Pts',(-1.09827129775852,-1.1015354832808,5.44506979806866));
#73476=CARTESIAN_POINT('Ctrl Pts',(-1.09809181694324,-1.10171440462488,
5.44508817109984));
#73477=CARTESIAN_POINT('Ctrl Pts',(-1.09799732935,-1.10180857345365,5.44509784139772));
#73478=CARTESIAN_POINT('Ctrl Pts',(-1.09321282033183,-1.10657571473158,
5.44558739999751));
#73479=CARTESIAN_POINT('Ctrl Pts',(-1.08849301815657,-1.11121871746479,
5.44606494504099));
#73480=CARTESIAN_POINT('Ctrl Pts',(-1.07791713728808,-1.12149046448134,
5.44712303654671));
#73481=CARTESIAN_POINT('Ctrl Pts',(-1.07204645330552,-1.12710364500374,
5.44770241563164));
#73482=CARTESIAN_POINT('Ctrl Pts',(-1.05437109262091,-1.14374066492307,
5.44942417078648));
#73483=CARTESIAN_POINT('Ctrl Pts',(-1.04243798201973,-1.15462730643651,
5.45055685599203));
#73484=CARTESIAN_POINT('Ctrl Pts',(-0.969263986921939,-1.21932492944561,
5.45734134487584));
#73485=CARTESIAN_POINT('Ctrl Pts',(-0.904032371853128,-1.26844584958117,
5.46272408535151));
#73486=CARTESIAN_POINT('Ctrl Pts',(-0.77050932373688,-1.35343405419328,
5.47314789669137));
#73487=CARTESIAN_POINT('Ctrl Pts',(-0.702819439396752,-1.38978858966198,
5.47817721861439));
#73488=CARTESIAN_POINT('Ctrl Pts',(-0.5913365409592,-1.43942837263412,5.48639175438763));
#73489=CARTESIAN_POINT('Ctrl Pts',(-0.549165599718193,-1.45603896530304,
5.48948318920828));
#73490=CARTESIAN_POINT('Ctrl Pts',(-0.490202873436202,-1.47633749702224,
5.49382197940525));
#73491=CARTESIAN_POINT('Ctrl Pts',(-0.473983189648467,-1.48162449963002,
5.49501705984585));
#73492=CARTESIAN_POINT('Ctrl Pts',(-0.446073060886537,-1.49021695527416,
5.49707794238948));
#73493=CARTESIAN_POINT('Ctrl Pts',(-0.434424595378966,-1.49365424552904,
5.49793936765119));
#73494=CARTESIAN_POINT('Ctrl Pts',(-0.410631104486835,-1.50037348542465,
5.49970220788646));
#73495=CARTESIAN_POINT('Ctrl Pts',(-0.398484152931951,-1.50364519166036,
5.5006038828026));
#73496=CARTESIAN_POINT('Ctrl Pts',(-0.367590103931512,-1.51156567899781,
5.50290219303504));
#73497=CARTESIAN_POINT('Ctrl Pts',(-0.348794137251851,-1.51601315096183,
5.50430516668958));
#73498=CARTESIAN_POINT('Ctrl Pts',(-0.269135135186256,-1.53330215573084,
5.5102735262068));
#73499=CARTESIAN_POINT('Ctrl Pts',(-0.207620865705634,-1.54283535705406,
5.51494053166543));
#73500=CARTESIAN_POINT('Ctrl Pts',(-0.0433451858979095,-1.5582914950787,
5.52754013488558));
#73501=CARTESIAN_POINT('Ctrl Pts',(0.0597127087849346,-1.55774954845205,
5.53559818847931));
#73502=CARTESIAN_POINT('Ctrl Pts',(0.190163278075731,-1.54409272431689,
5.54564864748023));
#73503=CARTESIAN_POINT('Ctrl Pts',(0.218282668049377,-1.54036920398571,
5.54780446586955));
#73504=CARTESIAN_POINT('Ctrl Pts',(0.265616686225664,-1.53277894863473,
5.55140012163969));
#73505=CARTESIAN_POINT('Ctrl Pts',(0.284888202360669,-1.52931433458504,
5.55285460324597));
#73506=CARTESIAN_POINT('Ctrl Pts',(0.312675569542116,-1.52377520457266,
5.55493336840922));
#73507=CARTESIAN_POINT('Ctrl Pts',(0.321246522978594,-1.52199131635983,
5.55557200065485));
#73508=CARTESIAN_POINT('Ctrl Pts',(0.336274648206556,-1.51873087644293,
5.55668673109968));
#73509=CARTESIAN_POINT('Ctrl Pts',(0.342738054555045,-1.51728532116043,
5.5571644883669));
#73510=CARTESIAN_POINT('Ctrl Pts',(0.357080720846315,-1.5139812205348,5.55822089230619));
#73511=CARTESIAN_POINT('Ctrl Pts',(0.364954935812276,-1.51210240391644,
5.55879839671195));
#73512=CARTESIAN_POINT('Ctrl Pts',(0.388360694549209,-1.50632421452209,
5.56050863350208));
#73513=CARTESIAN_POINT('Ctrl Pts',(0.403847637240471,-1.50224625362449,
5.56163186640449));
#73514=CARTESIAN_POINT('Ctrl Pts',(0.505375142390776,-1.47382876515868,
5.56895699368908));
#73515=CARTESIAN_POINT('Ctrl Pts',(0.589254314168118,-1.44234493949242,
5.57483218913564));
#73516=CARTESIAN_POINT('Ctrl Pts',(0.73445695181496,-1.37304721856563,5.58542219003687));
#73517=CARTESIAN_POINT('Ctrl Pts',(0.796740934423673,-1.33786720905471,
5.59011948391792));
#73518=CARTESIAN_POINT('Ctrl Pts',(0.892688137963855,-1.27458988108497,
5.59786755097302));
#73519=CARTESIAN_POINT('Ctrl Pts',(0.927969099527476,-1.24913741072054,
5.60083866149626));
#73520=CARTESIAN_POINT('Ctrl Pts',(0.975353457828333,-1.21183698359632,
5.60503643656849));
#73521=CARTESIAN_POINT('Ctrl Pts',(0.988401593924317,-1.20121833692233,
5.60621538346845));
#73522=CARTESIAN_POINT('Ctrl Pts',(1.01053723534928,-1.18259935990777,5.60825722622297));
#73523=CARTESIAN_POINT('Ctrl Pts',(1.01970845382683,-1.17470055939435,5.60911595523393));
#73524=CARTESIAN_POINT('Ctrl Pts',(1.03827316303654,-1.15833029379701,5.61088118354835));
#73525=CARTESIAN_POINT('Ctrl Pts',(1.04765734188957,-1.14984968892041,5.61178802493457));
#73526=CARTESIAN_POINT('Ctrl Pts',(1.0713543156893,-1.12790351044442,5.61411623053505));
#73527=CARTESIAN_POINT('Ctrl Pts',(1.08551686665898,-1.11427979662375,5.61554426965163));
#73528=CARTESIAN_POINT('Ctrl Pts',(1.14677112719925,-1.05307981356902,5.62188773036175));
#73529=CARTESIAN_POINT('Ctrl Pts',(1.19101517158888,-1.00276701712588,5.62692228364672));
#73530=CARTESIAN_POINT('Ctrl Pts',(1.29188112948638,-0.871940913129017,
5.63956985855039));
#73531=CARTESIAN_POINT('Ctrl Pts',(1.34437166160667,-0.788607248880685,
5.64726790177073));
#73532=CARTESIAN_POINT('Ctrl Pts',(1.40119258664077,-0.676028543132031,
5.65692596393689));
#73533=CARTESIAN_POINT('Ctrl Pts',(1.41306765233618,-0.650841956097149,
5.65904122872589));
#73534=CARTESIAN_POINT('Ctrl Pts',(1.43202761020508,-0.607659769720504,
5.66257726609157));
#73535=CARTESIAN_POINT('Ctrl Pts',(1.43946455910997,-0.589826537465558,
5.66401210854213));
#73536=CARTESIAN_POINT('Ctrl Pts',(1.44976955671436,-0.563759107816872,
5.66606827362465));
#73537=CARTESIAN_POINT('Ctrl Pts',(1.45290338031695,-0.555632861058138,
5.66670353323081));
#73538=CARTESIAN_POINT('Ctrl Pts',(1.45809581412612,-0.541824108967194,
5.66777283899854));
#73539=CARTESIAN_POINT('Ctrl Pts',(1.4601897866093,-0.536155350698382,5.66820890626339));
#73540=CARTESIAN_POINT('Ctrl Pts',(1.46493212999062,-0.523083093617968,
5.66920775139164));
#73541=CARTESIAN_POINT('Ctrl Pts',(1.46755747596099,-0.515671533273761,
5.66976918240121));
#73542=CARTESIAN_POINT('Ctrl Pts',(1.47484193114657,-0.49460064621538,5.67135237581244));
#73543=CARTESIAN_POINT('Ctrl Pts',(1.47936745242251,-0.480895519651347,
5.67236679767314));
#73544=CARTESIAN_POINT('Ctrl Pts',(1.51508421425955,-0.367451373582968,
5.68065345741046));
#73545=CARTESIAN_POINT('Ctrl Pts',(1.53634685153535,-0.264850001125193,
5.68746218616178));
#73546=CARTESIAN_POINT('Ctrl Pts',(1.55367329349452,-0.0982229060206245,
5.69849523671166));
#73547=CARTESIAN_POINT('Ctrl Pts',(1.55637601066361,-0.0352325784255422,
5.70265826081442));
#73548=CARTESIAN_POINT('Ctrl Pts',(1.55453394469138,0.0680268280765478,
5.70963963641047));
#73549=CARTESIAN_POINT('Ctrl Pts',(1.55225066405916,0.108262910391544,5.71239847735124));
#73550=CARTESIAN_POINT('Ctrl Pts',(1.54684619303097,0.164667555324142,5.71634630481624));
#73551=CARTESIAN_POINT('Ctrl Pts',(1.5450265039527,0.180946442166766,5.71749508152314));
#73552=CARTESIAN_POINT('Ctrl Pts',(1.54142502752959,0.209126437161502,5.71950161409378));
#73553=CARTESIAN_POINT('Ctrl Pts',(1.53976155660048,0.221041435589435,5.72035559003728));
#73554=CARTESIAN_POINT('Ctrl Pts',(1.53604419563493,0.245585351461588,5.72212684422236));
#73555=CARTESIAN_POINT('Ctrl Pts',(1.53397236411308,0.258210580395583,5.72304462913413));
#73556=CARTESIAN_POINT('Ctrl Pts',(1.52820076146422,0.290855880837561,5.72543578734649));
#73557=CARTESIAN_POINT('Ctrl Pts',(1.52426337095613,0.310830844313258,5.72691656261709));
#73558=CARTESIAN_POINT('Ctrl Pts',(1.50187193334053,0.413737644608457,5.7346407457897));
#73559=CARTESIAN_POINT('Ctrl Pts',(1.47704095767163,0.495119923312487,5.74108392243216));
#73560=CARTESIAN_POINT('Ctrl Pts',(1.41524906417467,0.650735796526316,5.75400031311279));
#73561=CARTESIAN_POINT('Ctrl Pts',(1.37874930691362,0.724870720990935,5.76044575843799));
#73562=CARTESIAN_POINT('Ctrl Pts',(1.31710930035695,0.828399799246312,5.76965378044345));
#73563=CARTESIAN_POINT('Ctrl Pts',(1.29648585262373,0.860318611806963,5.77252248245038));
#73564=CARTESIAN_POINT('Ctrl Pts',(1.26835532361954,0.900543207378694,5.77614788799235));
#73565=CARTESIAN_POINT('Ctrl Pts',(1.26190089368668,0.909565527472956,5.7769617311091));
#73566=CARTESIAN_POINT('Ctrl Pts',(1.2511791377066,0.92421908209416,5.77828363762656));
#73567=CARTESIAN_POINT('Ctrl Pts',(1.24696911625932,0.929891485772563,5.77879537513316));
#73568=CARTESIAN_POINT('Ctrl Pts',(1.23895217507802,0.940540809480468,5.77975585433789));
#73569=CARTESIAN_POINT('Ctrl Pts',(1.23515357567941,0.94552374621654,5.78020517178475));
#73570=CARTESIAN_POINT('Ctrl Pts',(1.22487231516354,0.958842829656581,5.78140631173893));
#73571=CARTESIAN_POINT('Ctrl Pts',(1.21833455901391,0.967136329104839,5.78215438612113));
#73572=CARTESIAN_POINT('Ctrl Pts',(1.19284420130964,0.998803504165049,5.78501420822213));
#73573=CARTESIAN_POINT('Ctrl Pts',(1.17329802236386,1.02169358055151,5.78708872828255));
#73574=CARTESIAN_POINT('Ctrl Pts',(1.09305309766497,1.11032380576659,5.79521855177529));
#73575=CARTESIAN_POINT('Ctrl Pts',(1.02739322846957,1.17134532249325,5.8010455900795));
#73576=CARTESIAN_POINT('Ctrl Pts',(0.900925733994054,1.27001723407601,5.8116223575826));
#73577=CARTESIAN_POINT('Ctrl Pts',(0.842091695323497,1.30976756903908,5.81633119265602));
#73578=CARTESIAN_POINT('Ctrl Pts',(0.755138453555622,1.36022915795142,5.82320093543274));
#73579=CARTESIAN_POINT('Ctrl Pts',(0.729104244124455,1.3743595794835,5.82524645422139));
#73580=CARTESIAN_POINT('Ctrl Pts',(0.689625125179295,1.39434991763002,5.82834173061752));
#73581=CARTESIAN_POINT('Ctrl Pts',(0.676474032564042,1.40077741394932,5.8293717165143));
#73582=CARTESIAN_POINT('Ctrl Pts',(0.652539397502234,1.41205962618346,5.83124541300879));
#73583=CARTESIAN_POINT('Ctrl Pts',(0.641787357941646,1.41697883761974,5.83208681735378));
#73584=CARTESIAN_POINT('Ctrl Pts',(0.618448096165011,1.42733675045644,5.83391315215404));
#73585=CARTESIAN_POINT('Ctrl Pts',(0.605843037113228,1.4327325077978,5.83489946678285));
#73586=CARTESIAN_POINT('Ctrl Pts',(0.570860037997591,1.44716323442029,5.83763754412333));
#73587=CARTESIAN_POINT('Ctrl Pts',(0.548341511132627,1.45584479821499,5.83940092799493));
#73588=CARTESIAN_POINT('Ctrl Pts',(0.432924641821117,1.49728385159557,5.8484485079143));
#73589=CARTESIAN_POINT('Ctrl Pts',(0.33728154179288,1.5216824978213,5.85599758830367));
#73590=CARTESIAN_POINT('Ctrl Pts',(0.174451430080643,1.54710929074434,5.86876889911588));
#73591=CARTESIAN_POINT('Ctrl Pts',(0.108321607269753,1.55314120131835,5.87392807257427));
#73592=CARTESIAN_POINT('Ctrl Pts',(0.0189685137864616,1.55555507088054,
5.88073748017832));
#73593=CARTESIAN_POINT('Ctrl Pts',(-0.00408170450262528,1.55566540117844,
5.88247926609734));
#73594=CARTESIAN_POINT('Ctrl Pts',(-0.0439488770477343,1.55497003356112,
5.88545754294958));
#73595=CARTESIAN_POINT('Ctrl Pts',(-0.0607657296007624,1.55440371073337,
5.88670327397402));
#73596=CARTESIAN_POINT('Ctrl Pts',(-0.0858130022068973,1.55315307657781,
5.88853981094884));
#73597=CARTESIAN_POINT('Ctrl Pts',(-0.0940518914480969,1.55267594835633,
5.88914086000298));
#73598=CARTESIAN_POINT('Ctrl Pts',(-0.108948986900014,1.55169421768988,
5.89022166345651));
#73599=CARTESIAN_POINT('Ctrl Pts',(-0.115608107540542,1.55121229894249,
5.89070258280972));
#73600=CARTESIAN_POINT('Ctrl Pts',(-0.130837720518675,1.5500115162799,5.89179751568691));
#73601=CARTESIAN_POINT('Ctrl Pts',(-0.139405609597813,1.54926443673051,
5.89240997720311));
#73602=CARTESIAN_POINT('Ctrl Pts',(-0.16658455836971,1.54666725855996,5.89434288622661));
#73603=CARTESIAN_POINT('Ctrl Pts',(-0.18516946869602,1.54455248281149,5.8956498005022));
#73604=CARTESIAN_POINT('Ctrl Pts',(-0.35584132537989,1.5220066229701,5.90755289312));
#73605=CARTESIAN_POINT('Ctrl Pts',(-0.504176002461071,1.47950912003686,
5.91724886467921));
#73606=CARTESIAN_POINT('Ctrl Pts',(-0.685890257238166,1.39687595912198,
5.93067715758492));
#73607=CARTESIAN_POINT('Ctrl Pts',(-0.7270052782106,1.37592534870155,5.9338227542899));
#73608=CARTESIAN_POINT('Ctrl Pts',(-0.782056113402773,1.34471671123798,
5.93822487156425));
#73609=CARTESIAN_POINT('Ctrl Pts',(-0.796844605925746,1.33600652357278,
5.93942699358277));
#73610=CARTESIAN_POINT('Ctrl Pts',(-0.821862415753385,1.32070828178135,
5.94149621596701));
#73611=CARTESIAN_POINT('Ctrl Pts',(-0.832164313949627,1.31424150571343,
5.94235884711758));
#73612=CARTESIAN_POINT('Ctrl Pts',(-0.851697782372793,1.30165807719495,
5.94401539628674));
#73613=CARTESIAN_POINT('Ctrl Pts',(-0.860941983413846,1.29556233038056,
5.94480849726516));
#73614=CARTESIAN_POINT('Ctrl Pts',(-0.884966363418037,1.27934966885143,
5.94689423809982));
#73615=CARTESIAN_POINT('Ctrl Pts',(-0.899637875526344,1.26907552284861,
5.94819274983266));
#73616=CARTESIAN_POINT('Ctrl Pts',(-0.953318981497306,1.23008511128515,
5.95303873171313));
#73617=CARTESIAN_POINT('Ctrl Pts',(-0.991154570462774,1.19980755224995,
5.95664514517999));
#73618=CARTESIAN_POINT('Ctrl Pts',(-1.11550428599869,1.09039752656929,5.9691748665564));
#73619=CARTESIAN_POINT('Ctrl Pts',(-1.19445971526106,1.00328340079883,5.97837078010903));
#73620=CARTESIAN_POINT('Ctrl Pts',(-1.28026143751037,0.883967146842678,
5.98964658886706));
#73621=CARTESIAN_POINT('Ctrl Pts',(-1.2969525839575,0.859291264677404,5.99191389710067));
#73622=CARTESIAN_POINT('Ctrl Pts',(-1.32379938764862,0.817035236315087,
5.99567255948169));
#73623=CARTESIAN_POINT('Ctrl Pts',(-1.33433795891441,0.799708515226675,
5.99718018444302));
#73624=CARTESIAN_POINT('Ctrl Pts',(-1.34899755313851,0.77450926251175,5.99931991532146));
#73625=CARTESIAN_POINT('Ctrl Pts',(-1.35339419853894,0.766800593095095,
5.99996751029557));
#73626=CARTESIAN_POINT('Ctrl Pts',(-1.36099080627317,0.75321250048554,6.00109631188464));
#73627=CARTESIAN_POINT('Ctrl Pts',(-1.364219126722,0.747349467227705,6.00157923790042));
#73628=CARTESIAN_POINT('Ctrl Pts',(-1.371239577101,0.734402360311117,6.00263653640742));
#73629=CARTESIAN_POINT('Ctrl Pts',(-1.37501478363253,0.727309533172104,
6.00320986934433));
#73630=CARTESIAN_POINT('Ctrl Pts',(-1.3857895488713,0.706682204405237,6.00486119481532));
#73631=CARTESIAN_POINT('Ctrl Pts',(-1.39264565386833,0.69307325725646,6.0059308312449));
#73632=CARTESIAN_POINT('Ctrl Pts',(-1.44123920171017,0.592984218352183,
6.01367013293471));
#73633=CARTESIAN_POINT('Ctrl Pts',(-1.47509478095636,0.502892925769997,
6.01995637297821));
#73634=CARTESIAN_POINT('Ctrl Pts',(-1.51827150523562,0.344978077444376,
6.03073226641404));
#73635=CARTESIAN_POINT('Ctrl Pts',(-1.53183798483718,0.278621160732913,
6.03519053309801));
#73636=CARTESIAN_POINT('Ctrl Pts',(-1.54676781674349,0.169887914987912,
6.042598042306));
#73637=CARTESIAN_POINT('Ctrl Pts',(-1.55079856868164,0.127968246974907,
6.04547707770907));
#73638=CARTESIAN_POINT('Ctrl Pts',(-1.55404318917488,0.0693305109071148,
6.04956662452576));
#73639=CARTESIAN_POINT('Ctrl Pts',(-1.55469570600136,0.0527084230119468,
6.05073275764942));
#73640=CARTESIAN_POINT('Ctrl Pts',(-1.5553615201138,0.0240109097994755,
6.05275955295973));
#73641=CARTESIAN_POINT('Ctrl Pts',(-1.55550101617352,0.0119396733131739,
6.05361621352016));
#73642=CARTESIAN_POINT('Ctrl Pts',(-1.55549999442795,-0.000131661105043114,
6.05447729365254));
#73643=CARTESIAN_POINT('Origin',(0.,0.,-1.2940562256037));
#73644=CARTESIAN_POINT('',(-1.55549991697348,0.000508228199595362,6.89275239802721));
#73645=CARTESIAN_POINT('',(-1.5555,-1.2376520005909E-10,6.75616363716894));
#73646=CARTESIAN_POINT('',(-1.5555,-1.46451138874614E-13,-1.2940562256037));
#73647=CARTESIAN_POINT('',(-1.55549936109204,-0.00142508202560441,6.19403092979389));
#73648=CARTESIAN_POINT('Ctrl Pts',(-1.55549991697361,0.000508227400676815,
6.8927523980872));
#73649=CARTESIAN_POINT('Ctrl Pts',(-1.55549342449748,0.0203793442693804,
6.89126023457575));
#73650=CARTESIAN_POINT('Ctrl Pts',(-1.55510615917786,0.0402497180585557,
6.88978222333507));
#73651=CARTESIAN_POINT('Ctrl Pts',(-1.55402627507162,0.0681743633031146,
6.88772972553868));
#73652=CARTESIAN_POINT('Ctrl Pts',(-1.55365156229955,0.0762380348004057,
6.88713992681524));
#73653=CARTESIAN_POINT('Ctrl Pts',(-1.55285741420605,0.0908703204861343,
6.88607536342126));
#73654=CARTESIAN_POINT('Ctrl Pts',(-1.55245903086773,0.0974398710232745,
6.88559948895312));
#73655=CARTESIAN_POINT('Ctrl Pts',(-1.55153303461324,0.111257821680616,
6.88460318461379));
#73656=CARTESIAN_POINT('Ctrl Pts',(-1.55099630922104,0.118505337091623,
6.88408325408978));
#73657=CARTESIAN_POINT('Ctrl Pts',(-1.5493921319165,0.138283865563624,6.8826708879077));
#73658=CARTESIAN_POINT('Ctrl Pts',(-1.54822344887407,0.150806448583604,
6.8817838251873));
#73659=CARTESIAN_POINT('Ctrl Pts',(-1.53967876647658,0.231741300147992,
6.87608894454265));
#73660=CARTESIAN_POINT('Ctrl Pts',(-1.52792115720393,0.299623430997248,
6.87148823334955));
#73661=CARTESIAN_POINT('Ctrl Pts',(-1.48388532731362,0.481252482250994,
6.85912751940839));
#73662=CARTESIAN_POINT('Ctrl Pts',(-1.44309657454036,0.592444118163773,
6.85147558106071));
#73663=CARTESIAN_POINT('Ctrl Pts',(-1.37686943514775,0.724350393368029,
6.84138953236598));
#73664=CARTESIAN_POINT('Ctrl Pts',(-1.36286575701312,0.750366356807447,
6.83934918828765));
#73665=CARTESIAN_POINT('Ctrl Pts',(-1.34094704980521,0.788446970763909,
6.83627571548063));
#73666=CARTESIAN_POINT('Ctrl Pts',(-1.3335907151863,0.800826695194638,6.83526246678439));
#73667=CARTESIAN_POINT('Ctrl Pts',(-1.32003736661037,0.822930442925678,
6.83342670452176));
#73668=CARTESIAN_POINT('Ctrl Pts',(-1.31390202523348,0.832691190132706,
6.83260649651835));
#73669=CARTESIAN_POINT('Ctrl Pts',(-1.30048686840046,0.853515990203702,
6.83083535442585));
#73670=CARTESIAN_POINT('Ctrl Pts',(-1.29317315679937,0.864557000311825,
6.82988320027177));
#73671=CARTESIAN_POINT('Ctrl Pts',(-1.27245361975139,0.894984668878109,
6.82722159441595));
#73672=CARTESIAN_POINT('Ctrl Pts',(-1.25874731347701,0.914161287672667,
6.82550090103568));
#73673=CARTESIAN_POINT('Ctrl Pts',(-1.19762732621862,0.995693061502733,
6.81799104430637));
#73674=CARTESIAN_POINT('Ctrl Pts',(-1.14598353095668,1.05471998529052,6.81204165300716));
#73675=CARTESIAN_POINT('Ctrl Pts',(-1.02925092609578,1.16940352904253,6.79941782007523));
#73676=CARTESIAN_POINT('Ctrl Pts',(-0.963561367754265,1.22409633970669,
6.79274633746764));
#73677=CARTESIAN_POINT('Ctrl Pts',(-0.86437221551257,1.29372578440817,6.78349559977576));
#73678=CARTESIAN_POINT('Ctrl Pts',(-0.834320973498121,1.31330678507143,
6.78079071459073));
#73679=CARTESIAN_POINT('Ctrl Pts',(-0.794161120196738,1.33753891088416,
6.77732591922588));
#73680=CARTESIAN_POINT('Ctrl Pts',(-0.784644165101397,1.3431439892473,6.77651550500294));
#73681=CARTESIAN_POINT('Ctrl Pts',(-0.769054216766427,1.35210353574585,
6.77520617713905));
#73682=CARTESIAN_POINT('Ctrl Pts',(-0.763017265955682,1.35551946376564,
6.77470355079349));
#73683=CARTESIAN_POINT('Ctrl Pts',(-0.750952875219959,1.36223979996799,
6.77370809944965));
#73684=CARTESIAN_POINT('Ctrl Pts',(-0.744925996976146,1.36554485714885,
6.77321524525308));
#73685=CARTESIAN_POINT('Ctrl Pts',(-0.72941593334125,1.37391711771678,6.771957696216));
#73686=CARTESIAN_POINT('Ctrl Pts',(-0.719901550179127,1.37892625813991,
6.77119654407822));
#73687=CARTESIAN_POINT('Ctrl Pts',(-0.678195797298543,1.40033419337853,
6.76790119818549));
#73688=CARTESIAN_POINT('Ctrl Pts',(-0.645487916613955,1.41570873658642,
6.76542263308532));
#73689=CARTESIAN_POINT('Ctrl Pts',(-0.543124381169593,1.45953898997125,
6.75789607720686));
#73690=CARTESIAN_POINT('Ctrl Pts',(-0.471916280569133,1.48409389918118,
6.75297575371484));
#73691=CARTESIAN_POINT('Ctrl Pts',(-0.314813232751636,1.52581038777286,
6.74227346169623));
#73692=CARTESIAN_POINT('Ctrl Pts',(-0.228692389286584,1.54107169755881,
6.73649465373794));
#73693=CARTESIAN_POINT('Ctrl Pts',(-0.119857285379126,1.55103122860766,
6.72897915844517));
#73694=CARTESIAN_POINT('Ctrl Pts',(-0.0979235790153293,1.55257029852886,
6.72745459059677));
#73695=CARTESIAN_POINT('Ctrl Pts',(-0.0618410957183949,1.554334553788,6.72492595338788));
#73696=CARTESIAN_POINT('Ctrl Pts',(-0.0477083438185087,1.55483250438405,
6.72393036659501));
#73697=CARTESIAN_POINT('Ctrl Pts',(-0.0220608897234783,1.55538616281825,
6.72211324131705));
#73698=CARTESIAN_POINT('Ctrl Pts',(-0.0105484957400943,1.55550683525241,
6.72129379676679));
#73699=CARTESIAN_POINT('Ctrl Pts',(0.0144039426147126,1.55549137293776,
6.71950895805211));
#73700=CARTESIAN_POINT('Ctrl Pts',(0.0278429078952762,1.55530885558072,
6.71854217542209));
#73701=CARTESIAN_POINT('Ctrl Pts',(0.0658082330556769,1.5543010359791,6.71579460484143));
#73702=CARTESIAN_POINT('Ctrl Pts',(0.0903188070033247,1.55306948328054,
6.71400135543403));
#73703=CARTESIAN_POINT('Ctrl Pts',(0.145922532807744,1.54895496524715,6.7098867729851));
#73704=CARTESIAN_POINT('Ctrl Pts',(0.176977834788359,1.54571455149333,6.7075554733893));
#73705=CARTESIAN_POINT('Ctrl Pts',(0.286963129644274,1.53088047996332,6.69918145406124));
#73706=CARTESIAN_POINT('Ctrl Pts',(0.365068923062777,1.51415493697405,6.69301023202755));
#73707=CARTESIAN_POINT('Ctrl Pts',(0.516215514325651,1.46941042077895,6.68078395274029));
#73708=CARTESIAN_POINT('Ctrl Pts',(0.589133013551162,1.44172467738669,6.67474776217071));
#73709=CARTESIAN_POINT('Ctrl Pts',(0.674310663003219,1.40183684484663,6.66772943405374));
#73710=CARTESIAN_POINT('Ctrl Pts',(0.688838947033825,1.39475530803565,6.66653381552239));
#73711=CARTESIAN_POINT('Ctrl Pts',(0.710392133403156,1.38383065912949,6.66476504616534));
#73712=CARTESIAN_POINT('Ctrl Pts',(0.717501497186652,1.38015792047352,6.66418243640727));
#73713=CARTESIAN_POINT('Ctrl Pts',(0.72976093398955,1.37370429055078,6.66317961170658));
#73714=CARTESIAN_POINT('Ctrl Pts',(0.734923972157448,1.37094903511661,6.66275786978976));
#73715=CARTESIAN_POINT('Ctrl Pts',(0.747137139583626,1.36434265233553,6.66176161238843));
#73716=CARTESIAN_POINT('Ctrl Pts',(0.754173145705648,1.36046596878214,6.66118871136267));
#73717=CARTESIAN_POINT('Ctrl Pts',(0.775413806698982,1.348547406247,6.65946139336219));
#73718=CARTESIAN_POINT('Ctrl Pts',(0.789522739716125,1.34033599417012,6.65831702405038));
#73719=CARTESIAN_POINT('Ctrl Pts',(0.861740535217963,1.29676899974673,6.65246092039309));
#73720=CARTESIAN_POINT('Ctrl Pts',(0.917620610546984,1.2578478482483,6.64793277641949));
#73721=CARTESIAN_POINT('Ctrl Pts',(1.06846628495678,1.13736150270851,6.63518692712743));
#73722=CARTESIAN_POINT('Ctrl Pts',(1.15638051507125,1.0478512119659,6.627066855546));
#73723=CARTESIAN_POINT('Ctrl Pts',(1.24610318389196,0.931286676784698,6.61691915042587));
#73724=CARTESIAN_POINT('Ctrl Pts',(1.259199506514,0.913501252055849,6.6153824971542));
#73725=CARTESIAN_POINT('Ctrl Pts',(1.27936010646699,0.884864598939954,6.61292253251035));
#73726=CARTESIAN_POINT('Ctrl Pts',(1.2866755157358,0.874193193479355,6.6120088760989));
#73727=CARTESIAN_POINT('Ctrl Pts',(1.30028123207379,0.853804967320327,6.61026824971638));
#73728=CARTESIAN_POINT('Ctrl Pts',(1.30659788751557,0.844106718198599,6.60944234820352));
#73729=CARTESIAN_POINT('Ctrl Pts',(1.32078904753555,0.821777387648905,6.60754496338971));
#73730=CARTESIAN_POINT('Ctrl Pts',(1.32859154152943,0.809102138208922,6.60647090898404));
#73731=CARTESIAN_POINT('Ctrl Pts',(1.35273526629831,0.768589261813121,6.60304621392579));
#73732=CARTESIAN_POINT('Ctrl Pts',(1.36839152557638,0.740355659019166,6.6006714190227));
#73733=CARTESIAN_POINT('Ctrl Pts',(1.40395021191578,0.671244795101186,6.59488268006597));
#73734=CARTESIAN_POINT('Ctrl Pts',(1.42296022501471,0.629943892926199,6.5914425288533));
#73735=CARTESIAN_POINT('Ctrl Pts',(1.46307327525252,0.531677562136893,6.58331546255814));
#73736=CARTESIAN_POINT('Ctrl Pts',(1.48270295400637,0.474189566342425,6.5786032278935));
#73737=CARTESIAN_POINT('Ctrl Pts',(1.51927573540323,0.342317698620794,6.56799295098523));
#73738=CARTESIAN_POINT('Ctrl Pts',(1.53421395534008,0.267526301050437,6.56211087485816));
#73739=CARTESIAN_POINT('Ctrl Pts',(1.54518832953776,0.179265839303977,6.55551565943411));
#73740=CARTESIAN_POINT('Ctrl Pts',(1.54660756504172,0.166578158161503,6.55457596191046));
#73741=CARTESIAN_POINT('Ctrl Pts',(1.54859339454342,0.146602016798972,6.55311107045756));
#73742=CARTESIAN_POINT('Ctrl Pts',(1.54926505956831,0.139324922498857,6.55258046855126));
#73743=CARTESIAN_POINT('Ctrl Pts',(1.55044907111383,0.125427329077983,6.55157328176952));
#73744=CARTESIAN_POINT('Ctrl Pts',(1.5509703451918,0.118807942370117,6.5510962564927));
#73745=CARTESIAN_POINT('Ctrl Pts',(1.55213790599631,0.102661339850625,6.54993884845402));
#73746=CARTESIAN_POINT('Ctrl Pts',(1.55273889390393,0.0931309271712147,
6.54926092911641));
#73747=CARTESIAN_POINT('Ctrl Pts',(1.55462859139125,0.058019170562004,6.54678058854424));
#73748=CARTESIAN_POINT('Ctrl Pts',(1.55537326532875,0.0324110880418939,
6.54500524316457));
#73749=CARTESIAN_POINT('Ctrl Pts',(1.55566915878671,-0.0353288835396494,
6.54037009980746));
#73750=CARTESIAN_POINT('Ctrl Pts',(1.55414200454341,-0.077445443790286,
6.53755047812076));
#73751=CARTESIAN_POINT('Ctrl Pts',(1.54047969579514,-0.254832002753672,
6.5257492407853));
#73752=CARTESIAN_POINT('Ctrl Pts',(1.51237382546127,-0.388253205563357,
6.5169986673229));
#73753=CARTESIAN_POINT('Ctrl Pts',(1.45970282601969,-0.537933460574715,
6.50606888377256));
#73754=CARTESIAN_POINT('Ctrl Pts',(1.45162498154463,-0.559365325783071,
6.5044774958865));
#73755=CARTESIAN_POINT('Ctrl Pts',(1.43813695070997,-0.592889148365251,
6.5019417192252));
#73756=CARTESIAN_POINT('Ctrl Pts',(1.43304021444263,-0.605104251887188,
6.50100783491967));
#73757=CARTESIAN_POINT('Ctrl Pts',(1.42321318292333,-0.627835502484376,
6.49925048099795));
#73758=CARTESIAN_POINT('Ctrl Pts',(1.418520598923,-0.6383670413574,6.49842834591411));
#73759=CARTESIAN_POINT('Ctrl Pts',(1.40770007598231,-0.661942923433136,
6.49656943269474));
#73760=CARTESIAN_POINT('Ctrl Pts',(1.40150712732724,-0.674956060674805,
6.49553046691707));
#73761=CARTESIAN_POINT('Ctrl Pts',(1.38204342316198,-0.714431622898365,
6.49233801361806));
#73762=CARTESIAN_POINT('Ctrl Pts',(1.36819802097219,-0.740601459368662,
6.4901648115206));
#73763=CARTESIAN_POINT('Ctrl Pts',(1.33378667858496,-0.80138202287171,6.48497818950137));
#73764=CARTESIAN_POINT('Ctrl Pts',(1.3126078443408,-0.835619659771455,6.48194542037987));
#73765=CARTESIAN_POINT('Ctrl Pts',(1.25276809677292,-0.924458895003148,
6.47378142644174));
#73766=CARTESIAN_POINT('Ctrl Pts',(1.21187362374784,-0.977452507544467,
6.46859517012091));
#73767=CARTESIAN_POINT('Ctrl Pts',(1.11917555562601,-1.08278390434268,6.4577138192272));
#73768=CARTESIAN_POINT('Ctrl Pts',(1.06680247194667,-1.13442033270303,6.45203179458958));
#73769=CARTESIAN_POINT('Ctrl Pts',(0.998650460172741,-1.19270295624394,
6.4453397165859));
#73770=CARTESIAN_POINT('Ctrl Pts',(0.986164747936227,-1.20304705988235,
6.44414019033588));
#73771=CARTESIAN_POINT('Ctrl Pts',(0.967270361846445,-1.21820871920309,
6.44236683388902));
#73772=CARTESIAN_POINT('Ctrl Pts',(0.960982939541029,-1.22317465390252,
6.44178347572466));
#73773=CARTESIAN_POINT('Ctrl Pts',(0.95003710435235,-1.23168339872076,6.44077992471751));
#73774=CARTESIAN_POINT('Ctrl Pts',(0.94539678650017,-1.23524872536742,6.44035819616115));
#73775=CARTESIAN_POINT('Ctrl Pts',(0.934346987829686,-1.24363994784659,
6.43936267143485));
#73776=CARTESIAN_POINT('Ctrl Pts',(0.927920151949377,-1.24844255483235,
6.43879048124495));
#73777=CARTESIAN_POINT('Ctrl Pts',(0.908348774127612,-1.26283310326922,
6.43706759607805));
#73778=CARTESIAN_POINT('Ctrl Pts',(0.895090211005005,-1.27226511038981,
6.43592687347324));
#73779=CARTESIAN_POINT('Ctrl Pts',(0.826076521575695,-1.31974770241644,
6.43010984067056));
#73780=CARTESIAN_POINT('Ctrl Pts',(0.768029270007336,-1.35435210528135,
6.42561441575182));
#73781=CARTESIAN_POINT('Ctrl Pts',(0.595859104949023,-1.44234793327941,
6.41284677000393));
#73782=CARTESIAN_POINT('Ctrl Pts',(0.477284981955651,-1.48580327132771,
6.40467696418149));
#73783=CARTESIAN_POINT('Ctrl Pts',(0.333383973601136,-1.51951245471997,
6.39447929640829));
#73784=CARTESIAN_POINT('Ctrl Pts',(0.311889299054972,-1.52406953769659,
6.39295041365603));
#73785=CARTESIAN_POINT('Ctrl Pts',(0.277618940426029,-1.53057987375258,
6.3904999646751));
#73786=CARTESIAN_POINT('Ctrl Pts',(0.264902497424346,-1.53283191342594,
6.3895879216786));
#73787=CARTESIAN_POINT('Ctrl Pts',(0.240734314445973,-1.53680229869426,
6.38784853715044));
#73788=CARTESIAN_POINT('Ctrl Pts',(0.229288495540479,-1.5385516201553,6.38702224217976));
#73789=CARTESIAN_POINT('Ctrl Pts',(0.203044868390537,-1.54226321940958,
6.38512132713153));
#73790=CARTESIAN_POINT('Ctrl Pts',(0.188236419536967,-1.54414056289323,
6.38404410119657));
#73791=CARTESIAN_POINT('Ctrl Pts',(0.141077800272161,-1.54943067564035,
6.38059779986305));
#73792=CARTESIAN_POINT('Ctrl Pts',(0.108648498473489,-1.55204174449783,
6.37820413364808));
#73793=CARTESIAN_POINT('Ctrl Pts',(0.0302669225208374,-1.55588421969001,
6.37235769627072));
#73794=CARTESIAN_POINT('Ctrl Pts',(-0.015702600348668,-1.55609914166582,
6.36887799714372));
#73795=CARTESIAN_POINT('Ctrl Pts',(-0.121722477203221,-1.55189658106195,
6.3607503367614));
#73796=CARTESIAN_POINT('Ctrl Pts',(-0.181643068539324,-1.54602863598897,
6.35607949086564));
#73797=CARTESIAN_POINT('Ctrl Pts',(-0.315996815293859,-1.52495193879886,
6.3455356476985));
#73798=CARTESIAN_POINT('Ctrl Pts',(-0.389972206914176,-1.50773229667347,
6.33967878809157));
#73799=CARTESIAN_POINT('Ctrl Pts',(-0.474580534252851,-1.4813899675131,
6.33310789414783));
#73800=CARTESIAN_POINT('Ctrl Pts',(-0.486711592315749,-1.47744873796477,
6.33216906740336));
#73801=CARTESIAN_POINT('Ctrl Pts',(-0.505712798017733,-1.47101603753172,
6.33070522056862));
#73802=CARTESIAN_POINT('Ctrl Pts',(-0.51261588740434,-1.4686247221823,6.33017480470086));
#73803=CARTESIAN_POINT('Ctrl Pts',(-0.525761570423404,-1.46396691271776,
6.32916773390703));
#73804=CARTESIAN_POINT('Ctrl Pts',(-0.53200682079032,-1.46170896382921,
6.32869064108331));
#73805=CARTESIAN_POINT('Ctrl Pts',(-0.547202136870961,-1.45610486100228,
6.32753274381423));
#73806=CARTESIAN_POINT('Ctrl Pts',(-0.556136382162363,-1.4527160361182,
6.32685440797989));
#73807=CARTESIAN_POINT('Ctrl Pts',(-0.588943574744586,-1.43992499814422,
6.32437058954716));
#73808=CARTESIAN_POINT('Ctrl Pts',(-0.612615536060612,-1.43001431188423,
6.32259228171073));
#73809=CARTESIAN_POINT('Ctrl Pts',(-0.674574841011769,-1.4022527293616,
6.31794688417625));
#73810=CARTESIAN_POINT('Ctrl Pts',(-0.712400083722901,-1.3834198792131,
6.31512019105145));
#73811=CARTESIAN_POINT('Ctrl Pts',(-0.868154652762827,-1.29778616488796,
6.30333104536437));
#73812=CARTESIAN_POINT('Ctrl Pts',(-0.97784575307332,-1.21727449455587,
6.29459736747511));
#73813=CARTESIAN_POINT('Ctrl Pts',(-1.09230440598828,-1.10769067806239,
6.28368350946017));
#73814=CARTESIAN_POINT('Ctrl Pts',(-1.10853666849747,-1.09144579065017,
6.28208797814043));
#73815=CARTESIAN_POINT('Ctrl Pts',(-1.13355761712477,-1.0652712844266,6.27954708754934));
#73816=CARTESIAN_POINT('Ctrl Pts',(-1.14258952818329,-1.05557800820723,
6.27861230558493));
#73817=CARTESIAN_POINT('Ctrl Pts',(-1.15924677646181,-1.03723674336491,
6.27685416586808));
#73818=CARTESIAN_POINT('Ctrl Pts',(-1.16690196894127,-1.02861699978342,
6.2760321541548));
#73819=CARTESIAN_POINT('Ctrl Pts',(-1.18389752983173,-1.00904610418042,
6.27417473180535));
#73820=CARTESIAN_POINT('Ctrl Pts',(-1.19318301380305,-0.998048932248872,
6.27313714862679));
#73821=CARTESIAN_POINT('Ctrl Pts',(-1.22054427473032,-0.964716267380358,
6.27000931033168));
#73822=CARTESIAN_POINT('Ctrl Pts',(-1.23815423753042,-0.942008325250203,
6.26790082688344));
#73823=CARTESIAN_POINT('Ctrl Pts',(-1.27823778129334,-0.887253923609298,
6.26286527664387));
#73824=CARTESIAN_POINT('Ctrl Pts',(-1.3001498714042,-0.854822329771179,
6.25991974081589));
#73825=CARTESIAN_POINT('Ctrl Pts',(-1.37238293729112,-0.738699749220427,
6.2495078807041));
#73826=CARTESIAN_POINT('Ctrl Pts',(-1.41602951579031,-0.651129947446211,
6.24187405099271));
#73827=CARTESIAN_POINT('Ctrl Pts',(-1.46977048519191,-0.511880553029146,
6.23037358139925));
#73828=CARTESIAN_POINT('Ctrl Pts',(-1.48595504695095,-0.462802043067066,
6.22643684985847));
#73829=CARTESIAN_POINT('Ctrl Pts',(-1.50289908952527,-0.401276164922847,
6.22171066780392));
#73830=CARTESIAN_POINT('Ctrl Pts',(-1.50599145246482,-0.389509953027391,
6.22081613317821));
#73831=CARTESIAN_POINT('Ctrl Pts',(-1.5106886891948,-0.370744475525187,
6.2194054930009));
#73832=CARTESIAN_POINT('Ctrl Pts',(-1.51238361689905,-0.36376858402326,
6.21888459812312));
#73833=CARTESIAN_POINT('Ctrl Pts',(-1.51556714190145,-0.350259028237999,
6.21788290659448));
#73834=CARTESIAN_POINT('Ctrl Pts',(-1.51706190148728,-0.343727126778364,
6.21740180350685));
#73835=CARTESIAN_POINT('Ctrl Pts',(-1.51999579009791,-0.3305143697706,6.21643476606779));
#73836=CARTESIAN_POINT('Ctrl Pts',(-1.52143320471308,-0.323833226670136,
6.21594892682967));
#73837=CARTESIAN_POINT('Ctrl Pts',(-1.52479974894767,-0.307668063178696,
6.21478054706931));
#73838=CARTESIAN_POINT('Ctrl Pts',(-1.52668451867039,-0.298174954858204,
6.21410030742499));
#73839=CARTESIAN_POINT('Ctrl Pts',(-1.53162855524272,-0.271996252420891,
6.21223908357287));
#73840=CARTESIAN_POINT('Ctrl Pts',(-1.53450376919123,-0.255276768131256,
6.2110666868383));
#73841=CARTESIAN_POINT('Ctrl Pts',(-1.54927635669024,-0.16007426657775,
6.20446598056749));
#73842=CARTESIAN_POINT('Ctrl Pts',(-1.55542661858188,-0.0808133767859318,
6.19925484041338));
#73843=CARTESIAN_POINT('Ctrl Pts',(-1.55549934726413,-0.00142501258095274,
6.19403090372774));
#73844=CARTESIAN_POINT('Ctrl Pts',(-1.55549934719923,-0.00142508342168083,
6.19403090838922));
#73845=CARTESIAN_POINT('Ctrl Pts',(-1.55549978240474,-0.00095005026471773,
6.19399965011654));
#73846=CARTESIAN_POINT('Ctrl Pts',(-1.55550000000003,-0.000475022378848535,
6.19396839221188));
#73847=CARTESIAN_POINT('Ctrl Pts',(-1.5555,8.75720568004264E-11,6.19393713463064));
#73848=CARTESIAN_POINT('Ctrl Pts',(-1.55549999442795,-0.000131661105043114,
6.05447729365254));
#73849=CARTESIAN_POINT('Ctrl Pts',(-1.55549891885685,-0.0128389130955966,
6.05538373546313));
#73850=CARTESIAN_POINT('Ctrl Pts',(-1.55534213067335,-0.0255453141076208,
6.05629500695454));
#73851=CARTESIAN_POINT('Ctrl Pts',(-1.55453944217419,-0.0581797939337343,
6.05864874442834));
#73852=CARTESIAN_POINT('Ctrl Pts',(-1.5536660460136,-0.0780993893125099,
6.06009817714194));
#73853=CARTESIAN_POINT('Ctrl Pts',(-1.54739798082632,-0.177395494315716,
6.0673905123979));
#73854=CARTESIAN_POINT('Ctrl Pts',(-1.53630276923752,-0.25628065862964,
6.07340723386863));
#73855=CARTESIAN_POINT('Ctrl Pts',(-1.49532160127272,-0.442709037849519,
6.08810130202347));
#73856=CARTESIAN_POINT('Ctrl Pts',(-1.45980906302283,-0.548576960683833,
6.0968517184342));
#73857=CARTESIAN_POINT('Ctrl Pts',(-1.40476453494278,-0.668306883055246,
6.10674733926469));
#73858=CARTESIAN_POINT('Ctrl Pts',(-1.39586693178538,-0.686697241296948,
6.10826634707701));
#73859=CARTESIAN_POINT('Ctrl Pts',(-1.38261906271256,-0.712756831298517,
6.11041217087565));
#73860=CARTESIAN_POINT('Ctrl Pts',(-1.37856231790894,-0.720571799791614,
6.1110548040551));
#73861=CARTESIAN_POINT('Ctrl Pts',(-1.37130193766944,-0.734272524136705,
6.11217934078617));
#73862=CARTESIAN_POINT('Ctrl Pts',(-1.36812631938116,-0.740172631655696,
6.11266289592588));
#73863=CARTESIAN_POINT('Ctrl Pts',(-1.36108744478608,-0.753050343441263,
6.11371665263352));
#73864=CARTESIAN_POINT('Ctrl Pts',(-1.35720853918558,-0.760018973927848,
6.11428587076964));
#73865=CARTESIAN_POINT('Ctrl Pts',(-1.34567799308509,-0.780364311208439,
6.11594569784607));
#73866=CARTESIAN_POINT('Ctrl Pts',(-1.33788070797264,-0.793657972628437,
6.11702762318056));
#73867=CARTESIAN_POINT('Ctrl Pts',(-1.29968268024331,-0.85661892677765,
6.12215022217867));
#73868=CARTESIAN_POINT('Ctrl Pts',(-1.26670330808152,-0.904674144576514,
6.12605616932858));
#73869=CARTESIAN_POINT('Ctrl Pts',(-1.14977676749239,-1.05607608183673,
6.13873967802301));
#73870=CARTESIAN_POINT('Ctrl Pts',(-1.05528414622087,-1.15050278480546,
6.14732639041046));
#73871=CARTESIAN_POINT('Ctrl Pts',(-0.931288871359076,-1.24612817779305,
6.15810397990325));
#73872=CARTESIAN_POINT('Ctrl Pts',(-0.912324978321146,-1.26007834293831,
6.1597387845353));
#73873=CARTESIAN_POINT('Ctrl Pts',(-0.881930092785917,-1.28139147088921,
6.16234299407571));
#73874=CARTESIAN_POINT('Ctrl Pts',(-0.870706138051312,-1.28904444860889,
6.1633013095483));
#73875=CARTESIAN_POINT('Ctrl Pts',(-0.849612536435622,-1.30302579000318,
6.16509701914697));
#73876=CARTESIAN_POINT('Ctrl Pts',(-0.83976872395198,-1.30939151820358,
6.16593293082245));
#73877=CARTESIAN_POINT('Ctrl Pts',(-0.817375814277437,-1.32351603187859,
6.16783033829811));
#73878=CARTESIAN_POINT('Ctrl Pts',(-0.804786552959673,-1.331208655594,6.16889417812965));
#73879=CARTESIAN_POINT('Ctrl Pts',(-0.766054414817103,-1.35412556682334,
6.17215962239853));
#73880=CARTESIAN_POINT('Ctrl Pts',(-0.739576607306232,-1.36876646073595,
6.17438173397606));
#73881=CARTESIAN_POINT('Ctrl Pts',(-0.676046610608144,-1.40151374436026,
6.1796931399739));
#73882=CARTESIAN_POINT('Ctrl Pts',(-0.638669360039749,-1.41893647949542,
6.18280268555536));
#73883=CARTESIAN_POINT('Ctrl Pts',(-0.540538333491575,-1.4600153274615,
6.19091865722211));
#73884=CARTESIAN_POINT('Ctrl Pts',(-0.478911087475831,-1.48137425091665,
6.19597231066857));
#73885=CARTESIAN_POINT('Ctrl Pts',(-0.34612826006643,-1.51824026452634,
6.20665661292017));
#73886=CARTESIAN_POINT('Ctrl Pts',(-0.274843638463538,-1.53274958321898,
6.21227455061706));
#73887=CARTESIAN_POINT('Ctrl Pts',(-0.186573757483619,-1.54435692800793,
6.2189195114759));
#73888=CARTESIAN_POINT('Ctrl Pts',(-0.170314155907629,-1.54623453351541,
6.22013055025551));
#73889=CARTESIAN_POINT('Ctrl Pts',(-0.145903378087527,-1.54866365067379,
6.22192639304776));
#73890=CARTESIAN_POINT('Ctrl Pts',(-0.137773153591343,-1.54940810144349,
6.22252081619508));
#73891=CARTESIAN_POINT('Ctrl Pts',(-0.123646269454219,-1.55058956283505,
6.22354682706165));
#73892=CARTESIAN_POINT('Ctrl Pts',(-0.117652571583259,-1.55105585580637,
6.22397997187299));
#73893=CARTESIAN_POINT('Ctrl Pts',(-0.103346461462103,-1.55208542435959,
6.22500872667083));
#73894=CARTESIAN_POINT('Ctrl Pts',(-0.0950320274336128,-1.55261668733294,
6.22560256886105));
#73895=CARTESIAN_POINT('Ctrl Pts',(-0.0695016890922142,-1.5540421275825,
6.22741471569362));
#73896=CARTESIAN_POINT('Ctrl Pts',(-0.0522741823592893,-1.5547169816929,
6.22862176272108));
#73897=CARTESIAN_POINT('Ctrl Pts',(-0.0112278487424111,-1.55564179724489,
6.23146782196757));
#73898=CARTESIAN_POINT('Ctrl Pts',(0.0125929534183763,-1.55563138686882,
6.23309560309643));
#73899=CARTESIAN_POINT('Ctrl Pts',(0.106972561377428,-1.55342189114631,
6.23948331706542));
#73900=CARTESIAN_POINT('Ctrl Pts',(0.17735029448606,-1.54696830419104,6.24411274157835));
#73901=CARTESIAN_POINT('Ctrl Pts',(0.338549188883912,-1.52103694495766,
6.25486031440793));
#73902=CARTESIAN_POINT('Ctrl Pts',(0.428539046689323,-1.49817237862083,
6.26097722623209));
#73903=CARTESIAN_POINT('Ctrl Pts',(0.538795062049203,-1.45940616855446,
6.26901400661568));
#73904=CARTESIAN_POINT('Ctrl Pts',(0.561444813765082,-1.45084323598586,
6.27069426177093));
#73905=CARTESIAN_POINT('Ctrl Pts',(0.596608897201168,-1.43660242914495,
6.27335452284987));
#73906=CARTESIAN_POINT('Ctrl Pts',(0.609264154830248,-1.43128120358727,
6.27432260668622));
#73907=CARTESIAN_POINT('Ctrl Pts',(0.632683683067844,-1.42106698637323,
6.27613501748594));
#73908=CARTESIAN_POINT('Ctrl Pts',(0.643465876706036,-1.41621738230264,
6.27697781338439));
#73909=CARTESIAN_POINT('Ctrl Pts',(0.667451370651397,-1.40509875974352,
6.27887204277289));
#73910=CARTESIAN_POINT('Ctrl Pts',(0.680623540577913,-1.39876567935891,
6.2799256274082));
#73911=CARTESIAN_POINT('Ctrl Pts',(0.72010536681641,-1.37909339211758,6.28312519625929));
#73912=CARTESIAN_POINT('Ctrl Pts',(0.746125324150211,-1.36519123418145,
6.28529048893181));
#73913=CARTESIAN_POINT('Ctrl Pts',(0.833910381606084,-1.31502931933881,
6.29279746022178));
#73914=CARTESIAN_POINT('Ctrl Pts',(0.893552150896871,-1.27525321279852,
6.29825550893196));
#73915=CARTESIAN_POINT('Ctrl Pts',(1.02171555102791,-1.17636256027635,6.31075288974442));
#73916=CARTESIAN_POINT('Ctrl Pts',(1.08825879703488,-1.11508974398282,6.31781402111175));
#73917=CARTESIAN_POINT('Ctrl Pts',(1.16870379465346,-1.0269160711064,6.32687110302669));
#73918=CARTESIAN_POINT('Ctrl Pts',(1.1876908866188,-1.00489591618518,6.32905225508688));
#73919=CARTESIAN_POINT('Ctrl Pts',(1.21263661074336,-0.974269695660277,
6.33196478546652));
#73920=CARTESIAN_POINT('Ctrl Pts',(1.21914093808951,-0.966118201150408,
6.33272877653351));
#73921=CARTESIAN_POINT('Ctrl Pts',(1.22940686109999,-0.952983725242446,
6.33394120395661));
#73922=CARTESIAN_POINT('Ctrl Pts',(1.23322114925306,-0.948042621149047,
6.33439317809719));
#73923=CARTESIAN_POINT('Ctrl Pts',(1.24130866152169,-0.937434492690548,
6.33535449875502));
#73924=CARTESIAN_POINT('Ctrl Pts',(1.24557307774413,-0.93176087848597,6.33586321199216));
#73925=CARTESIAN_POINT('Ctrl Pts',(1.25649583159727,-0.91701964095626,6.33717155602481));
#73926=CARTESIAN_POINT('Ctrl Pts',(1.26309505027691,-0.907908426095713,
6.3379672581638));
#73927=CARTESIAN_POINT('Ctrl Pts',(1.29257150196101,-0.866268198171507,
6.3415495616451));
#73928=CARTESIAN_POINT('Ctrl Pts',(1.31429706773243,-0.832937883801895,
6.34426882814623));
#73929=CARTESIAN_POINT('Ctrl Pts',(1.38144977422979,-0.720732906291548,
6.35307639058692));
#73930=CARTESIAN_POINT('Ctrl Pts',(1.4212382337216,-0.638704294957985,6.35898502313633));
#73931=CARTESIAN_POINT('Ctrl Pts',(1.48029636208297,-0.483648818504521,
6.3699618121975));
#73932=CARTESIAN_POINT('Ctrl Pts',(1.50186758119281,-0.411807182706992,
6.37497818575942));
#73933=CARTESIAN_POINT('Ctrl Pts',(1.52254992136098,-0.319100488292828,
6.3815521714696));
#73934=CARTESIAN_POINT('Ctrl Pts',(1.52654176636895,-0.299422036444443,
6.38295276442892));
#73935=CARTESIAN_POINT('Ctrl Pts',(1.53244137061089,-0.267143979001509,
6.38526150707143));
#73936=CARTESIAN_POINT('Ctrl Pts',(1.53457725851367,-0.254588059733397,
6.38616237509039));
#73937=CARTESIAN_POINT('Ctrl Pts',(1.53843459194216,-0.230097020159152,
6.38792570395225));
#73938=CARTESIAN_POINT('Ctrl Pts',(1.54017191326583,-0.218165292539245,
6.38878759405468));
#73939=CARTESIAN_POINT('Ctrl Pts',(1.54396393584145,-0.189814147942544,
6.39084282233865));
#73940=CARTESIAN_POINT('Ctrl Pts',(1.54589564861465,-0.173380074505319,
6.39203993790921));
#73941=CARTESIAN_POINT('Ctrl Pts',(1.55174799834675,-0.115663056454063,
6.39626613263632));
#73942=CARTESIAN_POINT('Ctrl Pts',(1.55427944975152,-0.0742603275400437,
6.39933748552198));
#73943=CARTESIAN_POINT('Ctrl Pts',(1.55654605810355,0.0331765021273517,
6.40741407800293));
#73944=CARTESIAN_POINT('Ctrl Pts',(1.55373695386934,0.0991775117761391,
6.41248251787791));
#73945=CARTESIAN_POINT('Ctrl Pts',(1.53627018918646,0.263119046787456,6.4252457416261));
#73946=CARTESIAN_POINT('Ctrl Pts',(1.51644212052324,0.360227768913582,6.43297100283408));
#73947=CARTESIAN_POINT('Ctrl Pts',(1.48313036904305,0.469180795237614,6.44145780121015));
#73948=CARTESIAN_POINT('Ctrl Pts',(1.47852583983205,0.483495289971375,6.44256872107262));
#73949=CARTESIAN_POINT('Ctrl Pts',(1.47115694426745,0.505313136160052,6.44425337044385));
#73950=CARTESIAN_POINT('Ctrl Pts',(1.4685412448811,0.512865225841132,6.44483490633406));
#73951=CARTESIAN_POINT('Ctrl Pts',(1.46362645685252,0.526709323486124,6.44589758608852));
#73952=CARTESIAN_POINT('Ctrl Pts',(1.46134485434721,0.533006882001296,6.44637965370148));
#73953=CARTESIAN_POINT('Ctrl Pts',(1.45592503669439,0.54766993422602,6.44749916469894));
#73954=CARTESIAN_POINT('Ctrl Pts',(1.45275533334928,0.556023399668781,6.4481347626378));
#73955=CARTESIAN_POINT('Ctrl Pts',(1.44202694052589,0.58357894219157,6.45022564834446));
#73956=CARTESIAN_POINT('Ctrl Pts',(1.43415776785115,0.602658843415823,6.45166410361225));
#73957=CARTESIAN_POINT('Ctrl Pts',(1.4137122332063,0.649561281959369,6.45519052282764));
#73958=CARTESIAN_POINT('Ctrl Pts',(1.40069178859891,0.677181576990041,6.45725868628581));
#73959=CARTESIAN_POINT('Ctrl Pts',(1.32969449510543,0.81696493721394,6.46777030344727));
#73960=CARTESIAN_POINT('Ctrl Pts',(1.2590328286754,0.922148345691461,6.47587116936669));
#73961=CARTESIAN_POINT('Ctrl Pts',(1.14983349281024,1.04838745618907,6.48714364232961));
#73962=CARTESIAN_POINT('Ctrl Pts',(1.12204098814967,1.0780801824028,6.4899249123312));
#73963=CARTESIAN_POINT('Ctrl Pts',(1.08114420445354,1.11847698989951,6.49392631879746));
#73964=CARTESIAN_POINT('Ctrl Pts',(1.06897839805036,1.1301100448707,6.4951059244687));
#73965=CARTESIAN_POINT('Ctrl Pts',(1.04783080289291,1.1496845259716,6.49714007609109));
#73966=CARTESIAN_POINT('Ctrl Pts',(1.03894141183013,1.15772390013262,6.49799036176624));
#73967=CARTESIAN_POINT('Ctrl Pts',(1.02050550359441,1.17401360693342,6.49974470491181));
#73968=CARTESIAN_POINT('Ctrl Pts',(1.01094975540191,1.18225209106726,6.5006491673846));
#73969=CARTESIAN_POINT('Ctrl Pts',(0.986375476327052,1.20292300773872,6.50296362597425));
#73970=CARTESIAN_POINT('Ctrl Pts',(0.971221888887568,1.21519065222927,6.50438014154919));
#73971=CARTESIAN_POINT('Ctrl Pts',(0.899359113021684,1.27116455903029,6.51105167738562));
#73972=CARTESIAN_POINT('Ctrl Pts',(0.839914430006482,1.311200646384,6.5164453010482));
#73973=CARTESIAN_POINT('Ctrl Pts',(0.753405667824963,1.36116213870039,6.5241086207056));
#73974=CARTESIAN_POINT('Ctrl Pts',(0.728497133916217,1.37465425002099,6.526294294851));
#73975=CARTESIAN_POINT('Ctrl Pts',(0.614046406490459,1.43266372666506,6.53622575270472));
#73976=CARTESIAN_POINT('Ctrl Pts',(0.520700832000476,1.46916712238704,6.54404073858959));
#73977=CARTESIAN_POINT('Ctrl Pts',(0.410127217922548,1.50053285047216,6.55260074366641));
#73978=CARTESIAN_POINT('Ctrl Pts',(0.395704787747305,1.50440052333271,6.55370375180703));
#73979=CARTESIAN_POINT('Ctrl Pts',(0.37350169210127,1.51001332784119,6.5553789449783));
#73980=CARTESIAN_POINT('Ctrl Pts',(0.365760039930331,1.51190719455393,6.55595880913418));
#73981=CARTESIAN_POINT('Ctrl Pts',(0.351482620879242,1.51528384260212,6.5570200143663));
#73982=CARTESIAN_POINT('Ctrl Pts',(0.344951591208921,1.51678395264939,6.55750225816576));
#73983=CARTESIAN_POINT('Ctrl Pts',(0.32965882952111,1.52019265431416,6.55862421992107));
#73984=CARTESIAN_POINT('Ctrl Pts',(0.320890006140209,1.52206775946427,6.55926206409218));
#73985=CARTESIAN_POINT('Ctrl Pts',(0.291698005184473,1.52804661109992,6.56136880287382));
#73986=CARTESIAN_POINT('Ctrl Pts',(0.271207647899094,1.53181614173672,6.56282051340074));
#73987=CARTESIAN_POINT('Ctrl Pts',(0.220115559116338,1.54015790641689,6.56638743237477));
#73988=CARTESIAN_POINT('Ctrl Pts',(0.189440707307601,1.54423110309084,6.56848224602219));
#73989=CARTESIAN_POINT('Ctrl Pts',(0.027483329973648,1.5608375705228,6.57939271554638));
#73990=CARTESIAN_POINT('Ctrl Pts',(-0.104872057558046,1.55755356377785,
6.58784179728223));
#73991=CARTESIAN_POINT('Ctrl Pts',(-0.270992468295974,1.53213974314578,
6.599238663491));
#73992=CARTESIAN_POINT('Ctrl Pts',(-0.306550283034025,1.52542312126633,
6.60172194868961));
#73993=CARTESIAN_POINT('Ctrl Pts',(-0.355988635001923,1.51428620108668,
6.60525473743337));
#73994=CARTESIAN_POINT('Ctrl Pts',(-0.370092056801003,1.51090120513725,
6.60627175807881));
#73995=CARTESIAN_POINT('Ctrl Pts',(-0.395823132000781,1.50434355050705,
6.60814535298705));
#73996=CARTESIAN_POINT('Ctrl Pts',(-0.407465301667483,1.50123198836702,
6.60899991344401));
#73997=CARTESIAN_POINT('Ctrl Pts',(-0.431119556579752,1.49461457799594,
6.61075078718267));
#73998=CARTESIAN_POINT('Ctrl Pts',(-0.443127811934734,1.49109843209545,
6.611647379321));
#73999=CARTESIAN_POINT('Ctrl Pts',(-0.473242258886061,1.48188470648877,
6.61391610880233));
#74000=CARTESIAN_POINT('Ctrl Pts',(-0.491288546861568,1.47600000793858,
6.61529425675202));
#74001=CARTESIAN_POINT('Ctrl Pts',(-0.569961919293046,1.44874285369375,
6.6213871515828));
#74002=CARTESIAN_POINT('Ctrl Pts',(-0.629330599190891,1.42395694924085,
6.62621186979829));
#74003=CARTESIAN_POINT('Ctrl Pts',(-0.776810511410972,1.35135803404859,
6.63877269413997));
#74004=CARTESIAN_POINT('Ctrl Pts',(-0.862146972872839,1.2985776765281,6.64661477972965));
#74005=CARTESIAN_POINT('Ctrl Pts',(-0.975603447949265,1.21226248699643,
6.65754609428304));
#74006=CARTESIAN_POINT('Ctrl Pts',(-1.00832655974209,1.18518381912265,6.66076401494641));
#74007=CARTESIAN_POINT('Ctrl Pts',(-1.04868846396093,1.14890047185223,6.66477942967224));
#74008=CARTESIAN_POINT('Ctrl Pts',(-1.05738343732964,1.14090318508391,6.66564732536241));
#74009=CARTESIAN_POINT('Ctrl Pts',(-1.07124397017137,1.12786023849808,6.66703432232451));
#74010=CARTESIAN_POINT('Ctrl Pts',(-1.07646677856929,1.1228765032505,6.66755777736794));
#74011=CARTESIAN_POINT('Ctrl Pts',(-1.08667320815643,1.11300060732359,6.66858199947769));
#74012=CARTESIAN_POINT('Ctrl Pts',(-1.09165890142797,1.10811094194642,6.66908291127039));
#74013=CARTESIAN_POINT('Ctrl Pts',(-1.10310672489565,1.09673135977941,6.67023493997014));
#74014=CARTESIAN_POINT('Ctrl Pts',(-1.10954491903652,1.09021750370645,6.67088423615697));
#74015=CARTESIAN_POINT('Ctrl Pts',(-1.13463418096081,1.06438091115564,6.67342196750682));
#74016=CARTESIAN_POINT('Ctrl Pts',(-1.1528423043679,1.0446321297173,6.67528016670533));
#74017=CARTESIAN_POINT('Ctrl Pts',(-1.20055264881421,0.990116959667581,
6.68022747335239));
#74018=CARTESIAN_POINT('Ctrl Pts',(-1.22905388113729,0.954507940817489,
6.68326932420219));
#74019=CARTESIAN_POINT('Ctrl Pts',(-1.31795762155564,0.832834981930269,
6.69324411218612));
#74020=CARTESIAN_POINT('Ctrl Pts',(-1.37120052306651,0.741912829850248,
6.70006532584687));
#74021=CARTESIAN_POINT('Ctrl Pts',(-1.43090289758623,0.61121708185954,6.70978643701531));
#74022=CARTESIAN_POINT('Ctrl Pts',(-1.44562420875239,0.575534248225999,
6.71243005202752));
#74023=CARTESIAN_POINT('Ctrl Pts',(-1.46417297234898,0.525357116757619,
6.71615584986652));
#74024=CARTESIAN_POINT('Ctrl Pts',(-1.46914163032768,0.511297796009036,
6.71720061972948));
#74025=CARTESIAN_POINT('Ctrl Pts',(-1.47743860611034,0.486700612298808,
6.71903112349834));
#74026=CARTESIAN_POINT('Ctrl Pts',(-1.48085822865961,0.476194514937793,
6.71981380790208));
#74027=CARTESIAN_POINT('Ctrl Pts',(-1.48781391455189,0.454024816074234,
6.72146764272665));
#74028=CARTESIAN_POINT('Ctrl Pts',(-1.49132538049082,0.442354351001214,
6.7223395357087));
#74029=CARTESIAN_POINT('Ctrl Pts',(-1.49948744887246,0.414025072302984,
6.7244597309339));
#74030=CARTESIAN_POINT('Ctrl Pts',(-1.50399794334546,0.397327964505051,
6.72571246942175));
#74031=CARTESIAN_POINT('Ctrl Pts',(-1.51303652285075,0.361506394191948,
6.72840778811516));
#74032=CARTESIAN_POINT('Ctrl Pts',(-1.51748241425307,0.34236449968466,6.72985273621019));
#74033=CARTESIAN_POINT('Ctrl Pts',(-1.54413072324572,0.216887687179912,
6.73935714262994));
#74034=CARTESIAN_POINT('Ctrl Pts',(-1.55550000000864,0.108580928990684,
6.74774433786957));
#74035=CARTESIAN_POINT('Ctrl Pts',(-1.5555,-1.23764089254852E-10,6.75616363716894));
#74036=CARTESIAN_POINT('Origin',(0.,0.,-1.2940562256037));
#74037=CARTESIAN_POINT('',(-1.5555,7.12052432324671E-12,7.59515300361487));
#74038=CARTESIAN_POINT('',(-1.55549969139622,0.000979831791607279,7.45702425421034));
#74039=CARTESIAN_POINT('',(-1.5555,-1.46451138874614E-13,-1.2940562256037));
#74040=CARTESIAN_POINT('',(-1.55549928515668,0.00114196767205917,7.59506639552504));
#74041=CARTESIAN_POINT('Ctrl Pts',(-1.5555,7.12052432324671E-12,7.59515300361487));
#74042=CARTESIAN_POINT('Ctrl Pts',(-1.5555,0.000381318786656916,7.59512425884146));
#74043=CARTESIAN_POINT('Ctrl Pts',(-1.55549985978398,0.000762638266299459,
7.5950955104834));
#74044=CARTESIAN_POINT('Ctrl Pts',(-1.55549957935039,0.00114395836942135,
7.59506675854921));
#74045=CARTESIAN_POINT('Ctrl Pts',(-1.55549958078474,0.00114200635226231,
7.59506690573332));
#74046=CARTESIAN_POINT('Ctrl Pts',(-1.55539690258863,0.140997525261179,
7.58452165790019));
#74047=CARTESIAN_POINT('Ctrl Pts',(-1.5364350984294,0.280184167848922,7.57346929296716));
#74048=CARTESIAN_POINT('Ctrl Pts',(-1.49113558112083,0.443838852949233,
7.56057837485354));
#74049=CARTESIAN_POINT('Ctrl Pts',(-1.48230784617497,0.472484912046339,
7.55832948361562));
#74050=CARTESIAN_POINT('Ctrl Pts',(-1.46940474836623,0.510423321243775,
7.55537642826436));
#74051=CARTESIAN_POINT('Ctrl Pts',(-1.46605908649633,0.519954854628499,
7.55463669503922));
#74052=CARTESIAN_POINT('Ctrl Pts',(-1.46032643477296,0.535791364834251,
7.55341206289291));
#74053=CARTESIAN_POINT('Ctrl Pts',(-1.45799092536346,0.542114518509698,
7.55292428458944));
#74054=CARTESIAN_POINT('Ctrl Pts',(-1.45341894213096,0.554249402754044,
7.55199072282582));
#74055=CARTESIAN_POINT('Ctrl Pts',(-1.45118857518932,0.560063161346824,
7.55154456514949));
#74056=CARTESIAN_POINT('Ctrl Pts',(-1.44494904456049,0.576039808064296,
7.55032112730695));
#74057=CARTESIAN_POINT('Ctrl Pts',(-1.44086753774523,0.586174341370557,
7.54954801244317));
#74058=CARTESIAN_POINT('Ctrl Pts',(-1.42341494134095,0.628225726624473,
7.54634905277599));
#74059=CARTESIAN_POINT('Ctrl Pts',(-1.40908644175102,0.659737437734344,
7.54397342040379));
#74060=CARTESIAN_POINT('Ctrl Pts',(-1.3554204296143,0.768019038473343,7.53579668765277));
#74061=CARTESIAN_POINT('Ctrl Pts',(-1.31076107466121,0.841977017426941,
7.53018074233204));
#74062=CARTESIAN_POINT('Ctrl Pts',(-1.22667573555633,0.958184204824523,
7.52072095353354));
#74063=CARTESIAN_POINT('Ctrl Pts',(-1.19062639134599,1.00262575160022,7.51692680723804));
#74064=CARTESIAN_POINT('Ctrl Pts',(-1.13483589245815,1.06414140246442,7.51129966710616));
#74065=CARTESIAN_POINT('Ctrl Pts',(-1.11698308300774,1.08286568922611,7.50953171157911));
#74066=CARTESIAN_POINT('Ctrl Pts',(-1.08388093255106,1.11589380133523,7.50630195794515));
#74067=CARTESIAN_POINT('Ctrl Pts',(-1.06879416232917,1.13035207720667,7.5048469855179));
#74068=CARTESIAN_POINT('Ctrl Pts',(-1.0527469753002,1.1451222188282,7.50331461323212));
#74069=CARTESIAN_POINT('Ctrl Pts',(-1.05207205393635,1.14574232852659,7.50325019150673));
#74070=CARTESIAN_POINT('Ctrl Pts',(-1.0507426484805,1.14696160529325,7.50312335282905));
#74071=CARTESIAN_POINT('Ctrl Pts',(-1.05008819891914,1.147560809647,7.50306093745084));
#74072=CARTESIAN_POINT('Ctrl Pts',(-1.04879010993488,1.14874728050099,7.5029371882959));
#74073=CARTESIAN_POINT('Ctrl Pts',(-1.04814648905173,1.14933456688584,7.50287585537263));
#74074=CARTESIAN_POINT('Ctrl Pts',(-1.04686031721185,1.15050618449608,7.50275334033047));
#74075=CARTESIAN_POINT('Ctrl Pts',(-1.04621776962111,1.15109051896027,7.50269215837656));
#74076=CARTESIAN_POINT('Ctrl Pts',(-1.04492330720554,1.15226572724585,7.50256895114121));
#74077=CARTESIAN_POINT('Ctrl Pts',(-1.04427137980577,1.15285658667487,7.50250692529661));
#74078=CARTESIAN_POINT('Ctrl Pts',(-1.04294626318161,1.15405552945545,7.50238090068928));
#74079=CARTESIAN_POINT('Ctrl Pts',(-1.04227304269551,1.15466357759097,7.50231690050442));
#74080=CARTESIAN_POINT('Ctrl Pts',(-1.04089090195365,1.15590972397057,7.50218555960168));
#74081=CARTESIAN_POINT('Ctrl Pts',(-1.04018192607556,1.15654775967016,7.50211821633582));
#74082=CARTESIAN_POINT('Ctrl Pts',(-1.03870961004172,1.15787030675017,7.50197842507667));
#74083=CARTESIAN_POINT('Ctrl Pts',(-1.03794617926215,1.15855471609794,7.50190597291));
#74084=CARTESIAN_POINT('Ctrl Pts',(-1.03695162458058,1.1594445540426,7.50181162884939));
#74085=CARTESIAN_POINT('Ctrl Pts',(-1.03672111383359,1.15965067056883,7.50178976543076));
#74086=CARTESIAN_POINT('Ctrl Pts',(-1.03604780494365,1.16025236411008,7.50172591227503));
#74087=CARTESIAN_POINT('Ctrl Pts',(-1.03560484215228,1.16064775597964,7.50168391488717));
#74088=CARTESIAN_POINT('Ctrl Pts',(-1.03417516935702,1.16192242245667,7.50154840244318));
#74089=CARTESIAN_POINT('Ctrl Pts',(-1.03318756730394,1.16280069120689,7.50145484585178));
#74090=CARTESIAN_POINT('Ctrl Pts',(-1.02358436382439,1.17131887077301,7.5005456430759));
#74091=CARTESIAN_POINT('Ctrl Pts',(-1.01488551300116,1.17886395709064,7.4997261085791));
#74092=CARTESIAN_POINT('Ctrl Pts',(-0.995879320688082,1.19498299741572,
7.49794364407895));
#74093=CARTESIAN_POINT('Ctrl Pts',(-0.985543365904937,1.2035215986791,7.4969793540628));
#74094=CARTESIAN_POINT('Ctrl Pts',(-0.956635118103986,1.22678078224174,
7.49429535946929));
#74095=CARTESIAN_POINT('Ctrl Pts',(-0.937835536834242,1.24121159681963,
7.49256437170897));
#74096=CARTESIAN_POINT('Ctrl Pts',(-0.832055279562801,1.31863459756003,
7.48289782519941));
#74097=CARTESIAN_POINT('Ctrl Pts',(-0.739075413016017,1.37290670687798,
7.47463897536454));
#74098=CARTESIAN_POINT('Ctrl Pts',(-0.585928165739531,1.44220595143434,
7.46160162324263));
#74099=CARTESIAN_POINT('Ctrl Pts',(-0.529166296610907,1.46398551124703,
7.45688664199853));
#74100=CARTESIAN_POINT('Ctrl Pts',(-0.440648151115006,1.49212672892797,
7.44982138133246));
#74101=CARTESIAN_POINT('Ctrl Pts',(-0.409725541702313,1.50091249003284,
7.44740538250197));
#74102=CARTESIAN_POINT('Ctrl Pts',(-0.368515263397383,1.51125239279505,
7.44427232374469));
#74103=CARTESIAN_POINT('Ctrl Pts',(-0.358454866863716,1.51367018140817,
7.44351422574362));
#74104=CARTESIAN_POINT('Ctrl Pts',(-0.341754102503843,1.51750798189817,
7.44226772885759));
#74105=CARTESIAN_POINT('Ctrl Pts',(-0.335127362489005,1.51898518725421,
7.44177623787765));
#74106=CARTESIAN_POINT('Ctrl Pts',(-0.321611481665128,1.52190533237724,
7.44078040068717));
#74107=CARTESIAN_POINT('Ctrl Pts',(-0.314721849679658,1.52334498668757,
7.44027623790376));
#74108=CARTESIAN_POINT('Ctrl Pts',(-0.296534226720535,1.52701680444864,
7.43895384844503));
#74109=CARTESIAN_POINT('Ctrl Pts',(-0.285220549470541,1.5291704050455,7.43813989759391));
#74110=CARTESIAN_POINT('Ctrl Pts',(-0.233668787928636,1.53839140560871,
7.43446592244168));
#74111=CARTESIAN_POINT('Ctrl Pts',(-0.19318214248939,1.54399823293092,7.4316766647968));
#74112=CARTESIAN_POINT('Ctrl Pts',(-0.00308236861972627,1.56272790202587,
7.41882979304328));
#74113=CARTESIAN_POINT('Ctrl Pts',(0.147694423946096,1.55573713980212,7.40927731497708));
#74114=CARTESIAN_POINT('Ctrl Pts',(0.322859675577482,1.52188668334205,7.39706756030304));
#74115=CARTESIAN_POINT('Ctrl Pts',(0.350428868147134,1.51577600115621,7.39511517166806));
#74116=CARTESIAN_POINT('Ctrl Pts',(0.391549839146004,1.50547980491476,7.39214815772038));
#74117=CARTESIAN_POINT('Ctrl Pts',(0.405236553384111,1.50185353207271,7.39115138201697));
#74118=CARTESIAN_POINT('Ctrl Pts',(0.42995996560274,1.49494054925149,7.38933301854265));
#74119=CARTESIAN_POINT('Ctrl Pts',(0.441013416173623,1.49171712181223,7.38851353898502));
#74120=CARTESIAN_POINT('Ctrl Pts',(0.464876340434263,1.48446976871056,7.38672970216871));
#74121=CARTESIAN_POINT('Ctrl Pts',(0.477671444152967,1.48040213338803,7.38576396839526));
#74122=CARTESIAN_POINT('Ctrl Pts',(0.512987474518724,1.46866946818924,7.38307183626967));
#74123=CARTESIAN_POINT('Ctrl Pts',(0.535386773774888,1.46065295067844,7.38133404293449));
#74124=CARTESIAN_POINT('Ctrl Pts',(0.654618990339468,1.41486976520334,7.3719145997941));
#74125=CARTESIAN_POINT('Ctrl Pts',(0.747650665361289,1.36798893527285,7.36393265727514));
#74126=CARTESIAN_POINT('Ctrl Pts',(0.888568105608705,1.27828577630645,7.35097903419832));
#74127=CARTESIAN_POINT('Ctrl Pts',(0.939726062804322,1.24116214157326,7.34607275663319));
#74128=CARTESIAN_POINT('Ctrl Pts',(1.0138575576604,1.18014945255675,7.33876504563673));
#74129=CARTESIAN_POINT('Ctrl Pts',(1.03856188656547,1.15846858422583,7.33629335898386));
#74130=CARTESIAN_POINT('Ctrl Pts',(1.07017553479034,1.12889912259303,7.33310070375485));
#74131=CARTESIAN_POINT('Ctrl Pts',(1.07771675836801,1.1217020588801,7.33233679698758));
#74132=CARTESIAN_POINT('Ctrl Pts',(1.09006063688264,1.10968210043244,7.33108335999714));
#74133=CARTESIAN_POINT('Ctrl Pts',(1.09490489789126,1.1049026323606,7.33059066993937));
#74134=CARTESIAN_POINT('Ctrl Pts',(1.10407368262416,1.09573696104061,7.32965690604934));
#74135=CARTESIAN_POINT('Ctrl Pts',(1.10840376139832,1.09135662811307,7.3292153707823));
#74136=CARTESIAN_POINT('Ctrl Pts',(1.12009540483364,1.07938793046968,7.32802127047399));
#74137=CARTESIAN_POINT('Ctrl Pts',(1.12740597889919,1.07174987543459,7.3272725356666));
#74138=CARTESIAN_POINT('Ctrl Pts',(1.15616266336523,1.04108513412876,7.32431599072203));
#74139=CARTESIAN_POINT('Ctrl Pts',(1.17698737872513,1.01748287608994,7.3221493751021));
#74140=CARTESIAN_POINT('Ctrl Pts',(1.25367275794186,0.925061456926306,7.31399604453422));
#74141=CARTESIAN_POINT('Ctrl Pts',(1.30433459807605,0.852143097645051,7.30822547274416));
#74142=CARTESIAN_POINT('Ctrl Pts',(1.38839166482852,0.705939281442061,7.29710678471561));
#74143=CARTESIAN_POINT('Ctrl Pts',(1.42285485436397,0.633611518020097,7.29178865702459));
#74144=CARTESIAN_POINT('Ctrl Pts',(1.46014873392443,0.536760461047925,7.28464599532562));
#74145=CARTESIAN_POINT('Ctrl Pts',(1.46818602598076,0.514369328746782,7.28299394496395));
#74146=CARTESIAN_POINT('Ctrl Pts',(1.47990768124947,0.479197325367883,7.28039274229701));
#74147=CARTESIAN_POINT('Ctrl Pts',(1.48394713744583,0.466537989150183,7.27945529198062));
#74148=CARTESIAN_POINT('Ctrl Pts',(1.49118613864123,0.442805783711019,7.27769479766798));
#74149=CARTESIAN_POINT('Ctrl Pts',(1.49442578275452,0.431746023556222,7.2768731337951));
#74150=CARTESIAN_POINT('Ctrl Pts',(1.50141967928809,0.406847375796675,7.27502004977091));
#74151=CARTESIAN_POINT('Ctrl Pts',(1.50510602078097,0.392990688358007,7.2739865011476));
#74152=CARTESIAN_POINT('Ctrl Pts',(1.51412489847635,0.35709935917171,7.27130270898195));
#74153=CARTESIAN_POINT('Ctrl Pts',(1.51916805067548,0.334996260132577,7.2696434204123));
#74154=CARTESIAN_POINT('Ctrl Pts',(1.55088553042386,0.180488565229036,7.25799410437029));
#74155=CARTESIAN_POINT('Ctrl Pts',(1.56069286359946,0.0452309269969691,
7.24746644241948));
#74156=CARTESIAN_POINT('Ctrl Pts',(1.54949367443541,-0.148966444705023,
7.23243634211637));
#74157=CARTESIAN_POINT('Ctrl Pts',(1.54266051169179,-0.2081388976497,7.22788043423073));
#74158=CARTESIAN_POINT('Ctrl Pts',(1.53034815963467,-0.278864143265942,
7.22256265183272));
#74159=CARTESIAN_POINT('Ctrl Pts',(1.52810153205659,-0.290923414276328,
7.22166053300618));
#74160=CARTESIAN_POINT('Ctrl Pts',(1.52431002742272,-0.310017798245634,
7.22024077293981));
#74161=CARTESIAN_POINT('Ctrl Pts',(1.52285860102057,-0.317070625994361,
7.2197182404839));
#74162=CARTESIAN_POINT('Ctrl Pts',(1.51998051577785,-0.33058009468454,7.21872128282758));
#74163=CARTESIAN_POINT('Ctrl Pts',(1.51856159294465,-0.337038065755799,
7.21824647115214));
#74164=CARTESIAN_POINT('Ctrl Pts',(1.51494480400623,-0.353012578679201,
7.21707595028892));
#74165=CARTESIAN_POINT('Ctrl Pts',(1.51269835405834,-0.362518058353448,
7.21638293980707));
#74166=CARTESIAN_POINT('Ctrl Pts',(1.50432533573781,-0.396513278659992,
7.21391492859844));
#74167=CARTESIAN_POINT('Ctrl Pts',(1.49769200728674,-0.420875670568505,
7.2121657691202));
#74168=CARTESIAN_POINT('Ctrl Pts',(1.46368883568163,-0.534747485918286,
7.20403518910618));
#74169=CARTESIAN_POINT('Ctrl Pts',(1.42886762299845,-0.621836579300651,
7.19794075627715));
#74170=CARTESIAN_POINT('Ctrl Pts',(1.35243316630773,-0.772091167205189,
7.18683277393607));
#74171=CARTESIAN_POINT('Ctrl Pts',(1.31366040007389,-0.836358131879249,
7.18186155662729));
#74172=CARTESIAN_POINT('Ctrl Pts',(1.25386868784669,-0.920985976299065,
7.17477363944725));
#74173=CARTESIAN_POINT('Ctrl Pts',(1.23668584598485,-0.943933152373516,
7.17279235826517));
#74174=CARTESIAN_POINT('Ctrl Pts',(1.21003361731337,-0.977548790318311,
7.16979033704218));
#74175=CARTESIAN_POINT('Ctrl Pts',(1.20103493366668,-0.988583864254332,
7.16878810191941));
#74176=CARTESIAN_POINT('Ctrl Pts',(1.18448526146271,-1.00831918694911,7.16696402008969));
#74177=CARTESIAN_POINT('Ctrl Pts',(1.17698662145754,-1.01706214029753,7.16614434707736));
#74178=CARTESIAN_POINT('Ctrl Pts',(1.16058004152239,-1.0357667618447,7.16436495312093));
#74179=CARTESIAN_POINT('Ctrl Pts',(1.15163949982251,-1.04569845531847,7.1634039093314));
#74180=CARTESIAN_POINT('Ctrl Pts',(1.12663008964768,-1.07277064563147,7.16073816277281));
#74181=CARTESIAN_POINT('Ctrl Pts',(1.11029974307498,-1.08966351953725,7.15902242557114));
#74182=CARTESIAN_POINT('Ctrl Pts',(0.999013892728845,-1.19968323346672,
7.14748590950593));
#74183=CARTESIAN_POINT('Ctrl Pts',(0.892847156125456,-1.28065558278529,
7.1371426245762));
#74184=CARTESIAN_POINT('Ctrl Pts',(0.740241368362435,-1.36875668780563,
7.12351078850172));
#74185=CARTESIAN_POINT('Ctrl Pts',(0.701883031035304,-1.38881706544295,
7.12018217004727));
#74186=CARTESIAN_POINT('Ctrl Pts',(0.639154167554966,-1.41835878297361,
7.11493934295683));
#74187=CARTESIAN_POINT('Ctrl Pts',(0.615295137240123,-1.42887080724425,
7.11298988619982));
#74188=CARTESIAN_POINT('Ctrl Pts',(0.582292250351068,-1.44243140010047,
7.11036409460971));
#74189=CARTESIAN_POINT('Ctrl Pts',(0.573369073462109,-1.4460015653746,7.10966110519878));
#74190=CARTESIAN_POINT('Ctrl Pts',(0.558216219081017,-1.45190189968399,
7.10847973633769));
#74191=CARTESIAN_POINT('Ctrl Pts',(0.552003746040857,-1.45427519580449,
7.10799889807658));
#74192=CARTESIAN_POINT('Ctrl Pts',(0.538956174446572,-1.45916398349868,
7.10699658542337));
#74193=CARTESIAN_POINT('Ctrl Pts',(0.532118362507497,-1.46167142093751,
7.10647557215104));
#74194=CARTESIAN_POINT('Ctrl Pts',(0.513356835232158,-1.46840219673453,
7.10505700212201));
#74195=CARTESIAN_POINT('Ctrl Pts',(0.501398500664107,-1.47252837741128,
7.10416489764243));
#74196=CARTESIAN_POINT('Ctrl Pts',(0.425421146095066,-1.49771117211207,
7.09856491302467));
#74197=CARTESIAN_POINT('Ctrl Pts',(0.360132489538943,-1.5147372350659,7.09405501815836));
#74198=CARTESIAN_POINT('Ctrl Pts',(0.24245472361139,-1.53738237621099,7.08612544050326));
#74199=CARTESIAN_POINT('Ctrl Pts',(0.190503744555038,-1.54468032065917,
7.08269158117875));
#74200=CARTESIAN_POINT('Ctrl Pts',(0.0827450436987772,-1.55429809045216,
7.07555281239651));
#74201=CARTESIAN_POINT('Ctrl Pts',(0.0269844168366512,-1.55626489956129,
7.07184947416365));
#74202=CARTESIAN_POINT('Ctrl Pts',(-0.0658550910428642,-1.5545481585412,
7.06555401922759));
#74203=CARTESIAN_POINT('Ctrl Pts',(-0.102912450346763,-1.55253519602004,
7.06300715402677));
#74204=CARTESIAN_POINT('Ctrl Pts',(-0.155462154540898,-1.54779106329478,
7.05932701600793));
#74205=CARTESIAN_POINT('Ctrl Pts',(-0.171041487461171,-1.5461469642815,
7.05822741662074));
#74206=CARTESIAN_POINT('Ctrl Pts',(-0.198185373520504,-1.54286718691133,
7.05629525478446));
#74207=CARTESIAN_POINT('Ctrl Pts',(-0.209761464858192,-1.54133601561334,
7.05546603863236));
#74208=CARTESIAN_POINT('Ctrl Pts',(-0.233757821912973,-1.53788668422474,
7.0537357638602));
#74209=CARTESIAN_POINT('Ctrl Pts',(-0.246174231068719,-1.53594804716261,
7.05283411376017));
#74210=CARTESIAN_POINT('Ctrl Pts',(-0.278586142805132,-1.53048431190558,
7.05046309366435));
#74211=CARTESIAN_POINT('Ctrl Pts',(-0.298537905712372,-1.52671788956101,
7.04898619758086));
#74212=CARTESIAN_POINT('Ctrl Pts',(-0.404007925354861,-1.50466122474207,
7.04108262632873));
#74213=CARTESIAN_POINT('Ctrl Pts',(-0.487929649173321,-1.47957685529943,
7.03444262145851));
#74214=CARTESIAN_POINT('Ctrl Pts',(-0.630064283695007,-1.42367987377651,
7.02264952354485));
#74215=CARTESIAN_POINT('Ctrl Pts',(-0.689275158980635,-1.39597460793067,
7.01756024766595));
#74216=CARTESIAN_POINT('Ctrl Pts',(-0.791470651501095,-1.34006493623007,
7.00858846773839));
#74217=CARTESIAN_POINT('Ctrl Pts',(-0.835137437374443,-1.31329601618832,
7.00468928163686));
#74218=CARTESIAN_POINT('Ctrl Pts',(-0.88720618553496,-1.27772697177467,
7.00002234678549));
#74219=CARTESIAN_POINT('Ctrl Pts',(-0.896927016511342,-1.27092209832548,
6.99915032755602));
#74220=CARTESIAN_POINT('Ctrl Pts',(-0.912350090150092,-1.25986037662173,
6.99776678085295));
#74221=CARTESIAN_POINT('Ctrl Pts',(-0.918102411110579,-1.25567464884299,
6.99725076179728));
#74222=CARTESIAN_POINT('Ctrl Pts',(-0.92918299377369,-1.24749491002729,
6.99625708247652));
#74223=CARTESIAN_POINT('Ctrl Pts',(-0.934514628689838,-1.24350592987063,
6.99577912705126));
#74224=CARTESIAN_POINT('Ctrl Pts',(-0.947806005168195,-1.2334279284993,
6.9945876136476));
#74225=CARTESIAN_POINT('Ctrl Pts',(-0.955733017712528,-1.2272958450116,
6.99387697928652));
#74226=CARTESIAN_POINT('Ctrl Pts',(-0.984920947884577,-1.20426268244441,
6.99125796376908));
#74227=CARTESIAN_POINT('Ctrl Pts',(-1.00579874122859,-1.18688120606247,
6.98937980686953));
#74228=CARTESIAN_POINT('Ctrl Pts',(-1.12266144652077,-1.08428927317036,
6.97876716189305));
#74229=CARTESIAN_POINT('Ctrl Pts',(-1.20826863693084,-0.988000651735009,
6.97055822786889));
#74230=CARTESIAN_POINT('Ctrl Pts',(-1.31332563932147,-0.835456935168933,
6.95819196247525));
#74231=CARTESIAN_POINT('Ctrl Pts',(-1.34297816820205,-0.786905994096305,
6.95434137180719));
#74232=CARTESIAN_POINT('Ctrl Pts',(-1.37846169548006,-0.720936815949845,
6.94914081286781));
#74233=CARTESIAN_POINT('Ctrl Pts',(-1.38674032973902,-0.704881372190737,
6.94787765719456));
#74234=CARTESIAN_POINT('Ctrl Pts',(-1.4000978672391,-0.677829486043225,
6.94575142942228));
#74235=CARTESIAN_POINT('Ctrl Pts',(-1.40533144353386,-0.666911065132555,
6.94489381962504));
#74236=CARTESIAN_POINT('Ctrl Pts',(-1.41541217431809,-0.645234710930449,
6.94319168423468));
#74237=CARTESIAN_POINT('Ctrl Pts',(-1.42026544215359,-0.634480508001762,
6.94234743964263));
#74238=CARTESIAN_POINT('Ctrl Pts',(-1.43184242481968,-0.608028878363311,
6.94027087483698));
#74239=CARTESIAN_POINT('Ctrl Pts',(-1.43843073710134,-0.592274275761857,
6.93903404908074));
#74240=CARTESIAN_POINT('Ctrl Pts',(-1.46099867244664,-0.535708764438644,
6.9345914556794));
#74241=CARTESIAN_POINT('Ctrl Pts',(-1.4755100302119,-0.494338408018343,
6.93133807683935));
#74242=CARTESIAN_POINT('Ctrl Pts',(-1.52407968646861,-0.334564444665204,
6.91875311365585));
#74243=CARTESIAN_POINT('Ctrl Pts',(-1.54577702329421,-0.212882604652054,
6.90908313443277));
#74244=CARTESIAN_POINT('Ctrl Pts',(-1.55464185047764,-0.0598247080940499,
6.89731533920326));
#74245=CARTESIAN_POINT('Ctrl Pts',(-1.5555097745333,-0.0296621909278112,
6.895017957575));
#74246=CARTESIAN_POINT('Ctrl Pts',(-1.55549991697361,0.000508227400676815,
6.8927523980872));
#74247=CARTESIAN_POINT('',(-1.55549951548814,-0.00134138022456237,6.75626748310733));
#74248=CARTESIAN_POINT('Ctrl Pts',(-1.5555,-1.2376520005909E-10,6.75616363716894));
#74249=CARTESIAN_POINT('Ctrl Pts',(-1.55549999999996,-0.00044681871954324,
6.75619828321149));
#74250=CARTESIAN_POINT('Ctrl Pts',(-1.55549980747644,-0.000893641999218809,
6.75623292926718));
#74251=CARTESIAN_POINT('Ctrl Pts',(-1.55549942241732,-0.00134046984005363,
6.75626757530168));
#74252=CARTESIAN_POINT('Ctrl Pts',(-1.55549942164341,-0.00134136759671164,
6.75626764491173));
#74253=CARTESIAN_POINT('Ctrl Pts',(-1.55543356401629,-0.0777123050950782,
6.76218927703849));
#74254=CARTESIAN_POINT('Ctrl Pts',(-1.54974336159869,-0.153984621809158,
6.7680982895917));
#74255=CARTESIAN_POINT('Ctrl Pts',(-1.53688625173814,-0.240158681815686,
6.7745849384911));
#74256=CARTESIAN_POINT('Ctrl Pts',(-1.53519179243515,-0.250762276864696,
6.77537969145555));
#74257=CARTESIAN_POINT('Ctrl Pts',(-1.53215729839804,-0.268566348617512,
6.77670745552424));
#74258=CARTESIAN_POINT('Ctrl Pts',(-1.53087599817814,-0.275776276012312,
6.77724329745044));
#74259=CARTESIAN_POINT('Ctrl Pts',(-1.52825896087146,-0.289921850295468,
6.77829061423902));
#74260=CARTESIAN_POINT('Ctrl Pts',(-1.5269268031055,-0.296858004127358,
6.77880226826464));
#74261=CARTESIAN_POINT('Ctrl Pts',(-1.52415613878415,-0.310771723097279,
6.77982451108939));
#74262=CARTESIAN_POINT('Ctrl Pts',(-1.52271685195391,-0.317748947320985,
6.78033504522336));
#74263=CARTESIAN_POINT('Ctrl Pts',(-1.51885552814052,-0.335838466091007,
6.78165385608453));
#74264=CARTESIAN_POINT('Ctrl Pts',(-1.5163594155357,-0.346934768629101,
6.78245808447844));
#74265=CARTESIAN_POINT('Ctrl Pts',(-1.50508179484595,-0.394619841508017,
6.78589766059699));
#74266=CARTESIAN_POINT('Ctrl Pts',(-1.49509526501567,-0.430913807499309,
6.78847365200962));
#74267=CARTESIAN_POINT('Ctrl Pts',(-1.45951757092909,-0.544000247662755,
6.7964705677088));
#74268=CARTESIAN_POINT('Ctrl Pts',(-1.42924669940302,-0.619179538743125,
6.8017482615632));
#74269=CARTESIAN_POINT('Ctrl Pts',(-1.36159568743238,-0.755452813043169,
6.81178144621418));
#74270=CARTESIAN_POINT('Ctrl Pts',(-1.32558953404252,-0.816983888008336,
6.81651132814119));
#74271=CARTESIAN_POINT('Ctrl Pts',(-1.26932550607837,-0.899565447977718,
6.82334437503284));
#74272=CARTESIAN_POINT('Ctrl Pts',(-1.25249977591337,-0.922848508511846,
6.82532898033634));
#74273=CARTESIAN_POINT('Ctrl Pts',(-1.2261548057372,-0.957255582282485,
6.82836029018886));
#74274=CARTESIAN_POINT('Ctrl Pts',(-1.21710673640751,-0.968733721844328,
6.82938876507205));
#74275=CARTESIAN_POINT('Ctrl Pts',(-1.20044944490694,-0.989262934131678,
6.83126087195295));
#74276=CARTESIAN_POINT('Ctrl Pts',(-1.19289611899561,-0.998358080950358,
6.83210221628006));
#74277=CARTESIAN_POINT('Ctrl Pts',(-1.17634940328792,-1.01782650612606,
6.83392974762176));
#74278=CARTESIAN_POINT('Ctrl Pts',(-1.1673209501098,-1.02816851352527,6.83491733375478));
#74279=CARTESIAN_POINT('Ctrl Pts',(-1.14199393971563,-1.05641673791046,
6.83766258150053));
#74280=CARTESIAN_POINT('Ctrl Pts',(-1.12541300963202,-1.07406327482656,
6.83943196416016));
#74281=CARTESIAN_POINT('Ctrl Pts',(-1.04339655873115,-1.15736583682646,
6.8480578212119));
#74282=CARTESIAN_POINT('Ctrl Pts',(-0.972602233893648,-1.21746116174307,
6.8551453260723));
#74283=CARTESIAN_POINT('Ctrl Pts',(-0.839226393857363,-1.3115872082482,
6.86778550364487));
#74284=CARTESIAN_POINT('Ctrl Pts',(-0.77885479261496,-1.34831294901422,
6.87328253931281));
#74285=CARTESIAN_POINT('Ctrl Pts',(-0.695055637373284,-1.39177766191555,
6.88048081562188));
#74286=CARTESIAN_POINT('Ctrl Pts',(-0.673664975489797,-1.40225640581979,
6.88228234997592));
#74287=CARTESIAN_POINT('Ctrl Pts',(-0.636390724955477,-1.41946618061489,
6.88535095840511));
#74288=CARTESIAN_POINT('Ctrl Pts',(-0.620620575505404,-1.42643175756307,
6.8866279873954));
#74289=CARTESIAN_POINT('Ctrl Pts',(-0.597061552951793,-1.43637291648053,
6.88850112849282));
#74290=CARTESIAN_POINT('Ctrl Pts',(-0.589359922507101,-1.43955011841694,
6.88910806097096));
#74291=CARTESIAN_POINT('Ctrl Pts',(-0.576057186044204,-1.44491332275271,
6.89014665520168));
#74292=CARTESIAN_POINT('Ctrl Pts',(-0.570468523127038,-1.44712890222484,
6.8905800197178));
#74293=CARTESIAN_POINT('Ctrl Pts',(-0.557260159994005,-1.45227683824166,
6.89159729179705));
#74294=CARTESIAN_POINT('Ctrl Pts',(-0.549630039791709,-1.45518168217065,
6.89217957679007));
#74295=CARTESIAN_POINT('Ctrl Pts',(-0.526636319331132,-1.46372890164956,
6.89391927304625));
#74296=CARTESIAN_POINT('Ctrl Pts',(-0.511205619437367,-1.4691892255961,
6.89506669164575));
#74297=CARTESIAN_POINT('Ctrl Pts',(-0.426789986836612,-1.49756951930608,
6.90125022252184));
#74298=CARTESIAN_POINT('Ctrl Pts',(-0.356341295080016,-1.5158785007227,
6.90607573519465));
#74299=CARTESIAN_POINT('Ctrl Pts',(-0.220773865907341,-1.54113239181254,
6.91517090346062));
#74300=CARTESIAN_POINT('Ctrl Pts',(-0.155999432313185,-1.54903004931677,
6.91943764929614));
#74301=CARTESIAN_POINT('Ctrl Pts',(-0.0498081194877144,-1.55524772942382,
6.92652033607769));
#74302=CARTESIAN_POINT('Ctrl Pts',(-0.00861801806893114,-1.55602111205891,
6.92928828604874));
#74303=CARTESIAN_POINT('Ctrl Pts',(0.0627753667807413,-1.55452672838982,
6.93416440977862));
#74304=CARTESIAN_POINT('Ctrl Pts',(0.092971924686231,-1.55301323629003,
6.93625109168742));
#74305=CARTESIAN_POINT('Ctrl Pts',(0.137806658450898,-1.54945381248803,
6.93939613683114));
#74306=CARTESIAN_POINT('Ctrl Pts',(0.152491895166693,-1.54807751342492,
6.94043374353235));
#74307=CARTESIAN_POINT('Ctrl Pts',(0.178917475238468,-1.54522126620056,
6.94231551098556));
#74308=CARTESIAN_POINT('Ctrl Pts',(0.190664851784905,-1.54381576770796,
6.94315727185257));
#74309=CARTESIAN_POINT('Ctrl Pts',(0.215906888420006,-1.54050322537017,
6.94497783601314));
#74310=CARTESIAN_POINT('Ctrl Pts',(0.229394715047186,-1.53855257129035,
6.94595795018703));
#74311=CARTESIAN_POINT('Ctrl Pts',(0.266306423276641,-1.53271812783106,
6.94866115711974));
#74312=CARTESIAN_POINT('Ctrl Pts',(0.289668850037129,-1.52847499578274,
6.95039539070234));
#74313=CARTESIAN_POINT('Ctrl Pts',(0.419765004339305,-1.50175699558045,
6.96018885265748));
#74314=CARTESIAN_POINT('Ctrl Pts',(0.523983561763028,-1.46864214777638,
6.96858192013735));
#74315=CARTESIAN_POINT('Ctrl Pts',(0.702172139143361,-1.39062658757346,
6.98366602552176));
#74316=CARTESIAN_POINT('Ctrl Pts',(0.777529630383351,-1.34994027656084,
6.99029873168174));
#74317=CARTESIAN_POINT('Ctrl Pts',(0.860275051868481,-1.29602578242185,
6.99762821764474));
#74318=CARTESIAN_POINT('Ctrl Pts',(0.871289707517869,-1.28864668175125,
6.99860469673896));
#74319=CARTESIAN_POINT('Ctrl Pts',(0.888410375825225,-1.27685705722736,
7.00012216088973));
#74320=CARTESIAN_POINT('Ctrl Pts',(0.894580687419041,-1.27254168519657,
7.00066898789664));
#74321=CARTESIAN_POINT('Ctrl Pts',(0.906272785674957,-1.26423743103727,
7.00170466674937));
#74322=CARTESIAN_POINT('Ctrl Pts',(0.911800015807825,-1.26025686954449,
7.00219400449772));
#74323=CARTESIAN_POINT('Ctrl Pts',(0.925205219204615,-1.25046844816577,
7.00338055380765));
#74324=CARTESIAN_POINT('Ctrl Pts',(0.93305502769512,-1.24462217800767,7.00407518895828));
#74325=CARTESIAN_POINT('Ctrl Pts',(0.960369339556774,-1.22387574033662,
7.00649367320614));
#74326=CARTESIAN_POINT('Ctrl Pts',(0.97953747618952,-1.20858909357693,7.00819344585391));
#74327=CARTESIAN_POINT('Ctrl Pts',(1.07988014188439,-1.12460916521844,7.01715466232082));
#74328=CARTESIAN_POINT('Ctrl Pts',(1.15421828521276,-1.04817546634035,7.02403595978699));
#74329=CARTESIAN_POINT('Ctrl Pts',(1.26880833156758,-0.903245640988257,
7.03624721938614));
#74330=CARTESIAN_POINT('Ctrl Pts',(1.31270984608384,-0.838163338072012,
7.04148887553691));
#74331=CARTESIAN_POINT('Ctrl Pts',(1.3613582222812,-0.752781042239624,7.04829226045155));
#74332=CARTESIAN_POINT('Ctrl Pts',(1.37086792099245,-0.73532073792715,7.04967945199191));
#74333=CARTESIAN_POINT('Ctrl Pts',(1.38589756528697,-0.706420106367791,
7.05197185804168));
#74334=CARTESIAN_POINT('Ctrl Pts',(1.39161684050416,-0.695085591967995,
7.052869994566));
#74335=CARTESIAN_POINT('Ctrl Pts',(1.40250517770954,-0.672833823761732,
7.05463213853963));
#74336=CARTESIAN_POINT('Ctrl Pts',(1.40768708989095,-0.661923839792053,
7.05549562128208));
#74337=CARTESIAN_POINT('Ctrl Pts',(1.41971770029561,-0.635814288664593,
7.05756153538044));
#74338=CARTESIAN_POINT('Ctrl Pts',(1.42644999281569,-0.62056307980319,7.05876785163742));
#74339=CARTESIAN_POINT('Ctrl Pts',(1.44838361835991,-0.568631318172157,
7.06287565062986));
#74340=CARTESIAN_POINT('Ctrl Pts',(1.46242415538043,-0.531480718226687,
7.06581505253145));
#74341=CARTESIAN_POINT('Ctrl Pts',(1.51549439644265,-0.372966658578356,
7.07836645208581));
#74342=CARTESIAN_POINT('Ctrl Pts',(1.54094746848227,-0.247588630682528,
7.08836976585726));
#74343=CARTESIAN_POINT('Ctrl Pts',(1.55319512380626,-0.0900143186193632,
7.10050483188289));
#74344=CARTESIAN_POINT('Ctrl Pts',(1.55466611331648,-0.0594237154998162,
7.10283750223579));
#74345=CARTESIAN_POINT('Ctrl Pts',(1.55561619014105,-0.0081324797782678,
7.1066911326726));
#74346=CARTESIAN_POINT('Ctrl Pts',(1.55558685962097,0.0125498159964593,
7.10822934883521));
#74347=CARTESIAN_POINT('Ctrl Pts',(1.55495409226146,0.0421659737962799,
7.11040404994012));
#74348=CARTESIAN_POINT('Ctrl Pts',(1.55468601670212,0.0511037982415989,
7.11105669770986));
#74349=CARTESIAN_POINT('Ctrl Pts',(1.55408231799457,0.0667328398451762,
7.11219098937646));
#74350=CARTESIAN_POINT('Ctrl Pts',(1.55378052270368,0.0734249052651159,
7.11267441179785));
#74351=CARTESIAN_POINT('Ctrl Pts',(1.553024122812,0.0880915109395472,7.1137288624341));
#74352=CARTESIAN_POINT('Ctrl Pts',(1.55255132377454,0.0960647431135248,
7.11429889604774));
#74353=CARTESIAN_POINT('Ctrl Pts',(1.5510131072941,0.119012370088535,7.11593120704107));
#74354=CARTESIAN_POINT('Ctrl Pts',(1.54979227503452,0.133975934444706,7.11698541794224));
#74355=CARTESIAN_POINT('Ctrl Pts',(1.5388645438123,0.247593882349314,7.12492870524367));
#74356=CARTESIAN_POINT('Ctrl Pts',(1.519962033883,0.345149037712844,7.13140663433357));
#74357=CARTESIAN_POINT('Ctrl Pts',(1.4732584614656,0.503415080672014,7.14226980336315));
#74358=CARTESIAN_POINT('Ctrl Pts',(1.45062785691922,0.565327516630805,7.14661400771911));
#74359=CARTESIAN_POINT('Ctrl Pts',(1.40748767260919,0.66353121763253,7.15385763524857));
#74360=CARTESIAN_POINT('Ctrl Pts',(1.38932568602314,0.700763066841547,7.15669109713421));
#74361=CARTESIAN_POINT('Ctrl Pts',(1.36186262717651,0.751787188862223,7.16072696874102));
#74362=CARTESIAN_POINT('Ctrl Pts',(1.35379246896179,0.76622431884272,7.16188660602014));
#74363=CARTESIAN_POINT('Ctrl Pts',(1.33944426324582,0.790958069585852,7.16390580102247));
#74364=CARTESIAN_POINT('Ctrl Pts',(1.33327373699532,0.801315624178988,7.16476144037103));
#74365=CARTESIAN_POINT('Ctrl Pts',(1.32033700789222,0.822467452868074,7.16653027144061));
#74366=CARTESIAN_POINT('Ctrl Pts',(1.31355736765755,0.833252392400646,7.16744390878648));
#74367=CARTESIAN_POINT('Ctrl Pts',(1.2957457897362,0.860829097585475,7.16981125117697));
#74368=CARTESIAN_POINT('Ctrl Pts',(1.28451992295688,0.877492099262659,7.17127208013978));
#74369=CARTESIAN_POINT('Ctrl Pts',(1.22971754596503,0.955531625049105,7.17826313614365));
#74370=CARTESIAN_POINT('Ctrl Pts',(1.18205284603531,1.01390030951067,7.18394693307072));
#74371=CARTESIAN_POINT('Ctrl Pts',(1.06805359454236,1.13448991728216,7.19670231534812));
#74372=CARTESIAN_POINT('Ctrl Pts',(1.00010594861484,1.19481946548832,7.20379889255666));
#74373=CARTESIAN_POINT('Ctrl Pts',(0.895409391353119,1.27255608074704,7.21377645560744));
#74374=CARTESIAN_POINT('Ctrl Pts',(0.86263077526118,1.29500027434961,7.216778947126));
#74375=CARTESIAN_POINT('Ctrl Pts',(0.819511901677323,1.32215994698611,7.2205441951291));
#74376=CARTESIAN_POINT('Ctrl Pts',(0.809932671763496,1.32804961100726,7.22136941638314));
#74377=CARTESIAN_POINT('Ctrl Pts',(0.794205104359225,1.33748602159825,7.22270501663736));
#74378=CARTESIAN_POINT('Ctrl Pts',(0.788095081274072,1.34109535607093,7.22321920871554));
#74379=CARTESIAN_POINT('Ctrl Pts',(0.776563957160568,1.34780103886767,7.22418055378909));
#74380=CARTESIAN_POINT('Ctrl Pts',(0.771148537154053,1.35090679072963,7.22462831860306));
#74381=CARTESIAN_POINT('Ctrl Pts',(0.75663395584758,1.35911520228295,7.22581894755174));
#74382=CARTESIAN_POINT('Ctrl Pts',(0.747501712930587,1.36415918468486,7.22655818298302));
#74383=CARTESIAN_POINT('Ctrl Pts',(0.712706656055614,1.38292307813006,7.22934023908978));
#74384=CARTESIAN_POINT('Ctrl Pts',(0.686709632173666,1.39601474443036,7.23134836728362));
#74385=CARTESIAN_POINT('Ctrl Pts',(0.578642122348085,1.4466855883651,7.23947406719521));
#74386=CARTESIAN_POINT('Ctrl Pts',(0.49373902682435,1.47781951040793,7.245352494799));
#74387=CARTESIAN_POINT('Ctrl Pts',(0.337504171883726,1.52013054002283,7.25602430027631));
#74388=CARTESIAN_POINT('Ctrl Pts',(0.267196509085141,1.53405034870421,7.26077642846143));
#74389=CARTESIAN_POINT('Ctrl Pts',(0.166923065750723,1.54679895917828,7.26768442563731));
#74390=CARTESIAN_POINT('Ctrl Pts',(0.137563338832664,1.54968592506361,7.26972184944561));
#74391=CARTESIAN_POINT('Ctrl Pts',(0.0935608589668794,1.55275246694,7.27280733000339));
#74392=CARTESIAN_POINT('Ctrl Pts',(0.0789677512149749,1.55356297792858,
7.27383580597469));
#74393=CARTESIAN_POINT('Ctrl Pts',(0.0525534007119759,1.55465692763251,
7.27570791373535));
#74394=CARTESIAN_POINT('Ctrl Pts',(0.040736096163147,1.55501144012544,7.27654925783732));
#74395=CARTESIAN_POINT('Ctrl Pts',(0.0151903218739158,1.55548640904937,
7.27837678741731));
#74396=CARTESIAN_POINT('Ctrl Pts',(0.00146209866686334,1.55555988456403,
7.27936437199902));
#74397=CARTESIAN_POINT('Ctrl Pts',(-0.0364762997474025,1.55526073630746,
7.28210961188887));
#74398=CARTESIAN_POINT('Ctrl Pts',(-0.0606786049949006,1.55450457166762,
7.2838789881436));
#74399=CARTESIAN_POINT('Ctrl Pts',(-0.177418451734728,1.5481269419551,7.29250574391708));
#74400=CARTESIAN_POINT('Ctrl Pts',(-0.269332155108154,1.53480593250714,
7.29959422272801));
#74401=CARTESIAN_POINT('Ctrl Pts',(-0.428160277455656,1.49707696217117,
7.31223466896849));
#74402=CARTESIAN_POINT('Ctrl Pts',(-0.495634021809718,1.47611253700752,
7.31773097710641));
#74403=CARTESIAN_POINT('Ctrl Pts',(-0.58366073968408,1.44204280920448,7.32492841959323));
#74404=CARTESIAN_POINT('Ctrl Pts',(-0.605669664631611,1.4329381380798,7.32672982886623));
#74405=CARTESIAN_POINT('Ctrl Pts',(-0.643234382759381,1.41637808930449,
7.32979824853974));
#74406=CARTESIAN_POINT('Ctrl Pts',(-0.658890961819159,1.40916291764155,
7.33107521234063));
#74407=CARTESIAN_POINT('Ctrl Pts',(-0.681932132904314,1.39807661327323,
7.33294827714352));
#74408=CARTESIAN_POINT('Ctrl Pts',(-0.689410162361361,1.39440427673655,
7.33355519730551));
#74409=CARTESIAN_POINT('Ctrl Pts',(-0.702233312337453,1.38797866221476,
7.33459377830803));
#74410=CARTESIAN_POINT('Ctrl Pts',(-0.707592375313756,1.38525428199628,
7.33502714177602));
#74411=CARTESIAN_POINT('Ctrl Pts',(-0.72019194584292,1.37875685464863,7.33604442262311));
#74412=CARTESIAN_POINT('Ctrl Pts',(-0.727418718012756,1.3749577883482,7.33662671730268));
#74413=CARTESIAN_POINT('Ctrl Pts',(-0.749042375059584,1.36337216302356,
7.33836647482544));
#74414=CARTESIAN_POINT('Ctrl Pts',(-0.763347145756502,1.35541481665359,
7.33951394395193));
#74415=CARTESIAN_POINT('Ctrl Pts',(-0.840568254335902,1.3108484308994,7.34570440947457));
#74416=CARTESIAN_POINT('Ctrl Pts',(-0.900988550450904,1.27007906411362,
7.35053620397165));
#74417=CARTESIAN_POINT('Ctrl Pts',(-1.01030080924381,1.18457788069213,7.35968917078256));
#74418=CARTESIAN_POINT('Ctrl Pts',(-1.0596250665221,1.14066951770463,7.36400669224855));
#74419=CARTESIAN_POINT('Ctrl Pts',(-1.13463024463664,1.06482435186035,7.37111202092495));
#74420=CARTESIAN_POINT('Ctrl Pts',(-1.16209981538722,1.03477550427565,7.37384865140367));
#74421=CARTESIAN_POINT('Ctrl Pts',(-1.2076989651629,0.980786371529975,7.37867564156021));
#74422=CARTESIAN_POINT('Ctrl Pts',(-1.2263726401147,0.957334134119339,7.3807451340714));
#74423=CARTESIAN_POINT('Ctrl Pts',(-1.25317844467766,0.921596553591422,
7.38386940465024));
#74424=CARTESIAN_POINT('Ctrl Pts',(-1.26183318270666,0.909710621336774,
7.3849038402507));
#74425=CARTESIAN_POINT('Ctrl Pts',(-1.27714396462003,0.888044730496262,
7.38678223841189));
#74426=CARTESIAN_POINT('Ctrl Pts',(-1.28385947491143,0.878308023578491,
7.38762384003068));
#74427=CARTESIAN_POINT('Ctrl Pts',(-1.29809116923485,0.857161721861683,
7.38944675226847));
#74428=CARTESIAN_POINT('Ctrl Pts',(-1.30556932211668,0.845727866470525,
7.3904294038507));
#74429=CARTESIAN_POINT('Ctrl Pts',(-1.32571399904795,0.814023306143538,
7.39314686269637));
#74430=CARTESIAN_POINT('Ctrl Pts',(-1.33806492298063,0.793557619058135,
7.39489300602276));
#74431=CARTESIAN_POINT('Ctrl Pts',(-1.40277091877301,0.680530614532037,
7.40449883010841));
#74432=CARTESIAN_POINT('Ctrl Pts',(-1.44599136298936,0.583086183931659,
7.41267348448418));
#74433=CARTESIAN_POINT('Ctrl Pts',(-1.49779897912627,0.424128923200931,
7.42563717202522));
#74434=CARTESIAN_POINT('Ctrl Pts',(-1.51325163175455,0.365181236580673,
7.43036297573141));
#74435=CARTESIAN_POINT('Ctrl Pts',(-1.53155567366816,0.27379138177627,7.43745361467981));
#74436=CARTESIAN_POINT('Ctrl Pts',(-1.53691347006018,0.241912887800901,
7.43988352680141));
#74437=CARTESIAN_POINT('Ctrl Pts',(-1.54269475423801,0.199459082121118,
7.44304355194652));
#74438=CARTESIAN_POINT('Ctrl Pts',(-1.54400911742531,0.189015586252565,
7.44381484385131));
#74439=CARTESIAN_POINT('Ctrl Pts',(-1.54601485806347,0.171658285064845,
7.44508582658828));
#74440=CARTESIAN_POINT('Ctrl Pts',(-1.54676608821382,0.164751885556382,
7.44558868083709));
#74441=CARTESIAN_POINT('Ctrl Pts',(-1.5481174348179,0.151503252164928,7.44654754652565));
#74442=CARTESIAN_POINT('Ctrl Pts',(-1.54872490023507,0.145162029150087,
7.44700398581681));
#74443=CARTESIAN_POINT('Ctrl Pts',(-1.5502856627862,0.127742855895553,7.44825138624544));
#74444=CARTESIAN_POINT('Ctrl Pts',(-1.55115919051009,0.116657867414643,
7.44903806432084));
#74445=CARTESIAN_POINT('Ctrl Pts',(-1.55428153014994,0.0707558561728834,
7.45226974807506));
#74446=CARTESIAN_POINT('Ctrl Pts',(-1.55547771071824,0.0358746791423457,
7.45466404925903));
#74447=CARTESIAN_POINT('Ctrl Pts',(-1.55549969139753,0.000979827635642597,
7.4570242544914));
#74448=CARTESIAN_POINT('Origin',(0.,0.,-1.2940562256037));
#74449=CARTESIAN_POINT('',(-1.5555,1.39005191776138E-11,8.29490354205207));
#74450=CARTESIAN_POINT('',(-1.55549980343579,0.000781991825156256,8.1559437743963));
#74451=CARTESIAN_POINT('',(-1.5555,-1.46451138874614E-13,-1.2940562256037));
#74452=CARTESIAN_POINT('Ctrl Pts',(-1.5555,1.39005191776138E-11,8.29490354205207));
#74453=CARTESIAN_POINT('Ctrl Pts',(-1.5555,0.0498749277555234,8.2915600034077));
#74454=CARTESIAN_POINT('Ctrl Pts',(-1.55310128629853,0.0997166037084997,
8.28816961820895));
#74455=CARTESIAN_POINT('Ctrl Pts',(-1.54660273194361,0.167085571741959,
8.28346863249098));
#74456=CARTESIAN_POINT('Ctrl Pts',(-1.54458784708901,0.184786189183087,
8.28222246654726));
#74457=CARTESIAN_POINT('Ctrl Pts',(-1.54085697631155,0.213208387603212,
8.28020173933394));
#74458=CARTESIAN_POINT('Ctrl Pts',(-1.53933191347003,0.223953761646126,
8.27943322035399));
#74459=CARTESIAN_POINT('Ctrl Pts',(-1.53591604314458,0.246335384476098,
8.27782247476751));
#74460=CARTESIAN_POINT('Ctrl Pts',(-1.53400515189999,0.257967813965996,
8.27697965943087));
#74461=CARTESIAN_POINT('Ctrl Pts',(-1.52912633822019,0.285693307821899,
8.27495673027745));
#74462=CARTESIAN_POINT('Ctrl Pts',(-1.52603636462686,0.301763152351375,
8.27377281459713));
#74463=CARTESIAN_POINT('Ctrl Pts',(-1.51412351221886,0.358845358588525,
8.2695249602609));
#74464=CARTESIAN_POINT('Ctrl Pts',(-1.50389663576708,0.399542613280656,
8.26641727889269));
#74465=CARTESIAN_POINT('Ctrl Pts',(-1.47290174394729,0.504700314325537,
8.25817453812039));
#74466=CARTESIAN_POINT('Ctrl Pts',(-1.44954916068012,0.568302267880589,
8.25297168138752));
#74467=CARTESIAN_POINT('Ctrl Pts',(-1.3828667240716,0.718786124973094,8.24022235538064));
#74468=CARTESIAN_POINT('Ctrl Pts',(-1.33540281202833,0.803539806723317,
8.23265443823666));
#74469=CARTESIAN_POINT('Ctrl Pts',(-1.27180170983869,0.895727374432254,
8.22431019134419));
#74470=CARTESIAN_POINT('Ctrl Pts',(-1.26306823834814,0.908000984756745,
8.22319711919407));
#74471=CARTESIAN_POINT('Ctrl Pts',(-1.24949693195612,0.926498644676224,
8.2215185964789));
#74472=CARTESIAN_POINT('Ctrl Pts',(-1.24478809374085,0.932815592964994,
8.22094520036954));
#74473=CARTESIAN_POINT('Ctrl Pts',(-1.23613761242704,0.944238131378665,
8.21990843680867));
#74474=CARTESIAN_POINT('Ctrl Pts',(-1.23221205696043,0.949355199777328,
8.2194440561872));
#74475=CARTESIAN_POINT('Ctrl Pts',(-1.22303971467008,0.961158850615359,
8.21837287510442));
#74476=CARTESIAN_POINT('Ctrl Pts',(-1.2177698098575,0.967827039743228,8.21776769870591));
#74477=CARTESIAN_POINT('Ctrl Pts',(-1.20063394868642,0.989148046121565,
8.2158313258862));
#74478=CARTESIAN_POINT('Ctrl Pts',(-1.1885556300063,1.0036290812869,8.21451404888314));
#74479=CARTESIAN_POINT('Ctrl Pts',(-1.15849097566115,1.03837017806146,8.21133832802212));
#74480=CARTESIAN_POINT('Ctrl Pts',(-1.1402325574487,1.0583873867404,8.20949519734665));
#74481=CARTESIAN_POINT('Ctrl Pts',(-1.05691879731478,1.14506648188989,8.2013992385625));
#74482=CARTESIAN_POINT('Ctrl Pts',(-0.986474622263151,1.20628536746132,
8.19535789655482));
#74483=CARTESIAN_POINT('Ctrl Pts',(-0.851487821977131,1.30381532714595,
8.18433530076217));
#74484=CARTESIAN_POINT('Ctrl Pts',(-0.789042927450533,1.34252565838235,
8.17941689745753));
#74485=CARTESIAN_POINT('Ctrl Pts',(-0.706636999630091,1.38586937611445,
8.17297063429914));
#74486=CARTESIAN_POINT('Ctrl Pts',(-0.688996885039989,1.39472327292096,
8.17159356935438));
#74487=CARTESIAN_POINT('Ctrl Pts',(-0.659962877099033,1.40861074868608,
8.16932882073245));
#74488=CARTESIAN_POINT('Ctrl Pts',(-0.648668207434421,1.41384750976527,
8.16844823629734));
#74489=CARTESIAN_POINT('Ctrl Pts',(-0.626615118402635,1.42375252559121,
8.16672904387845));
#74490=CARTESIAN_POINT('Ctrl Pts',(-0.615864340915131,1.4284358089969,8.16589102246685));
#74491=CARTESIAN_POINT('Ctrl Pts',(-0.590339595825652,1.43921325736795,
8.16390099510722));
#74492=CARTESIAN_POINT('Ctrl Pts',(-0.575522894612236,1.44520206230261,
8.16274551392185));
#74493=CARTESIAN_POINT('Ctrl Pts',(-0.524038484907674,1.46509441762896,
8.15872795045633));
#74494=CARTESIAN_POINT('Ctrl Pts',(-0.486941829054092,1.47783799484669,
8.15582823995077));
#74495=CARTESIAN_POINT('Ctrl Pts',(-0.391265532994785,1.50671156403513,
8.14833293882958));
#74496=CARTESIAN_POINT('Ctrl Pts',(-0.332152878147633,1.52083581366658,
8.14368474066949));
#74497=CARTESIAN_POINT('Ctrl Pts',(-0.178346242655299,1.54819031534426,
8.13161201535519));
#74498=CARTESIAN_POINT('Ctrl Pts',(-0.0829779185374421,1.55621875739644,
8.12413817701859));
#74499=CARTESIAN_POINT('Ctrl Pts',(0.0355490640440596,1.55526413634446,
8.11520254823744));
#74500=CARTESIAN_POINT('Ctrl Pts',(0.0585651203015629,1.5545676376251,8.1134847466427));
#74501=CARTESIAN_POINT('Ctrl Pts',(0.0909620166392629,1.55286664824077,
8.11109866084603));
#74502=CARTESIAN_POINT('Ctrl Pts',(0.10036095300839,1.55228753997022,8.11041020284145));
#74503=CARTESIAN_POINT('Ctrl Pts',(0.116356102426689,1.55115611995029,8.10924567863055));
#74504=CARTESIAN_POINT('Ctrl Pts',(0.122954992250006,1.5506470030533,8.1087673191013));
#74505=CARTESIAN_POINT('Ctrl Pts',(0.136890355597368,1.54948234139476,8.10776171099461));
#74506=CARTESIAN_POINT('Ctrl Pts',(0.144225690901881,1.54881679090983,8.10723500935038));
#74507=CARTESIAN_POINT('Ctrl Pts',(0.164528788754112,1.54682915281767,8.10578378013568));
#74508=CARTESIAN_POINT('Ctrl Pts',(0.177485442587997,1.54539609727671,8.10486513028809));
#74509=CARTESIAN_POINT('Ctrl Pts',(0.206837873151978,1.54177556350944,8.10279779712114));
#74510=CARTESIAN_POINT('Ctrl Pts',(0.223220058960657,1.5394890870877,8.10165378487478));
#74511=CARTESIAN_POINT('Ctrl Pts',(0.277340447103427,1.53105333171405,8.09789760878443));
#74512=CARTESIAN_POINT('Ctrl Pts',(0.314890272061174,1.52377378604029,8.09532885366987));
#74513=CARTESIAN_POINT('Ctrl Pts',(0.467281505637384,1.48835576883424,8.0849200897899));
#74514=CARTESIAN_POINT('Ctrl Pts',(0.57899682786174,1.44855709295447,8.07729663498998));
#74515=CARTESIAN_POINT('Ctrl Pts',(0.719035275405329,1.37985326482531,8.06673537361935));
#74516=CARTESIAN_POINT('Ctrl Pts',(0.752323845071721,1.36198943224894,8.06414621009425));
#74517=CARTESIAN_POINT('Ctrl Pts',(0.797511806891221,1.33557764264314,8.0604995170239));
#74518=CARTESIAN_POINT('Ctrl Pts',(0.80999187436025,1.3280458801925,8.05947793849715));
#74519=CARTESIAN_POINT('Ctrl Pts',(0.831512132198664,1.31464214923158,8.0576899179335));
#74520=CARTESIAN_POINT('Ctrl Pts',(0.840600692844574,1.30884944555208,8.0569264094461));
#74521=CARTESIAN_POINT('Ctrl Pts',(0.859560341062551,1.29648635344244,8.05531547736298));
#74522=CARTESIAN_POINT('Ctrl Pts',(0.86941792035381,1.2898966276277,8.05446736653036));
#74523=CARTESIAN_POINT('Ctrl Pts',(0.893015612861251,1.27372833965384,8.05241089044082));
#74524=CARTESIAN_POINT('Ctrl Pts',(0.906677949446313,1.26403948641139,8.05119839292632));
#74525=CARTESIAN_POINT('Ctrl Pts',(0.956356270985716,1.22758955700567,8.0467064670573));
#74526=CARTESIAN_POINT('Ctrl Pts',(0.99136280374378,1.19949676428923,8.04337629491164));
#74527=CARTESIAN_POINT('Ctrl Pts',(1.08219136073053,1.11991215086681,8.03427374522129));
#74528=CARTESIAN_POINT('Ctrl Pts',(1.13553604611237,1.06578472526734,8.02841306829191));
#74529=CARTESIAN_POINT('Ctrl Pts',(1.23897567812935,0.944209477582968,8.01603310733143));
#74530=CARTESIAN_POINT('Ctrl Pts',(1.28800540508865,0.876148918183707,8.0095275510102));
#74531=CARTESIAN_POINT('Ctrl Pts',(1.33956289015135,0.790825841415402,8.00209143674399));
#74532=CARTESIAN_POINT('Ctrl Pts',(1.34759558838533,0.777058833463272,8.00091267803622));
#74533=CARTESIAN_POINT('Ctrl Pts',(1.35932017644035,0.756235572301677,7.99916372534939));
#74534=CARTESIAN_POINT('Ctrl Pts',(1.36317152234137,0.749270973025572,7.99858436751788));
#74535=CARTESIAN_POINT('Ctrl Pts',(1.36976286526275,0.737132425314385,7.99758468632347));
#74536=CARTESIAN_POINT('Ctrl Pts',(1.37252727191749,0.731972274262188,7.99716287391728));
#74537=CARTESIAN_POINT('Ctrl Pts',(1.37903712627482,0.719654161344171,7.9961633734691));
#74538=CARTESIAN_POINT('Ctrl Pts',(1.38275603240297,0.71248247006364,7.99558733733913));
#74539=CARTESIAN_POINT('Ctrl Pts',(1.39392719605544,0.690522579749311,7.99384034974358));
#74540=CARTESIAN_POINT('Ctrl Pts',(1.40119961792467,0.675643507569316,7.99267978385194));
#74541=CARTESIAN_POINT('Ctrl Pts',(1.41787394338265,0.640100740187546,7.98995506285775));
#74542=CARTESIAN_POINT('Ctrl Pts',(1.42706405491241,0.619341403553678,7.98840107520557));
#74543=CARTESIAN_POINT('Ctrl Pts',(1.46084706203817,0.538280952363602,7.98244848901143));
#74544=CARTESIAN_POINT('Ctrl Pts',(1.4820999386259,0.476656585835822,7.97816433201871));
#74545=CARTESIAN_POINT('Ctrl Pts',(1.52633232424204,0.316408004911839,7.96722464804931));
#74546=CARTESIAN_POINT('Ctrl Pts',(1.54366561223733,0.216558928860968,7.9605797507473));
#74547=CARTESIAN_POINT('Ctrl Pts',(1.552963839516,0.0919408351150383,7.95198354681935));
#74548=CARTESIAN_POINT('Ctrl Pts',(1.55419155567525,0.0681051178718693,
7.95032693204113));
#74549=CARTESIAN_POINT('Ctrl Pts',(1.55525283472131,0.03081495091358,7.94771070236386));
#74550=CARTESIAN_POINT('Ctrl Pts',(1.55546104299214,0.0173742502842062,
7.94676276450098));
#74551=CARTESIAN_POINT('Ctrl Pts',(1.55552413638347,-0.00757966629252008,
7.94499277504774));
#74552=CARTESIAN_POINT('Ctrl Pts',(1.55542543243638,-0.0190919157169097,
7.94417223612611));
#74553=CARTESIAN_POINT('Ctrl Pts',(1.55492081024851,-0.0447371292593568,
7.94233499038163));
#74554=CARTESIAN_POINT('Ctrl Pts',(1.55444997171525,-0.0588676290986065,
7.94131631766446));
#74555=CARTESIAN_POINT('Ctrl Pts',(1.55246684320428,-0.101084193783883,
7.93825291456962));
#74556=CARTESIAN_POINT('Ctrl Pts',(1.55038541710038,-0.129136291236553,
7.93619073924407));
#74557=CARTESIAN_POINT('Ctrl Pts',(1.54126355870704,-0.218984433742546,
7.92949606285495));
#74558=CARTESIAN_POINT('Ctrl Pts',(1.53127847105869,-0.280414159182216,
7.9247790755692));
#74559=CARTESIAN_POINT('Ctrl Pts',(1.49548381989311,-0.439685805323688,
7.91222381179662));
#74560=CARTESIAN_POINT('Ctrl Pts',(1.46376458789457,-0.535899934222685,
7.90429558315751));
#74561=CARTESIAN_POINT('Ctrl Pts',(1.4108043371113,-0.655830265525908,7.89433768279793));
#74562=CARTESIAN_POINT('Ctrl Pts',(1.39787823387293,-0.682948718002875,
7.89208234416779));
#74563=CARTESIAN_POINT('Ctrl Pts',(1.3794301386574,-0.71893035383222,7.88910022975451));
#74564=CARTESIAN_POINT('Ctrl Pts',(1.37459351130218,-0.728135327792465,
7.88833827746536));
#74565=CARTESIAN_POINT('Ctrl Pts',(1.3667608855413,-0.742685980315719,7.88713614044877));
#74566=CARTESIAN_POINT('Ctrl Pts',(1.36382508792764,-0.748063444274921,
7.88669237590003));
#74567=CARTESIAN_POINT('Ctrl Pts',(1.35754348297583,-0.759409478536809,
7.885757366907));
#74568=CARTESIAN_POINT('Ctrl Pts',(1.35418991229818,-0.76537360132106,7.88526665298829));
#74569=CARTESIAN_POINT('Ctrl Pts',(1.34553932117405,-0.780523293425523,
7.88402165775359));
#74570=CARTESIAN_POINT('Ctrl Pts',(1.3401874125863,-0.78967739746249,7.88327078069417));
#74571=CARTESIAN_POINT('Ctrl Pts',(1.31697469208712,-0.828465468905031,
7.88009195651391));
#74572=CARTESIAN_POINT('Ctrl Pts',(1.29821999840131,-0.857556202567658,
7.87771488120675));
#74573=CARTESIAN_POINT('Ctrl Pts',(1.23902691429891,-0.94297258877348,7.87067951656161));
#74574=CARTESIAN_POINT('Ctrl Pts',(1.19577804507411,-0.997246812083528,
7.8661304917929));
#74575=CARTESIAN_POINT('Ctrl Pts',(1.0848135394717,-1.11885757327701,7.85529724406268));
#74576=CARTESIAN_POINT('Ctrl Pts',(1.01425097864081,-1.18319683326125,7.84901539437596));
#74577=CARTESIAN_POINT('Ctrl Pts',(0.920813384843231,-1.25385839582865,
7.84095804251916));
#74578=CARTESIAN_POINT('Ctrl Pts',(0.903101469183544,-1.26667510530303,
7.83944191017711));
#74579=CARTESIAN_POINT('Ctrl Pts',(0.873527168881357,-1.28714004302279,
7.83692430433954));
#74580=CARTESIAN_POINT('Ctrl Pts',(0.861819987823117,-1.29500791133799,
7.83593118248055));
#74581=CARTESIAN_POINT('Ctrl Pts',(0.840367057140992,-1.30900571900514,
7.83411660781216));
#74582=CARTESIAN_POINT('Ctrl Pts',(0.830657062793434,-1.31518880549084,
7.83329721921227));
#74583=CARTESIAN_POINT('Ctrl Pts',(0.809437982938206,-1.32837187644752,
7.83151023493493));
#74584=CARTESIAN_POINT('Ctrl Pts',(0.797904888752767,-1.33533121645665,
7.83054122557862));
#74585=CARTESIAN_POINT('Ctrl Pts',(0.764981532500986,-1.35461913547849,
7.82778050014743));
#74586=CARTESIAN_POINT('Ctrl Pts',(0.743386989515621,-1.36658896586155,
7.82597613123709));
#74587=CARTESIAN_POINT('Ctrl Pts',(0.693637908699188,-1.39263673653997,
7.82183122408097));
#74588=CARTESIAN_POINT('Ctrl Pts',(0.665323241184622,-1.40638379058277,
7.8194805009776));
#74589=CARTESIAN_POINT('Ctrl Pts',(0.562694603887872,-1.4524180780777,7.81099065826851));
#74590=CARTESIAN_POINT('Ctrl Pts',(0.486305826518423,-1.47974581428383,
7.80471902142107));
#74591=CARTESIAN_POINT('Ctrl Pts',(0.334756323017078,-1.52095450401104,
7.79253808429345));
#74592=CARTESIAN_POINT('Ctrl Pts',(0.259995514896561,-1.5355028342328,7.78664787318167));
#74593=CARTESIAN_POINT('Ctrl Pts',(0.168373359356863,-1.54644536481923,
7.7797619623278));
#74594=CARTESIAN_POINT('Ctrl Pts',(0.152252730518989,-1.54811563373617,
7.77856297050395));
#74595=CARTESIAN_POINT('Ctrl Pts',(0.128128495800055,-1.55023466104612,
7.77679023587213));
#74596=CARTESIAN_POINT('Ctrl Pts',(0.120143335079668,-1.55087394792957,
7.77620697476157));
#74597=CARTESIAN_POINT('Ctrl Pts',(0.106316619663395,-1.55187347162566,
7.77520351400373));
#74598=CARTESIAN_POINT('Ctrl Pts',(0.100477612117348,-1.55226246109607,
7.77478177982324));
#74599=CARTESIAN_POINT('Ctrl Pts',(0.0866269028915636,-1.55310669856902,
7.77378614512297));
#74600=CARTESIAN_POINT('Ctrl Pts',(0.0786136956273406,-1.5535329194684,
7.77321385176959));
#74601=CARTESIAN_POINT('Ctrl Pts',(0.0543370607723487,-1.55463586585914,
7.77149032804589));
#74602=CARTESIAN_POINT('Ctrl Pts',(0.038065367958459,-1.5551193761906,7.7703490808232));
#74603=CARTESIAN_POINT('Ctrl Pts',(-0.0457786464836099,-1.5562939142157,
7.76452645096702));
#74604=CARTESIAN_POINT('Ctrl Pts',(-0.113343840037139,-1.55283668762211,
7.76002633918739));
#74605=CARTESIAN_POINT('Ctrl Pts',(-0.305349137925343,-1.53040778528859,
7.74726187364575));
#74606=CARTESIAN_POINT('Ctrl Pts',(-0.427978530902885,-1.50073886531438,
7.7390992386982));
#74607=CARTESIAN_POINT('Ctrl Pts',(-0.56628711455893,-1.44892463721571,
7.72890877973017));
#74608=CARTESIAN_POINT('Ctrl Pts',(-0.586710368673162,-1.44077568006091,
7.72737877538248));
#74609=CARTESIAN_POINT('Ctrl Pts',(-0.618846831649249,-1.42715651326519,
7.72492695359932));
#74610=CARTESIAN_POINT('Ctrl Pts',(-0.630676883834851,-1.42196827127722,
7.7240146783709));
#74611=CARTESIAN_POINT('Ctrl Pts',(-0.652984961366595,-1.41185159949463,
7.72227511731249));
#74612=CARTESIAN_POINT('Ctrl Pts',(-0.663475301074231,-1.40695231272407,
7.72144888121579));
#74613=CARTESIAN_POINT('Ctrl Pts',(-0.687357178937619,-1.39547231376919,
7.71954848394858));
#74614=CARTESIAN_POINT('Ctrl Pts',(-0.700710485243082,-1.38881519898406,
7.71847172199472));
#74615=CARTESIAN_POINT('Ctrl Pts',(-0.742832736594558,-1.36705358617228,
7.71502858482346));
#74616=CARTESIAN_POINT('Ctrl Pts',(-0.771223415446381,-1.35124022105183,
7.71263768290214));
#74617=CARTESIAN_POINT('Ctrl Pts',(-0.83845721471574,-1.31098226403963,
7.70679971505475));
#74618=CARTESIAN_POINT('Ctrl Pts',(-0.876752723347024,-1.28568619076414,
7.70332582762222));
#74619=CARTESIAN_POINT('Ctrl Pts',(-0.962619271141025,-1.22334513110346,
7.6951980668136));
#74620=CARTESIAN_POINT('Ctrl Pts',(-1.00926785940533,-1.1851527083484,7.69052094884011));
#74621=CARTESIAN_POINT('Ctrl Pts',(-1.10941137037855,-1.09295271560774,
7.67996724707086));
#74622=CARTESIAN_POINT('Ctrl Pts',(-1.16141091746499,-1.03752903976306,
7.67410677608936));
#74623=CARTESIAN_POINT('Ctrl Pts',(-1.21718514621918,-0.968608940625206,
7.66753240490009));
#74624=CARTESIAN_POINT('Ctrl Pts',(-1.22508755641713,-0.958594527016345,
7.66659345801247));
#74625=CARTESIAN_POINT('Ctrl Pts',(-1.23732086897498,-0.942693316341622,
7.66512946835919));
#74626=CARTESIAN_POINT('Ctrl Pts',(-1.24173480340049,-0.936871552226248,
7.66459902809574));
#74627=CARTESIAN_POINT('Ctrl Pts',(-1.25008232743238,-0.92569893748762,
7.66359194458746));
#74628=CARTESIAN_POINT('Ctrl Pts',(-1.25402287633284,-0.920353723139987,
7.66311486309041));
#74629=CARTESIAN_POINT('Ctrl Pts',(-1.26354900829962,-0.90725709213594,
7.66195704033614));
#74630=CARTESIAN_POINT('Ctrl Pts',(-1.26909775391023,-0.899478977492918,
7.66127876693306));
#74631=CARTESIAN_POINT('Ctrl Pts',(-1.28927819960503,-0.870631912265411,
7.65879546149752));
#74632=CARTESIAN_POINT('Ctrl Pts',(-1.30346068143328,-0.849251816106625,
7.65701758977415));
#74633=CARTESIAN_POINT('Ctrl Pts',(-1.37438030582783,-0.736374993620883,
7.64789653122593));
#74634=CARTESIAN_POINT('Ctrl Pts',(-1.42203991842964,-0.639512804817598,
7.64093771155881));
#74635=CARTESIAN_POINT('Ctrl Pts',(-1.48577481225728,-0.466792198781864,
7.6287650073626));
#74636=CARTESIAN_POINT('Ctrl Pts',(-1.50691010203791,-0.393244794852944,
7.62365106254135));
#74637=CARTESIAN_POINT('Ctrl Pts',(-1.5266098384456,-0.299057042742007,
7.61698986841265));
#74638=CARTESIAN_POINT('Ctrl Pts',(-1.53029458021167,-0.279591039710081,
7.61560775544697));
#74639=CARTESIAN_POINT('Ctrl Pts',(-1.53569030779542,-0.247771845730677,
7.61333688700059));
#74640=CARTESIAN_POINT('Ctrl Pts',(-1.53762635013508,-0.235458701369292,
7.61245530771335));
#74641=CARTESIAN_POINT('Ctrl Pts',(-1.54099745297788,-0.212200222137321,
7.61078412101403));
#74642=CARTESIAN_POINT('Ctrl Pts',(-1.54246438919643,-0.20126023161635,
7.60999557898374));
#74643=CARTESIAN_POINT('Ctrl Pts',(-1.54521149816861,-0.17897490416236,
7.60838385098927));
#74644=CARTESIAN_POINT('Ctrl Pts',(-1.54648343381458,-0.167629252787794,
7.60756045572661));
#74645=CARTESIAN_POINT('Ctrl Pts',(-1.54980376176165,-0.134746354578356,
7.6051652839023));
#74646=CARTESIAN_POINT('Ctrl Pts',(-1.55152779921143,-0.113179862214762,
7.60358352539287));
#74647=CARTESIAN_POINT('Ctrl Pts',(-1.55460023182954,-0.0610877409083802,
7.59973508029491));
#74648=CARTESIAN_POINT('Ctrl Pts',(-1.5555,-0.0305461090157058,7.59745564652037));
#74649=CARTESIAN_POINT('Ctrl Pts',(-1.5555,7.12052432324671E-12,7.59515300361487));
#74650=CARTESIAN_POINT('Ctrl Pts',(-1.55549969139753,0.000979827635642597,
7.4570242544914));
#74651=CARTESIAN_POINT('Ctrl Pts',(-1.55554501108635,-0.0709662569765335,
7.4618905175078));
#74652=CARTESIAN_POINT('Ctrl Pts',(-1.55059873048183,-0.142833707437426,
7.46660555340356));
#74653=CARTESIAN_POINT('Ctrl Pts',(-1.52818695969918,-0.304108542309095,
7.47732492511803));
#74654=CARTESIAN_POINT('Ctrl Pts',(-1.50781860512254,-0.392833006397477,
7.48332821162779));
#74655=CARTESIAN_POINT('Ctrl Pts',(-1.47236311015355,-0.502308381022113,
7.49124120957554));
#74656=CARTESIAN_POINT('Ctrl Pts',(-1.46436403898692,-0.525171105088764,
7.49292195921004));
#74657=CARTESIAN_POINT('Ctrl Pts',(-1.45099930040647,-0.56068689033579,
7.49558283082459));
#74658=CARTESIAN_POINT('Ctrl Pts',(-1.445993958705,-0.573472064371543,7.49655102155029));
#74659=CARTESIAN_POINT('Ctrl Pts',(-1.4363648897729,-0.597139785805706,
7.49836353105899));
#74660=CARTESIAN_POINT('Ctrl Pts',(-1.43178502306543,-0.608039187825413,
7.49920631741373));
#74661=CARTESIAN_POINT('Ctrl Pts',(-1.42126728914897,-0.632291935734599,
7.50110039234493));
#74662=CARTESIAN_POINT('Ctrl Pts',(-1.41526465435722,-0.645615776032481,
7.50215383040761));
#74663=CARTESIAN_POINT('Ctrl Pts',(-1.39658609541388,-0.685563247233039,
7.50535245857226));
#74664=CARTESIAN_POINT('Ctrl Pts',(-1.38334068868298,-0.711911517572619,
7.50751694021133));
#74665=CARTESIAN_POINT('Ctrl Pts',(-1.33515636046828,-0.801333548544738,
7.51505883579101));
#74666=CARTESIAN_POINT('Ctrl Pts',(-1.29659079138147,-0.862338567550063,
7.52055459377995));
#74667=CARTESIAN_POINT('Ctrl Pts',(-1.20005873142889,-0.993846317926974,
7.53315044886879));
#74668=CARTESIAN_POINT('Ctrl Pts',(-1.1398357096647,-1.06237795471466,7.5402724543805));
#74669=CARTESIAN_POINT('Ctrl Pts',(-1.05362757989018,-1.14465685977957,
7.54930682696506));
#74670=CARTESIAN_POINT('Ctrl Pts',(-1.0327690628747,-1.16351137143775,7.55141433230204));
#74671=CARTESIAN_POINT('Ctrl Pts',(-1.00358394317558,-1.18848879269371,
7.55424582498861));
#74672=CARTESIAN_POINT('Ctrl Pts',(-0.995691850961683,-1.1951084028938,
7.5550002395648));
#74673=CARTESIAN_POINT('Ctrl Pts',(-0.982454434648219,-1.20598932254475,
7.55624622350705));
#74674=CARTESIAN_POINT('Ctrl Pts',(-0.977145831440899,-1.21029458959364,
7.55674080559601));
#74675=CARTESIAN_POINT('Ctrl Pts',(-0.966095798362048,-1.21913604330129,
7.5577595231638));
#74676=CARTESIAN_POINT('Ctrl Pts',(-0.960350459330092,-1.223666941958,7.5582832989696));
#74677=CARTESIAN_POINT('Ctrl Pts',(-0.944888800362732,-1.23568436505123,
7.5596778362951));
#74678=CARTESIAN_POINT('Ctrl Pts',(-0.935115302857628,-1.24309697541163,
7.56054364637968));
#74679=CARTESIAN_POINT('Ctrl Pts',(-0.880895093088227,-1.28321835019784,
7.56526773909854));
#74680=CARTESIAN_POINT('Ctrl Pts',(-0.834814606447781,-1.31366339708889,
7.56899450754268));
#74681=CARTESIAN_POINT('Ctrl Pts',(-0.689990184224478,-1.39864190332242,
7.58017441863464));
#74682=CARTESIAN_POINT('Ctrl Pts',(-0.586862610127516,-1.44494922200853,
7.5874523432492));
#74683=CARTESIAN_POINT('Ctrl Pts',(-0.439414548173491,-1.49274337639757,
7.59790486905357));
#74684=CARTESIAN_POINT('Ctrl Pts',(-0.398682163169277,-1.50413428729183,
7.60079358334716));
#74685=CARTESIAN_POINT('Ctrl Pts',(-0.34089003335134,-1.51778354496018,
7.60492486829894));
#74686=CARTESIAN_POINT('Ctrl Pts',(-0.324177809055433,-1.52144063693451,
7.60612322393444));
#74687=CARTESIAN_POINT('Ctrl Pts',(-0.295613822092171,-1.52719923545792,
7.60817946430359));
#74688=CARTESIAN_POINT('Ctrl Pts',(-0.283791525200369,-1.52944022180075,
7.60903284354371));
#74689=CARTESIAN_POINT('Ctrl Pts',(-0.259598669439202,-1.53373596533948,
7.61078452636559));
#74690=CARTESIAN_POINT('Ctrl Pts',(-0.247226913469297,-1.53577873301453,
7.61168314205691));
#74691=CARTESIAN_POINT('Ctrl Pts',(-0.2159373122994,-1.54055725905988,7.61396367870161));
#74692=CARTESIAN_POINT('Ctrl Pts',(-0.196991721959828,-1.54309422664626,
7.61535174050453));
#74693=CARTESIAN_POINT('Ctrl Pts',(-0.112409963510521,-1.55283741813895,
7.62158360048232));
#74694=CARTESIAN_POINT('Ctrl Pts',(-0.0464097455189875,-1.55620820396565,
7.62654389250547));
#74695=CARTESIAN_POINT('Ctrl Pts',(0.0813748462475464,-1.55459817525299,
7.63631871039768));
#74696=CARTESIAN_POINT('Ctrl Pts',(0.143048662305526,-1.55013990312827,
7.64111312513598));
#74697=CARTESIAN_POINT('Ctrl Pts',(0.280169309291714,-1.53197390890923,
7.65183574469314));
#74698=CARTESIAN_POINT('Ctrl Pts',(0.355211412975751,-1.51633319593973,
7.657748518799));
#74699=CARTESIAN_POINT('Ctrl Pts',(0.441277824915646,-1.49165094091487,
7.66438960607644));
#74700=CARTESIAN_POINT('Ctrl Pts',(0.453707139681548,-1.48791750750077,
7.66534501482946));
#74701=CARTESIAN_POINT('Ctrl Pts',(0.473215165700044,-1.48179062332647,
7.66683722000366));
#74702=CARTESIAN_POINT('Ctrl Pts',(0.480325512241547,-1.4795010824526,7.66737955682743));
#74703=CARTESIAN_POINT('Ctrl Pts',(0.493911285669533,-1.47501817846959,
7.66841247027955));
#74704=CARTESIAN_POINT('Ctrl Pts',(0.500389110822044,-1.47283323045834,
7.66890347074883));
#74705=CARTESIAN_POINT('Ctrl Pts',(0.516244358208881,-1.46736863081503,
7.67010198147855));
#74706=CARTESIAN_POINT('Ctrl Pts',(0.525605376226126,-1.4640416450091,7.67080678506493));
#74707=CARTESIAN_POINT('Ctrl Pts',(0.560656808433647,-1.45120453160755,
7.67343760442499));
#74708=CARTESIAN_POINT('Ctrl Pts',(0.586128065665676,-1.4411053984601,7.6753326425775));
#74709=CARTESIAN_POINT('Ctrl Pts',(0.653991175847012,-1.41210095672429,
7.68037062049658));
#74710=CARTESIAN_POINT('Ctrl Pts',(0.69582693857555,-1.39196230555116,7.68346495140166));
#74711=CARTESIAN_POINT('Ctrl Pts',(0.83987232392017,-1.31450246778687,7.69428600676893));
#74712=CARTESIAN_POINT('Ctrl Pts',(0.936437633789859,-1.24755163216969,
7.70187975334574));
#74713=CARTESIAN_POINT('Ctrl Pts',(1.04732900944869,-1.15047683658335,7.71194323452745));
#74714=CARTESIAN_POINT('Ctrl Pts',(1.06949881943101,-1.12989693132421,7.71403092695091));
#74715=CARTESIAN_POINT('Ctrl Pts',(1.10156804786942,-1.0983377022807,7.71717719237729));
#74716=CARTESIAN_POINT('Ctrl Pts',(1.11193451643538,-1.08784165989357,7.71821498430634));
#74717=CARTESIAN_POINT('Ctrl Pts',(1.13034309840462,-1.06866491873034,7.72009694799972));
#74718=CARTESIAN_POINT('Ctrl Pts',(1.138438509269,-1.06003678007625,7.72093871758969));
#74719=CARTESIAN_POINT('Ctrl Pts',(1.15564391480141,-1.0412747281855,7.72275914335087));
#74720=CARTESIAN_POINT('Ctrl Pts',(1.16472068357953,-1.03111183908427,7.72373910864727));
#74721=CARTESIAN_POINT('Ctrl Pts',(1.18967101869046,-1.00242612722106,7.72648919478016));
#74722=CARTESIAN_POINT('Ctrl Pts',(1.2052434843862,-0.983647951197445,7.72827138705222));
#74723=CARTESIAN_POINT('Ctrl Pts',(1.2717552846064,-0.899492656974708,7.73618506959834));
#74724=CARTESIAN_POINT('Ctrl Pts',(1.31785703449716,-0.830480272124849,
7.74249607873002));
#74725=CARTESIAN_POINT('Ctrl Pts',(1.40457896102814,-0.675113554800244,
7.75624344708667));
#74726=CARTESIAN_POINT('Ctrl Pts',(1.44321167516665,-0.588015219119412,
7.76368241281157));
#74727=CARTESIAN_POINT('Ctrl Pts',(1.48110347531414,-0.475872759306487,
7.77260868062961));
#74728=CARTESIAN_POINT('Ctrl Pts',(1.48806116739201,-0.453647988197631,
7.77434650998924));
#74729=CARTESIAN_POINT('Ctrl Pts',(1.49717988827809,-0.422048374407086,
7.77676598517714));
#74730=CARTESIAN_POINT('Ctrl Pts',(1.49975672308582,-0.412798052793245,
7.77746809908561));
#74731=CARTESIAN_POINT('Ctrl Pts',(1.50400706407234,-0.396974797911779,
7.77865796008569));
#74732=CARTESIAN_POINT('Ctrl Pts',(1.50572351196272,-0.390413821667677,
7.77914806065925));
#74733=CARTESIAN_POINT('Ctrl Pts',(1.50927534931498,-0.376465278684778,
7.78018288636546));
#74734=CARTESIAN_POINT('Ctrl Pts',(1.51109949944088,-0.369075189429433,
7.78072698763484));
#74735=CARTESIAN_POINT('Ctrl Pts',(1.51604196160468,-0.348400921531763,
7.78223832384033));
#74736=CARTESIAN_POINT('Ctrl Pts',(1.51903993116211,-0.335088275633844,
7.7831990776728));
#74737=CARTESIAN_POINT('Ctrl Pts',(1.52547222287481,-0.304662636573098,
7.7853702446455));
#74738=CARTESIAN_POINT('Ctrl Pts',(1.52879454363351,-0.287527608567049,
7.78657538991443));
#74739=CARTESIAN_POINT('Ctrl Pts',(1.53899471157172,-0.229730276543013,
7.79059253443933));
#74740=CARTESIAN_POINT('Ctrl Pts',(1.54454433243337,-0.188849161350949,
7.79335494055843));
#74741=CARTESIAN_POINT('Ctrl Pts',(1.5614980496291,-0.0112211677687543,
7.80519916367641));
#74742=CARTESIAN_POINT('Ctrl Pts',(1.55640850037308,0.126462917313448,7.81403696156534));
#74743=CARTESIAN_POINT('Ctrl Pts',(1.52947174446485,0.284292097957906,7.82507097351137));
#74744=CARTESIAN_POINT('Ctrl Pts',(1.52511593347312,0.306801417298446,7.82666477675015));
#74745=CARTESIAN_POINT('Ctrl Pts',(1.51744418312457,0.342229430904738,7.82920980178042));
#74746=CARTESIAN_POINT('Ctrl Pts',(1.51445670566381,0.355216411740045,7.83015056354671));
#74747=CARTESIAN_POINT('Ctrl Pts',(1.50849274972262,0.379698345419017,7.83193967413344));
#74748=CARTESIAN_POINT('Ctrl Pts',(1.50555077676461,0.391200784379005,7.83278685555756));
#74749=CARTESIAN_POINT('Ctrl Pts',(1.49853864898678,0.417365169759882,7.83472959446937));
#74750=CARTESIAN_POINT('Ctrl Pts',(1.49438450300826,0.43200311809666,7.83582780219911));
#74751=CARTESIAN_POINT('Ctrl Pts',(1.48057771738103,0.478069806601441,7.83932112474375));
#74752=CARTESIAN_POINT('Ctrl Pts',(1.4701436693649,0.509252794487029,7.84174117507829));
#74753=CARTESIAN_POINT('Ctrl Pts',(1.44262990658821,0.583566186402928,7.84764709289507));
#74754=CARTESIAN_POINT('Ctrl Pts',(1.42459442725173,0.626307085626742,7.85116011975138));
#74755=CARTESIAN_POINT('Ctrl Pts',(1.37915667721416,0.721829059536207,7.85926561878956));
#74756=CARTESIAN_POINT('Ctrl Pts',(1.35058263810123,0.773974353633779,7.86387816460538));
#74757=CARTESIAN_POINT('Ctrl Pts',(1.27929767481832,0.888041508362317,7.87430399548356));
#74758=CARTESIAN_POINT('Ctrl Pts',(1.23493296021063,0.948769399816142,7.88010111069342));
#74759=CARTESIAN_POINT('Ctrl Pts',(1.17799083416599,1.01591577035975,7.88663052903239));
#74760=CARTESIAN_POINT('Ctrl Pts',(1.1695095810532,1.02566789301412,7.88758189842874));
#74761=CARTESIAN_POINT('Ctrl Pts',(1.15594341391301,1.0408797708619,7.88906926048383));
#74762=CARTESIAN_POINT('Ctrl Pts',(1.1509393116236,1.04641033096636,7.88961073637658));
#74763=CARTESIAN_POINT('Ctrl Pts',(1.14126898326161,1.05694473028553,7.89064314301965));
#74764=CARTESIAN_POINT('Ctrl Pts',(1.13660926682391,1.06195406288122,7.89113448555217));
#74765=CARTESIAN_POINT('Ctrl Pts',(1.12508241489515,1.07418298424364,7.89233540804815));
#74766=CARTESIAN_POINT('Ctrl Pts',(1.11817851943387,1.08136780814526,7.89304225497267));
#74767=CARTESIAN_POINT('Ctrl Pts',(1.09187769716035,1.10821760281892,7.89569094586617));
#74768=CARTESIAN_POINT('Ctrl Pts',(1.0720259374624,1.12743238591035,7.89760126525488));
#74769=CARTESIAN_POINT('Ctrl Pts',(1.01703404800888,1.17789300289287,7.90269466053605));
#74770=CARTESIAN_POINT('Ctrl Pts',(0.980971021051693,1.20809216230312,7.90582780845656));
#74771=CARTESIAN_POINT('Ctrl Pts',(0.848558641444292,1.30912892404046,7.91684419688309));
#74772=CARTESIAN_POINT('Ctrl Pts',(0.745490409130914,1.37044237654542,7.92459447942765));
#74773=CARTESIAN_POINT('Ctrl Pts',(0.611048232535262,1.43072481308491,7.93467973317257));
#74774=CARTESIAN_POINT('Ctrl Pts',(0.585376855251253,1.44141847111609,7.93660247877976));
#74775=CARTESIAN_POINT('Ctrl Pts',(0.54593030357956,1.45662273534549,7.93956075544931));
#74776=CARTESIAN_POINT('Ctrl Pts',(0.532355076491546,1.46163871628751,7.94057946569314));
#74777=CARTESIAN_POINT('Ctrl Pts',(0.507573323398698,1.47040442411563,7.94244137534904));
#74778=CARTESIAN_POINT('Ctrl Pts',(0.496390171271181,1.47421729499361,7.94328240716746));
#74779=CARTESIAN_POINT('Ctrl Pts',(0.472012608895858,1.48221994759158,7.9451180646437));
#74780=CARTESIAN_POINT('Ctrl Pts',(0.45880363096384,1.48636169259715,7.94611418931359));
#74781=CARTESIAN_POINT('Ctrl Pts',(0.421135317884833,1.49762284769399,7.94895995574469));
#74782=CARTESIAN_POINT('Ctrl Pts',(0.396554983519485,1.50431816887764,7.9508230757082));
#74783=CARTESIAN_POINT('Ctrl Pts',(0.3401556857631,1.51820220207478,7.95511438391351));
#74784=CARTESIAN_POINT('Ctrl Pts',(0.308253577745842,1.52499943520829,7.95755357376472));
#74785=CARTESIAN_POINT('Ctrl Pts',(0.191369183724955,1.54608607556438,7.96653113128168));
#74786=CARTESIAN_POINT('Ctrl Pts',(0.105457668379776,1.55431023266949,7.97321800289549));
#74787=CARTESIAN_POINT('Ctrl Pts',(-0.048717988878883,1.55622500730806,
7.98516739973318));
#74788=CARTESIAN_POINT('Ctrl Pts',(-0.116741969594229,1.55260517797626,
7.9904180726374));
#74789=CARTESIAN_POINT('Ctrl Pts',(-0.200536081905883,1.54260570701948,
7.99671631707399));
#74790=CARTESIAN_POINT('Ctrl Pts',(-0.216725528395855,1.54041461587412,
7.99792504316677));
#74791=CARTESIAN_POINT('Ctrl Pts',(-0.240944147480382,1.53674744759384,
7.99971816136057));
#74792=CARTESIAN_POINT('Ctrl Pts',(-0.249000528164656,1.53546264847509,
8.00031213182518));
#74793=CARTESIAN_POINT('Ctrl Pts',(-0.262976057150327,1.53312099589648,
8.00133770159134));
#74794=CARTESIAN_POINT('Ctrl Pts',(-0.268899547174166,1.53209315360091,
8.00177085266144));
#74795=CARTESIAN_POINT('Ctrl Pts',(-0.283023317204938,1.52955796252907,
8.00280004750523));
#74796=CARTESIAN_POINT('Ctrl Pts',(-0.291217636334798,1.52801899711343,
8.00339431814377));
#74797=CARTESIAN_POINT('Ctrl Pts',(-0.316348447669188,1.52308969889965,
8.00520922405427));
#74798=CARTESIAN_POINT('Ctrl Pts',(-0.333241837158182,1.51948297580786,
8.00641855160604));
#74799=CARTESIAN_POINT('Ctrl Pts',(-0.373338800183416,1.51022137096864,
8.00927108719921));
#74800=CARTESIAN_POINT('Ctrl Pts',(-0.396479564465928,1.5043119800221,8.01090299455057));
#74801=CARTESIAN_POINT('Ctrl Pts',(-0.487791052547428,1.47874035890117,
8.01731842897144));
#74802=CARTESIAN_POINT('Ctrl Pts',(-0.554721623925365,1.45495651178569,
8.02197029547813));
#74803=CARTESIAN_POINT('Ctrl Pts',(-0.704307467571703,1.38997153960911,
8.03270629350585));
#74804=CARTESIAN_POINT('Ctrl Pts',(-0.785377643599008,1.34582655744088,
8.03878926897317));
#74805=CARTESIAN_POINT('Ctrl Pts',(-0.882248482703065,1.28132981264859,
8.04679157504217));
#74806=CARTESIAN_POINT('Ctrl Pts',(-0.902118400686632,1.26741893438338,
8.0484746068063));
#74807=CARTESIAN_POINT('Ctrl Pts',(-0.932720100726244,1.24491050642659,
8.05113828977852));
#74808=CARTESIAN_POINT('Ctrl Pts',(-0.943677459375091,1.23662516002074,
8.05210696701926));
#74809=CARTESIAN_POINT('Ctrl Pts',(-0.963857688656701,1.22094158856382,
8.05391991479804));
#74810=CARTESIAN_POINT('Ctrl Pts',(-0.973108787511704,1.21358117988817,
8.05476264656508));
#74811=CARTESIAN_POINT('Ctrl Pts',(-0.993598597906197,1.1968940436875,8.05665597880033));
#74812=CARTESIAN_POINT('Ctrl Pts',(-1.00479152439945,1.18751315405681,8.05770872099892));
#74813=CARTESIAN_POINT('Ctrl Pts',(-1.03814192957157,1.1587527963208,8.06090292818672));
#74814=CARTESIAN_POINT('Ctrl Pts',(-1.05988183802746,1.1389016557154,8.06306360563173));
#74815=CARTESIAN_POINT('Ctrl Pts',(-1.13420448602974,1.06706448002473,8.07073779300856));
#74816=CARTESIAN_POINT('Ctrl Pts',(-1.18362677185058,1.01196414470508,8.07637732824673));
#74817=CARTESIAN_POINT('Ctrl Pts',(-1.28656600970207,0.879297906224671,
8.08934893362486));
#74818=CARTESIAN_POINT('Ctrl Pts',(-1.33734344073776,0.799956705824113,
8.09670319035794));
#74819=CARTESIAN_POINT('Ctrl Pts',(-1.39195375757237,0.69472831084078,8.10565648818055));
#74820=CARTESIAN_POINT('Ctrl Pts',(-1.40274340943432,0.672676583908957,
8.10749067071032));
#74821=CARTESIAN_POINT('Ctrl Pts',(-1.41710169652014,0.641481818835518,
8.11001833198619));
#74822=CARTESIAN_POINT('Ctrl Pts',(-1.42111211731469,0.632547631045668,
8.11073471144544));
#74823=CARTESIAN_POINT('Ctrl Pts',(-1.42776895139142,0.617334980311334,
8.11194107131618));
#74824=CARTESIAN_POINT('Ctrl Pts',(-1.43045893029285,0.611076028826127,
8.11243357069672));
#74825=CARTESIAN_POINT('Ctrl Pts',(-1.43603484576512,0.597863565778048,
8.11346494516924));
#74826=CARTESIAN_POINT('Ctrl Pts',(-1.4389115467078,0.590906497383016,8.11400328503842));
#74827=CARTESIAN_POINT('Ctrl Pts',(-1.44671119705628,0.571648921121078,
8.11548115601483));
#74828=CARTESIAN_POINT('Ctrl Pts',(-1.4515278193047,0.559305638540478,8.11641466331292));
#74829=CARTESIAN_POINT('Ctrl Pts',(-1.4860272788179,0.46744702058334,8.12327136091529));
#74830=CARTESIAN_POINT('Ctrl Pts',(-1.5093196091122,0.385671174262824,8.1288811744231));
#74831=CARTESIAN_POINT('Ctrl Pts',(-1.54551745552437,0.203022818168026,
8.14114667021932));
#74832=CARTESIAN_POINT('Ctrl Pts',(-1.55545445899327,0.101980137035506,
8.14777563842846));
#74833=CARTESIAN_POINT('Ctrl Pts',(-1.55549984383366,0.000697017553365729,
8.15470102582708));
#74834=CARTESIAN_POINT('Origin',(0.,0.,-1.2940562256037));
#74835=CARTESIAN_POINT('',(-1.55549989237731,-0.000578631300119371,8.99405622560371));
#74836=CARTESIAN_POINT('',(-1.55549943430639,-0.00132660186739827,8.85594377445462));
#74837=CARTESIAN_POINT('',(-1.5555,-1.46451138874614E-13,-1.2940562256037));
#74838=CARTESIAN_POINT('Ctrl Pts',(-1.55549985441797,-0.000672982681023649,
8.99269866830482));
#74839=CARTESIAN_POINT('Ctrl Pts',(-1.55553267497311,0.0751868725337522,
8.98742630842159));
#74840=CARTESIAN_POINT('Ctrl Pts',(-1.55001602977296,0.150960035608289,
8.98240020028567));
#74841=CARTESIAN_POINT('Ctrl Pts',(-1.52948678893842,0.290733889955134,
8.97309402340842));
#74842=CARTESIAN_POINT('Ctrl Pts',(-1.51591498278765,0.354764016580911,
8.96881628542807));
#74843=CARTESIAN_POINT('Ctrl Pts',(-1.48224134326083,0.475542369316228,
8.96046486238954));
#74844=CARTESIAN_POINT('Ctrl Pts',(-1.46279985096064,0.532348806198154,
8.95641083970952));
#74845=CARTESIAN_POINT('Ctrl Pts',(-1.43322416462683,0.604799529158405,
8.95098178540607));
#74846=CARTESIAN_POINT('Ctrl Pts',(-1.42602273462414,0.621589162969467,
8.9497050981529));
#74847=CARTESIAN_POINT('Ctrl Pts',(-1.41356812740971,0.649269967237543,
8.94756694407566));
#74848=CARTESIAN_POINT('Ctrl Pts',(-1.40848053196524,0.660233986733171,
8.94671121123491));
#74849=CARTESIAN_POINT('Ctrl Pts',(-1.39823555126334,0.681654984428218,
8.94502125175909));
#74850=CARTESIAN_POINT('Ctrl Pts',(-1.39308733506298,0.692115480049023,
8.94418739059113));
#74851=CARTESIAN_POINT('Ctrl Pts',(-1.38029969988858,0.717377455103239,
8.94215206023508));
#74852=CARTESIAN_POINT('Ctrl Pts',(-1.37253933582564,0.732115705170182,
8.94094637805252));
#74853=CARTESIAN_POINT('Ctrl Pts',(-1.34470869299248,0.782972565801001,
8.93672029669511));
#74854=CARTESIAN_POINT('Ctrl Pts',(-1.32343883285864,0.818411006594746,
8.93365773422455));
#74855=CARTESIAN_POINT('Ctrl Pts',(-1.24275822895639,0.941451245971655,
8.92259086409341));
#74856=CARTESIAN_POINT('Ctrl Pts',(-1.17585751867034,1.02378331594169,8.91434171520101));
#74857=CARTESIAN_POINT('Ctrl Pts',(-1.05919316212951,1.14070838440239,8.9015520918593));
#74858=CARTESIAN_POINT('Ctrl Pts',(-1.01487802545282,1.18030920119306,8.89698874553265));
#74859=CARTESIAN_POINT('Ctrl Pts',(-0.95639946410656,1.22683152065423,8.8914187863839));
#74860=CARTESIAN_POINT('Ctrl Pts',(-0.944254980961323,1.23620309555228,
8.89028501230685));
#74861=CARTESIAN_POINT('Ctrl Pts',(-0.925727346168003,1.25006799361298,
8.88859198680759));
#74862=CARTESIAN_POINT('Ctrl Pts',(-0.919446176225109,1.25469512002804,
8.88802423971861));
#74863=CARTESIAN_POINT('Ctrl Pts',(-0.907874109613773,1.26308630147697,
8.88698997936066));
#74864=CARTESIAN_POINT('Ctrl Pts',(-0.902594295793504,1.26686461131741,
8.88652254437835));
#74865=CARTESIAN_POINT('Ctrl Pts',(-0.890428722670759,1.2754558040985,8.88545544435651));
#74866=CARTESIAN_POINT('Ctrl Pts',(-0.883527426278372,1.28024611460107,
8.88485728989135));
#74867=CARTESIAN_POINT('Ctrl Pts',(-0.861060874402768,1.29557233831768,
8.88293199360437));
#74868=CARTESIAN_POINT('Ctrl Pts',(-0.845342693180059,1.30588258512195,
8.8816187407413));
#74869=CARTESIAN_POINT('Ctrl Pts',(-0.74503382768297,1.36910917331893,8.87342193271221));
#74870=CARTESIAN_POINT('Ctrl Pts',(-0.655692897678767,1.41407470291416,
8.86692298541292));
#74871=CARTESIAN_POINT('Ctrl Pts',(-0.489882370095687,1.47840715372255,
8.85521038862082));
#74872=CARTESIAN_POINT('Ctrl Pts',(-0.415100300813759,1.50112038314158,
8.85004338496912));
#74873=CARTESIAN_POINT('Ctrl Pts',(-0.310582470666327,1.52445487743302,
8.84272074511322));
#74874=CARTESIAN_POINT('Ctrl Pts',(-0.282060524558848,1.52998883042445,
8.84071333703546));
#74875=CARTESIAN_POINT('Ctrl Pts',(-0.239259822237774,1.53705576889773,
8.83767808685636));
#74876=CARTESIAN_POINT('Ctrl Pts',(-0.225086632746572,1.53919514118514,
8.83666929812719));
#74877=CARTESIAN_POINT('Ctrl Pts',(-0.199439795840611,1.54270460359195,
8.83483618342761));
#74878=CARTESIAN_POINT('Ctrl Pts',(-0.187976474561442,1.54414330875063,
8.83401408410056));
#74879=CARTESIAN_POINT('Ctrl Pts',(-0.163225684585162,1.54696997074087,
8.83223260304774));
#74880=CARTESIAN_POINT('Ctrl Pts',(-0.149934321853342,1.54831469442623,
8.83127192987676));
#74881=CARTESIAN_POINT('Ctrl Pts',(-0.11334180292428,1.55154127656386,8.82861528577729));
#74882=CARTESIAN_POINT('Ctrl Pts',(-0.0900138553004687,1.5530692493693,
8.82690847524604));
#74883=CARTESIAN_POINT('Ctrl Pts',(0.065969882727109,1.55976013093717,8.81540175380699));
#74884=CARTESIAN_POINT('Ctrl Pts',(0.198762797828011,1.54844546091379,8.80508307599745));
#74885=CARTESIAN_POINT('Ctrl Pts',(0.370454402900628,1.51135322317808,8.79150310801523));
#74886=CARTESIAN_POINT('Ctrl Pts',(0.412045831304786,1.50054780924646,8.78820074445084));
#74887=CARTESIAN_POINT('Ctrl Pts',(0.47796263214271,1.48047469666119,8.78299275722727));
#74888=CARTESIAN_POINT('Ctrl Pts',(0.502595081993481,1.47229480319194,8.78105267547694));
#74889=CARTESIAN_POINT('Ctrl Pts',(0.536063150952893,1.46024281321834,8.77843530481333));
#74890=CARTESIAN_POINT('Ctrl Pts',(0.545083143749574,1.45689984363657,8.7777317848158));
#74891=CARTESIAN_POINT('Ctrl Pts',(0.560305072584805,1.45109716241409,8.77654842682252));
#74892=CARTESIAN_POINT('Ctrl Pts',(0.566523157756987,1.44868087170798,8.77606614571825));
#74893=CARTESIAN_POINT('Ctrl Pts',(0.579524720930552,1.44353206496688,8.77506030839839));
#74894=CARTESIAN_POINT('Ctrl Pts',(0.586304758495825,1.44079160907065,8.774537222014));
#74895=CARTESIAN_POINT('Ctrl Pts',(0.604859502310031,1.43313920931707,8.77310898405896));
#74896=CARTESIAN_POINT('Ctrl Pts',(0.616593817598843,1.42812993198109,8.77220938901327));
#74897=CARTESIAN_POINT('Ctrl Pts',(0.697395876080976,1.39245460333515,8.766031141383));
#74898=CARTESIAN_POINT('Ctrl Pts',(0.764220043649146,1.35693099489578,8.76100229023325));
#74899=CARTESIAN_POINT('Ctrl Pts',(0.878753883669385,1.28488837190784,8.75207177040058));
#74900=CARTESIAN_POINT('Ctrl Pts',(0.927430018801354,1.2502079825342,8.74816288035007));
#74901=CARTESIAN_POINT('Ctrl Pts',(1.01007089659661,1.18384048446953,8.74113251847141));
#74902=CARTESIAN_POINT('Ctrl Pts',(1.04483702187327,1.1532721347867,8.73803597924413));
#74903=CARTESIAN_POINT('Ctrl Pts',(1.10174747472538,1.09854501426182,8.73265882609977));
#74904=CARTESIAN_POINT('Ctrl Pts',(1.12458620015126,1.07515313764514,8.73040715993164));
#74905=CARTESIAN_POINT('Ctrl Pts',(1.15677691954164,1.04003420201023,8.72707898062912));
#74906=CARTESIAN_POINT('Ctrl Pts',(1.16672403526809,1.02886295535205,8.72602763622425));
#74907=CARTESIAN_POINT('Ctrl Pts',(1.18408807608228,1.00878636965667,8.72414985587718));
#74908=CARTESIAN_POINT('Ctrl Pts',(1.19156958903233,0.999938204463611,8.72332617607216));
#74909=CARTESIAN_POINT('Ctrl Pts',(1.20717497513209,0.981058328046565,8.72157625664145));
#74910=CARTESIAN_POINT('Ctrl Pts',(1.21527418164574,0.971007470822354,8.72064910173805));
#74911=CARTESIAN_POINT('Ctrl Pts',(1.23678784848405,0.943618874521721,8.7181336773604));
#74912=CARTESIAN_POINT('Ctrl Pts',(1.24996196887213,0.926097050989003,8.71653612252511));
#74913=CARTESIAN_POINT('Ctrl Pts',(1.33662335771646,0.805616828358604,8.70562339865553));
#74914=CARTESIAN_POINT('Ctrl Pts',(1.39767111156665,0.694322197021517,8.69583434962223));
#74915=CARTESIAN_POINT('Ctrl Pts',(1.46951057352821,0.51443447905573,8.68081960147854));
#74916=CARTESIAN_POINT('Ctrl Pts',(1.49038060916645,0.450412683994701,8.67563005265339));
#74917=CARTESIAN_POINT('Ctrl Pts',(1.51106488809414,0.369495699509406,8.66939674120381));
#74918=CARTESIAN_POINT('Ctrl Pts',(1.51484165620203,0.353693341625041,8.66819464299067));
#74919=CARTESIAN_POINT('Ctrl Pts',(1.52011156440548,0.330008116003868,8.66641833243938));
#74920=CARTESIAN_POINT('Ctrl Pts',(1.52179230889233,0.322168746267745,8.66583454144613));
#74921=CARTESIAN_POINT('Ctrl Pts',(1.52459416614423,0.308588854380744,8.66483080181685));
#74922=CARTESIAN_POINT('Ctrl Pts',(1.52574359572114,0.302854644681742,8.66440930901672));
#74923=CARTESIAN_POINT('Ctrl Pts',(1.52838998724825,0.289254900152996,8.66341517173262));
#74924=CARTESIAN_POINT('Ctrl Pts',(1.52985860026244,0.281384116670855,8.66284412299237));
#74925=CARTESIAN_POINT('Ctrl Pts',(1.53411614588725,0.257547238282533,8.66112670408433));
#74926=CARTESIAN_POINT('Ctrl Pts',(1.53671648695876,0.241547970381527,8.65999023362522));
#74927=CARTESIAN_POINT('Ctrl Pts',(1.54973084393972,0.152727320006722,8.65375604609985));
#74928=CARTESIAN_POINT('Ctrl Pts',(1.5552203220981,0.0792701796070533,8.64887582904145));
#74929=CARTESIAN_POINT('Ctrl Pts',(1.55573435553431,-0.0611930989910091,
8.63961565435611));
#74930=CARTESIAN_POINT('Ctrl Pts',(1.55166484794895,-0.128023041368751,
8.63523988570708));
#74931=CARTESIAN_POINT('Ctrl Pts',(1.53828463811049,-0.234255634372873,
8.62810537057456));
#74932=CARTESIAN_POINT('Ctrl Pts',(1.53171951914929,-0.273916567054004,
8.62540191313969));
#74933=CARTESIAN_POINT('Ctrl Pts',(1.51767192973829,-0.34223724329438,8.62063601085943));
#74934=CARTESIAN_POINT('Ctrl Pts',(1.51089316077976,-0.371020323370508,
8.61859407802205));
#74935=CARTESIAN_POINT('Ctrl Pts',(1.49960055046496,-0.413504152618828,
8.61551929210359));
#74936=CARTESIAN_POINT('Ctrl Pts',(1.49570951844169,-0.427364606525818,
8.61450638382327));
#74937=CARTESIAN_POINT('Ctrl Pts',(1.4883900846621,-0.452112202148676,8.61267925056458));
#74938=CARTESIAN_POINT('Ctrl Pts',(1.48503312977889,-0.463019522472326,
8.61186740886039));
#74939=CARTESIAN_POINT('Ctrl Pts',(1.47754035823443,-0.486444781873004,
8.61010917461645));
#74940=CARTESIAN_POINT('Ctrl Pts',(1.47336483575905,-0.49894897221002,8.60916152711336));
#74941=CARTESIAN_POINT('Ctrl Pts',(1.46156938442938,-0.532832319253829,
8.606567923491));
#74942=CARTESIAN_POINT('Ctrl Pts',(1.45363993941149,-0.554099423851205,
8.60491186749038));
#74943=CARTESIAN_POINT('Ctrl Pts',(1.39465243692118,-0.702315527663511,
8.59316467443468));
#74944=CARTESIAN_POINT('Ctrl Pts',(1.32751055839644,-0.822194049727416,
8.58251213240894));
#74945=CARTESIAN_POINT('Ctrl Pts',(1.22056757239217,-0.965162966130685,
8.56870703953378));
#74946=CARTESIAN_POINT('Ctrl Pts',(1.19421112717351,-0.99758958573062,8.56549660346181));
#74947=CARTESIAN_POINT('Ctrl Pts',(1.14973458576417,-1.04801677663082,8.5604155343826));
#74948=CARTESIAN_POINT('Ctrl Pts',(1.13242162142142,-1.06670063448791,8.55851192891728));
#74949=CARTESIAN_POINT('Ctrl Pts',(1.10801453418281,-1.09177594776829,8.55593731808865));
#74950=CARTESIAN_POINT('Ctrl Pts',(1.10130989414631,-1.09853878287706,8.55524088589171));
#74951=CARTESIAN_POINT('Ctrl Pts',(1.08983162989559,-1.10990596059625,8.55406743891075));
#74952=CARTESIAN_POINT('Ctrl Pts',(1.08508997949475,-1.11454204339672,8.55358803584301));
#74953=CARTESIAN_POINT('Ctrl Pts',(1.07505604592461,-1.12422784537089,8.55258493896932));
#74954=CARTESIAN_POINT('Ctrl Pts',(1.0697576000532,-1.12927075281901,8.55206174330038));
#74955=CARTESIAN_POINT('Ctrl Pts',(1.05509410505249,-1.14303121976397,8.55063084708253));
#74956=CARTESIAN_POINT('Ctrl Pts',(1.045656515759,-1.15167114181665,8.54972875609336));
#74957=CARTESIAN_POINT('Ctrl Pts',(0.978826636853056,-1.21135366576549,
8.54346211704602));
#74958=CARTESIAN_POINT('Ctrl Pts',(0.91782136549886,-1.25820766630131,8.538356029285));
#74959=CARTESIAN_POINT('Ctrl Pts',(0.802277215440299,-1.33405394213476,
8.52923804926565));
#74960=CARTESIAN_POINT('Ctrl Pts',(0.749010283104518,-1.36467289970733,
8.52522078665453));
#74961=CARTESIAN_POINT('Ctrl Pts',(0.654100549414535,-1.41199426569515,
8.51817912849731));
#74962=CARTESIAN_POINT('Ctrl Pts',(0.613289978071359,-1.43019239374418,
8.5151862915719));
#74963=CARTESIAN_POINT('Ctrl Pts',(0.542096656064354,-1.45833072463409,
8.50996864507241));
#74964=CARTESIAN_POINT('Ctrl Pts',(0.512086566813048,-1.46913729661563,
8.50777041405878));
#74965=CARTESIAN_POINT('Ctrl Pts',(0.467674750817236,-1.48360380421202,
8.50450640384338));
#74966=CARTESIAN_POINT('Ctrl Pts',(0.453517815577891,-1.48799243429573,
8.50346440581033));
#74967=CARTESIAN_POINT('Ctrl Pts',(0.428200213377002,-1.49544599676828,
8.50159704518089));
#74968=CARTESIAN_POINT('Ctrl Pts',(0.417063834316329,-1.49858996955978,
8.5007743279169));
#74969=CARTESIAN_POINT('Ctrl Pts',(0.393359802187278,-1.504997306523,8.49901981251343));
#74970=CARTESIAN_POINT('Ctrl Pts',(0.380784357193257,-1.50822812629815,
8.49808702927632));
#74971=CARTESIAN_POINT('Ctrl Pts',(0.346514748759987,-1.51657659634958,
8.49553895889787));
#74972=CARTESIAN_POINT('Ctrl Pts',(0.324749422790677,-1.52138580264801,
8.49391396605883));
#74973=CARTESIAN_POINT('Ctrl Pts',(0.181790665866913,-1.54976618777586,
8.48319169304855));
#74974=CARTESIAN_POINT('Ctrl Pts',(0.058282047598181,-1.5592993772551,8.47364714032615));
#74975=CARTESIAN_POINT('Ctrl Pts',(-0.133903731543495,-1.55125842747295,
8.45873638028983));
#74976=CARTESIAN_POINT('Ctrl Pts',(-0.20252225636218,-1.54380034531773,
8.45341325479084));
#74977=CARTESIAN_POINT('Ctrl Pts',(-0.28659488616317,-1.52895821602703,
8.44704025948605));
#74978=CARTESIAN_POINT('Ctrl Pts',(-0.302719159107059,-1.52584764072448,
8.44582507661434));
#74979=CARTESIAN_POINT('Ctrl Pts',(-0.326675858247995,-1.52083135631309,
8.44403311371989));
#74980=CARTESIAN_POINT('Ctrl Pts',(-0.334547031994612,-1.51911929149427,
8.44344653689665));
#74981=CARTESIAN_POINT('Ctrl Pts',(-0.348116805280319,-1.51605713235211,
8.44243948124428));
#74982=CARTESIAN_POINT('Ctrl Pts',(-0.353821454452966,-1.51473592428718,
8.44201743302356));
#74983=CARTESIAN_POINT('Ctrl Pts',(-0.367291044812638,-1.51153609113264,
8.4410239863096));
#74984=CARTESIAN_POINT('Ctrl Pts',(-0.375049148723181,-1.50962982545764,
8.44045416185437));
#74985=CARTESIAN_POINT('Ctrl Pts',(-0.39838587659003,-1.50370468280836,
8.43874630151658));
#74986=CARTESIAN_POINT('Ctrl Pts',(-0.413917746715257,-1.49950366181776,
8.43761798103461));
#74987=CARTESIAN_POINT('Ctrl Pts',(-0.50480489709013,-1.47340083812973,
8.43104935897011));
#74988=CARTESIAN_POINT('Ctrl Pts',(-0.578490200517025,-1.44606025295714,
8.42585845251485));
#74989=CARTESIAN_POINT('Ctrl Pts',(-0.721950174682886,-1.38009909621693,
8.41545721930481));
#74990=CARTESIAN_POINT('Ctrl Pts',(-0.791445947801712,-1.34145369893032,
8.41026058939153));
#74991=CARTESIAN_POINT('Ctrl Pts',(-0.896073288467977,-1.27230116046381,
8.40182306061934));
#74992=CARTESIAN_POINT('Ctrl Pts',(-0.933312709124304,-1.24524066720399,
8.39868453778051));
#74993=CARTESIAN_POINT('Ctrl Pts',(-0.982507086806654,-1.20604536398207,
8.394308201103));
#74994=CARTESIAN_POINT('Ctrl Pts',(-0.99554580391714,-1.19530502748934,
8.39312489348467));
#74995=CARTESIAN_POINT('Ctrl Pts',(-1.01745473833548,-1.17665089351467,
8.39109448953057));
#74996=CARTESIAN_POINT('Ctrl Pts',(-1.02641406734323,-1.16884370977891,
8.39025179109059));
#74997=CARTESIAN_POINT('Ctrl Pts',(-1.04330753791432,-1.15377867791037,
8.38863842982717));
#74998=CARTESIAN_POINT('Ctrl Pts',(-1.05125762724929,-1.14653968386288,
8.38786858979521));
#74999=CARTESIAN_POINT('Ctrl Pts',(-1.06972690309027,-1.12936879927586,
8.38605465524481));
#75000=CARTESIAN_POINT('Ctrl Pts',(-1.08018367993076,-1.11937157515258,
8.38500779707664));
#75001=CARTESIAN_POINT('Ctrl Pts',(-1.11668697388585,-1.08348469641496,
8.38128103196783));
#75002=CARTESIAN_POINT('Ctrl Pts',(-1.14195263354852,-1.05682195936664,
8.37856768622705));
#75003=CARTESIAN_POINT('Ctrl Pts',(-1.23882244495793,-0.947062689311923,
8.36760541269428));
#75004=CARTESIAN_POINT('Ctrl Pts',(-1.30248697525743,-0.857397302255552,
8.35907056362665));
#75005=CARTESIAN_POINT('Ctrl Pts',(-1.37807930922783,-0.722825095911406,
8.34712365320878));
#75006=CARTESIAN_POINT('Ctrl Pts',(-1.39828401373771,-0.682920949841104,
8.3436812071962));
#75007=CARTESIAN_POINT('Ctrl Pts',(-1.42773563792439,-0.617948349643967,
8.33828390243078));
#75008=CARTESIAN_POINT('Ctrl Pts',(-1.43810489739571,-0.593416997797286,
8.33629149515575));
#75009=CARTESIAN_POINT('Ctrl Pts',(-1.45138026564541,-0.559615374337244,
8.33361839725681));
#75010=CARTESIAN_POINT('Ctrl Pts',(-1.45483645805979,-0.550567830455759,
8.33290983986568));
#75011=CARTESIAN_POINT('Ctrl Pts',(-1.46052733847477,-0.535242498883359,
8.33172200045825));
#75012=CARTESIAN_POINT('Ctrl Pts',(-1.46280656492827,-0.528981663066348,
8.33124019557813));
#75013=CARTESIAN_POINT('Ctrl Pts',(-1.46748258722143,-0.51587566298971,
8.33023906264301));
#75014=CARTESIAN_POINT('Ctrl Pts',(-1.46987184416224,-0.509028104259469,
8.32972016380384));
#75015=CARTESIAN_POINT('Ctrl Pts',(-1.47625160774832,-0.490324306391796,
8.3283134912406));
#75016=CARTESIAN_POINT('Ctrl Pts',(-1.48014722981443,-0.478435930045978,
8.32743101996545));
#75017=CARTESIAN_POINT('Ctrl Pts',(-1.50204015428969,-0.408796491783894,
8.32232209697308));
#75018=CARTESIAN_POINT('Ctrl Pts',(-1.51680205742121,-0.350075051712818,
8.31825427213832));
#75019=CARTESIAN_POINT('Ctrl Pts',(-1.54626123119472,-0.195184634162695,
8.30778995457972));
#75020=CARTESIAN_POINT('Ctrl Pts',(-1.55543208973097,-0.0982440506574577,
8.30148832580142));
#75021=CARTESIAN_POINT('Ctrl Pts',(-1.55549987478443,-0.000720777658553386,
8.29495185940666));
#75022=CARTESIAN_POINT('Ctrl Pts',(-1.5555,-0.000360387957164358,8.29492770190879));
#75023=CARTESIAN_POINT('Ctrl Pts',(-1.5555,1.39005191776138E-11,8.29490354205207));
#75024=CARTESIAN_POINT('Ctrl Pts',(-1.55549980343579,0.000781991825156257,
8.1559437743963));
#75025=CARTESIAN_POINT('Ctrl Pts',(-1.55552936418458,-0.0580188005300481,
8.16013588671271));
#75026=CARTESIAN_POINT('Ctrl Pts',(-1.55222041418191,-0.116815327805788,
8.16432799902912));
#75027=CARTESIAN_POINT('Ctrl Pts',(-1.54560073260284,-0.17521023194314,
8.16852011134553));
#75028=CARTESIAN_POINT('Ctrl Pts',(-1.53897825413943,-0.233629808535023,
8.17271399487301));
#75029=CARTESIAN_POINT('Ctrl Pts',(-1.52904232516819,-0.291646928848665,
8.17690787840049));
#75030=CARTESIAN_POINT('Ctrl Pts',(-1.51587230703867,-0.34887160783484,
8.18110176192796));
#75031=CARTESIAN_POINT('Ctrl Pts',(-1.50268199083999,-0.406184483395979,
8.18530210920796));
#75032=CARTESIAN_POINT('Ctrl Pts',(-1.48624775480599,-0.462701993433649,
8.18950245648796));
#75033=CARTESIAN_POINT('Ctrl Pts',(-1.46669934333799,-0.518047571417836,
8.19370280376796));
#75034=CARTESIAN_POINT('Ctrl Pts',(-1.44713327893872,-0.573443128485241,
8.19790694411533));
#75035=CARTESIAN_POINT('Ctrl Pts',(-1.42444763581157,-0.62766418693826,
8.2021110844627));
#75036=CARTESIAN_POINT('Ctrl Pts',(-1.39881978898772,-0.680355383557988,
8.20631522481007));
#75037=CARTESIAN_POINT('Ctrl Pts',(-1.37314037354939,-0.733152605940389,
8.21052782477149));
#75038=CARTESIAN_POINT('Ctrl Pts',(-1.34450718489918,-0.784413388617838,
8.2147404247329));
#75039=CARTESIAN_POINT('Ctrl Pts',(-1.31314231809916,-0.833809032343236,
8.21895302469431));
#75040=CARTESIAN_POINT('Ctrl Pts',(-1.30490869044903,-0.846775940207582,
8.22005887920798));
#75041=CARTESIAN_POINT('Ctrl Pts',(-1.29648703674868,-0.859614489536206,
8.22116473372164));
#75042=CARTESIAN_POINT('Ctrl Pts',(-1.28788183119252,-0.872319115280753,
8.2222705882353));
#75043=CARTESIAN_POINT('Ctrl Pts',(-1.25560500531684,-0.919972246899313,
8.22641848143185));
#75044=CARTESIAN_POINT('Ctrl Pts',(-1.2206119932366,-0.965931613939869,
8.2305663746284));
#75045=CARTESIAN_POINT('Ctrl Pts',(-1.183106798534,-1.00987056262801,8.23471426782495));
#75046=CARTESIAN_POINT('Ctrl Pts',(-1.14566829117055,-1.05373138423014,
8.23885478572423));
#75047=CARTESIAN_POINT('Ctrl Pts',(-1.10572680259751,-1.09557852511303,
8.2429953036235));
#75048=CARTESIAN_POINT('Ctrl Pts',(-1.06352887083094,-1.13511523243636,
8.24713582152278));
#75049=CARTESIAN_POINT('Ctrl Pts',(-1.02137291525576,-1.17461261080864,
8.25127222066162));
#75050=CARTESIAN_POINT('Ctrl Pts',(-0.976965341807128,-1.21180375487596,
8.25540861980046));
#75051=CARTESIAN_POINT('Ctrl Pts',(-0.930590928396772,-1.24642720364474,
8.2595450189393));
#75052=CARTESIAN_POINT('Ctrl Pts',(-0.884244814608526,-1.28102952372542,
8.263678893873));
#75053=CARTESIAN_POINT('Ctrl Pts',(-0.835934656580026,-1.31306694359385,
8.26781276880671));
#75054=CARTESIAN_POINT('Ctrl Pts',(-0.785978149076146,-1.342318367294,8.27194664374041));
#75055=CARTESIAN_POINT('Ctrl Pts',(-0.736032919694587,-1.37156318722717,
8.27607958541538));
#75056=CARTESIAN_POINT('Ctrl Pts',(-0.68444252795948,-1.39802299659105,
8.28021252709034));
#75057=CARTESIAN_POINT('Ctrl Pts',(-0.631551582474378,-1.42152131488561,
8.28434546876531));
#75058=CARTESIAN_POINT('Ctrl Pts',(-0.578612804049106,-1.44504088433465,
8.28848214814528));
#75059=CARTESIAN_POINT('Ctrl Pts',(-0.524371598063827,-1.4655933973829,
8.29261882752526));
#75060=CARTESIAN_POINT('Ctrl Pts',(-0.469193755053609,-1.48305005654519,
8.29675550690523));
#75061=CARTESIAN_POINT('Ctrl Pts',(-0.413993103902056,-1.50051393153774,
8.30089389621011));
#75062=CARTESIAN_POINT('Ctrl Pts',(-0.357855549260668,-1.51487927085603,
8.30503228551499));
#75063=CARTESIAN_POINT('Ctrl Pts',(-0.301160160392097,-1.52606775989555,
8.30917067481987));
#75064=CARTESIAN_POINT('Ctrl Pts',(-0.244354187118708,-1.53727807209257,
8.31331713605666));
#75065=CARTESIAN_POINT('Ctrl Pts',(-0.186988722836364,-1.54529907762868,
8.31746359729344));
#75066=CARTESIAN_POINT('Ctrl Pts',(-0.12945018795521,-1.550104157416,8.32161005853022));
#75067=CARTESIAN_POINT('Ctrl Pts',(-0.0749972835052497,-1.55465155423577,
8.3255341566672));
#75068=CARTESIAN_POINT('Ctrl Pts',(-0.020389782718023,-1.55631914526793,
8.32945825480419));
#75069=CARTESIAN_POINT('Ctrl Pts',(0.0340469216032327,-1.55512734434494,
8.33338235294118));
#75070=CARTESIAN_POINT('Ctrl Pts',(0.0915914686065827,-1.5538675023856,
8.33753048153391));
#75071=CARTESIAN_POINT('Ctrl Pts',(0.149186781034701,-1.54940671355827,
8.34167861012665));
#75072=CARTESIAN_POINT('Ctrl Pts',(0.206447744916351,-1.54173914091164,
8.34582673871939));
#75073=CARTESIAN_POINT('Ctrl Pts',(0.263606876129832,-1.5340852042454,8.3499674902969));
#75074=CARTESIAN_POINT('Ctrl Pts',(0.320432327088291,-1.52323587181396,
8.35410824187442));
#75075=CARTESIAN_POINT('Ctrl Pts',(0.376541027563167,-1.50923725920137,
8.35824899345193));
#75076=CARTESIAN_POINT('Ctrl Pts',(0.432593901171643,-1.49525257488635,
8.36238562507686));
#75077=CARTESIAN_POINT('Ctrl Pts',(0.487930934516398,-1.47812494411918,
8.3665222567018));
#75078=CARTESIAN_POINT('Ctrl Pts',(0.542177958469255,-1.45795175206524,
8.37065888832673));
#75079=CARTESIAN_POINT('Ctrl Pts',(0.596391859938059,-1.43779087748392,
8.37479299418149));
#75080=CARTESIAN_POINT('Ctrl Pts',(0.649516584182981,-1.41458830896911,
8.37892710003626));
#75081=CARTESIAN_POINT('Ctrl Pts',(0.701194011910412,-1.3884909822037,8.38306120589102));
#75082=CARTESIAN_POINT('Ctrl Pts',(0.752859749414292,-1.36239955905224,
8.38719437654789));
#75083=CARTESIAN_POINT('Ctrl Pts',(0.803078375730401,-1.33341491231873,
8.39132754720475));
#75084=CARTESIAN_POINT('Ctrl Pts',(0.851514647952251,-1.30173079180096,
8.39546071786162));
#75085=CARTESIAN_POINT('Ctrl Pts',(0.899994665244785,-1.27001805586694,
8.39959762137889));
#75086=CARTESIAN_POINT('Ctrl Pts',(0.946688674031446,-1.23560125879504,
8.40373452489616));
#75087=CARTESIAN_POINT('Ctrl Pts',(0.991289994255716,-1.19871781386968,
8.40787142841343));
#75088=CARTESIAN_POINT('Ctrl Pts',(1.03590972524781,-1.1618191440017,8.41201003958351));
#75089=CARTESIAN_POINT('Ctrl Pts',(1.07843466168232,-1.12245215003644,8.4161486507536));
#75090=CARTESIAN_POINT('Ctrl Pts',(1.11859332491079,-1.08089278999585,8.42028726192368));
#75091=CARTESIAN_POINT('Ctrl Pts',(1.15883024806078,-1.0392524404005,8.42443393828716));
#75092=CARTESIAN_POINT('Ctrl Pts',(1.19669134031385,-0.995411581656071,
8.42858061465065));
#75093=CARTESIAN_POINT('Ctrl Pts',(1.23194455931703,-0.949680395064139,
8.43272729101412));
#75094=CARTESIAN_POINT('Ctrl Pts',(1.26529002123253,-0.906423989437334,
8.43664956655843));
#75095=CARTESIAN_POINT('Ctrl Pts',(1.29630238303193,-0.861476900372323,
8.44057184210275));
#75096=CARTESIAN_POINT('Ctrl Pts',(1.3248224615,-0.815123116777518,8.44449411764705));
#75097=CARTESIAN_POINT('Ctrl Pts',(1.35498571239949,-0.766098679264947,
8.44864237346172));
#75098=CARTESIAN_POINT('Ctrl Pts',(1.3824873648381,-0.715294892279789,8.45279062927639));
#75099=CARTESIAN_POINT('Ctrl Pts',(1.40711358534507,-0.663032131904138,
8.45693888509106));
#75100=CARTESIAN_POINT('Ctrl Pts',(1.43169603846838,-0.610862256438854,
8.4610797683451));
#75101=CARTESIAN_POINT('Ctrl Pts',(1.45341298298267,-0.557239021481411,
8.46522065159914));
#75102=CARTESIAN_POINT('Ctrl Pts',(1.472095338036,-0.502509269300256,8.46936153485318));
#75103=CARTESIAN_POINT('Ctrl Pts',(1.4907591169349,-0.447833935757737,8.47349830076299));
#75104=CARTESIAN_POINT('Ctrl Pts',(1.50639411724182,-0.392054755200792,
8.4776350666728));
#75105=CARTESIAN_POINT('Ctrl Pts',(1.51887915688401,-0.335538905021935,
8.48177183258261));
#75106=CARTESIAN_POINT('Ctrl Pts',(1.53135658068223,-0.279057529374942,
8.48590607507522));
#75107=CARTESIAN_POINT('Ctrl Pts',(1.54068774061331,-0.22184088232573,8.49004031756784));
#75108=CARTESIAN_POINT('Ctrl Pts',(1.54680178710342,-0.164269538909861,
8.49417456006045));
#75109=CARTESIAN_POINT('Ctrl Pts',(1.55291445365554,-0.106711189324582,
8.49830786945608));
#75110=CARTESIAN_POINT('Ctrl Pts',(1.55581139330419,-0.0487988198840324,
8.50244117885172));
#75111=CARTESIAN_POINT('Ctrl Pts',(1.5554734934391,0.00908081540229456,
8.50657448824735));
#75112=CARTESIAN_POINT('Ctrl Pts',(1.55513528823633,0.0670127526726037,
8.51071153264029));
#75113=CARTESIAN_POINT('Ctrl Pts',(1.55155640385267,0.124911374668306,8.51484857703323));
#75114=CARTESIAN_POINT('Ctrl Pts',(1.54476990279131,0.182390233922014,8.51898562142618));
#75115=CARTESIAN_POINT('Ctrl Pts',(1.53798059816,0.23989283825449,8.52312437487261));
#75116=CARTESIAN_POINT('Ctrl Pts',(1.52798112394513,0.296974819867029,8.52726312831903));
#75117=CARTESIAN_POINT('Ctrl Pts',(1.51485601926137,0.353258391135437,8.53140188176546));
#75118=CARTESIAN_POINT('Ctrl Pts',(1.50170533621045,0.409651648527132,8.53554870086605));
#75119=CARTESIAN_POINT('Ctrl Pts',(1.48541699586244,0.465242884291628,8.53969551996664));
#75120=CARTESIAN_POINT('Ctrl Pts',(1.46612568125884,0.519668872218949,8.54384233906723));
#75121=CARTESIAN_POINT('Ctrl Pts',(1.4478840516408,0.571133416433058,8.54776352016247));
#75122=CARTESIAN_POINT('Ctrl Pts',(1.42695793352342,0.621555884348664,8.5516847012577));
#75123=CARTESIAN_POINT('Ctrl Pts',(1.40349938543629,0.670648734495166,8.55560588235294));
#75124=CARTESIAN_POINT('Ctrl Pts',(1.37868903446763,0.72257056860283,8.55975302218543));
#75125=CARTESIAN_POINT('Ctrl Pts',(1.35094134090304,0.773223041853965,8.56390016201792));
#75126=CARTESIAN_POINT('Ctrl Pts',(1.32040923384716,0.822252823145754,8.56804730185041));
#75127=CARTESIAN_POINT('Ctrl Pts',(1.28993142693501,0.871195406912454,8.57218706615888));
#75128=CARTESIAN_POINT('Ctrl Pts',(1.25667930846831,0.918520588068721,8.57632683046735));
#75129=CARTESIAN_POINT('Ctrl Pts',(1.22085232808823,0.963898253448755,8.58046659477582));
#75130=CARTESIAN_POINT('Ctrl Pts',(1.18506098987666,1.00923077524205,8.58460224067477));
#75131=CARTESIAN_POINT('Ctrl Pts',(1.14670018613223,1.05261921299141,8.58873788657372));
#75132=CARTESIAN_POINT('Ctrl Pts',(1.10601244355904,1.09376264550064,8.59287353247267));
#75133=CARTESIAN_POINT('Ctrl Pts',(1.06534951917612,1.13488098186367,8.59700665576308));
#75134=CARTESIAN_POINT('Ctrl Pts',(1.02236283510628,1.17375665769604,8.6011397790535));
#75135=CARTESIAN_POINT('Ctrl Pts',(0.977333486651823,1.210123756427,8.60527290234391));
#75136=CARTESIAN_POINT('Ctrl Pts',(0.932314274856989,1.24648266847718,8.60940509521748));
#75137=CARTESIAN_POINT('Ctrl Pts',(0.885253716711833,1.28033379728367,8.61353728809105));
#75138=CARTESIAN_POINT('Ctrl Pts',(0.836466171950625,1.31145133084772,8.61766948096463));
#75139=CARTESIAN_POINT('Ctrl Pts',(0.787634374263119,1.34259708968784,8.62180542195932));
#75140=CARTESIAN_POINT('Ctrl Pts',(0.737072899290895,1.37100401637494,8.62594136295401));
#75141=CARTESIAN_POINT('Ctrl Pts',(0.685124159759577,1.39649029202273,8.6300773039487));
#75142=CARTESIAN_POINT('Ctrl Pts',(0.633153887095882,1.42198713191814,8.63421495932118));
#75143=CARTESIAN_POINT('Ctrl Pts',(0.579795683979693,1.44456070275556,8.63835261469365));
#75144=CARTESIAN_POINT('Ctrl Pts',(0.525412614205191,1.46407712735158,8.64249027006613));
#75145=CARTESIAN_POINT('Ctrl Pts',(0.470923225762024,1.48363170647417,8.64663601453715));
#75146=CARTESIAN_POINT('Ctrl Pts',(0.415405467720194,1.50011704573008,8.65078175900817));
#75147=CARTESIAN_POINT('Ctrl Pts',(0.359237374320549,1.51344929181366,8.65492750347918));
#75148=CARTESIAN_POINT('Ctrl Pts',(0.305991619112582,1.52608788195216,8.65885755133906));
#75149=CARTESIAN_POINT('Ctrl Pts',(0.252161912898589,1.53589331464948,8.66278759919894));
#75150=CARTESIAN_POINT('Ctrl Pts',(0.198074609147642,1.54283722382208,8.66671764705882));
#75151=CARTESIAN_POINT('Ctrl Pts',(0.14097417660744,1.55016796855841,8.67086663244245));
#75152=CARTESIAN_POINT('Ctrl Pts',(0.0833465647416978,1.55433986640978,
8.67501561782608));
#75153=CARTESIAN_POINT('Ctrl Pts',(0.0255718487286833,1.55528978989531,
8.67916460320971));
#75154=CARTESIAN_POINT('Ctrl Pts',(-0.0321000232977279,1.55623802243496,
8.68330620304086));
#75155=CARTESIAN_POINT('Ctrl Pts',(-0.0899179635182985,1.55397565623342,
8.68744780287201));
#75156=CARTESIAN_POINT('Ctrl Pts',(-0.147496184456423,1.54849124168359,
8.69158940270316));
#75157=CARTESIAN_POINT('Ctrl Pts',(-0.205017048519614,1.54301229046477,
8.6957268768559));
#75158=CARTESIAN_POINT('Ctrl Pts',(-0.262298150846453,1.53431769938897,
8.69986435100862));
#75159=CARTESIAN_POINT('Ctrl Pts',(-0.318954870054094,1.52244804209168,
8.70400182516135));
#75160=CARTESIAN_POINT('Ctrl Pts',(-0.375576905737759,1.51058565103834,
8.70813676647798));
#75161=CARTESIAN_POINT('Ctrl Pts',(-0.431574807545122,1.49555215326039,
8.7122717077946));
#75162=CARTESIAN_POINT('Ctrl Pts',(-0.486572442200073,1.47743951094163,
8.71640664911123));
#75163=CARTESIAN_POINT('Ctrl Pts',(-0.541557526175869,1.45933100199995,
8.72054064681779));
#75164=CARTESIAN_POINT('Ctrl Pts',(-0.595542301973042,1.43814490626192,
8.72467464452435));
#75165=CARTESIAN_POINT('Ctrl Pts',(-0.648166279563418,1.41402288667366,
8.72880864223091));
#75166=CARTESIAN_POINT('Ctrl Pts',(-0.700837524233219,1.38987920058531,
8.73294635311171));
#75167=CARTESIAN_POINT('Ctrl Pts',(-0.752145053219385,1.36279453703939,
8.7370840639925));
#75168=CARTESIAN_POINT('Ctrl Pts',(-0.801750111840515,1.33295799189762,
8.7412217748733));
#75169=CARTESIAN_POINT('Ctrl Pts',(-0.851375529867434,1.30310920094167,
8.7453611839949));
#75170=CARTESIAN_POINT('Ctrl Pts',(-0.899296652382154,1.27050656899263,
8.74950059311651));
#75171=CARTESIAN_POINT('Ctrl Pts',(-0.945203782165776,1.23538255620658,
8.75364000223811));
#75172=CARTESIAN_POINT('Ctrl Pts',(-0.991200065311743,1.20019033127455,
8.75778745024699));
#75173=CARTESIAN_POINT('Ctrl Pts',(-1.03517414217713,1.16246727941071,8.76193489825587));
#75174=CARTESIAN_POINT('Ctrl Pts',(-1.07685020588591,1.12248558301809,8.76608234626475));
#75175=CARTESIAN_POINT('Ctrl Pts',(-1.11619741000755,1.08473806492036,8.76999803476473));
#75176=CARTESIAN_POINT('Ctrl Pts',(-1.15349632838697,1.04497788410429,8.77391372326472));
#75177=CARTESIAN_POINT('Ctrl Pts',(-1.1885481979314,1.00346072728036,8.7778294117647));
#75178=CARTESIAN_POINT('Ctrl Pts',(-1.22543402886394,0.959771336462947,
8.78194997440151));
#75179=CARTESIAN_POINT('Ctrl Pts',(-1.2599909742097,0.913946641923029,8.78607053703832));
#75180=CARTESIAN_POINT('Ctrl Pts',(-1.29196078906812,0.866266454106636,
8.79019109967512));
#75181=CARTESIAN_POINT('Ctrl Pts',(-1.32388304105718,0.818657202157527,
8.79430553197357));
#75182=CARTESIAN_POINT('Ctrl Pts',(-1.35322549524949,0.769198359162392,
8.79841996427202));
#75183=CARTESIAN_POINT('Ctrl Pts',(-1.37976971947166,0.718203154566374,
8.80253439657047));
#75184=CARTESIAN_POINT('Ctrl Pts',(-1.40628498923961,0.667263575567268,
8.80664434084393));
#75185=CARTESIAN_POINT('Ctrl Pts',(-1.43000783591687,0.614791422342897,
8.81075428511738));
#75186=CARTESIAN_POINT('Ctrl Pts',(-1.45076405764136,0.561127346558663,
8.81486422939084));
#75187=CARTESIAN_POINT('Ctrl Pts',(-1.47150928084373,0.5074917068517,8.81897199584438));
#75188=CARTESIAN_POINT('Ctrl Pts',(-1.48929079903155,0.452665885671134,
8.82307976229793));
#75189=CARTESIAN_POINT('Ctrl Pts',(-1.50398207295083,0.397011554293467,
8.82718752875147));
#75190=CARTESIAN_POINT('Ctrl Pts',(-1.51866896460598,0.341373824061626,
8.83129406989823));
#75191=CARTESIAN_POINT('Ctrl Pts',(-1.53026731166723,0.28490858579035,8.83540061104499));
#75192=CARTESIAN_POINT('Ctrl Pts',(-1.53870081597823,0.227991335159742,
8.83950715219175));
#75193=CARTESIAN_POINT('Ctrl Pts',(-1.54713806779638,0.171048792812259,
8.84361551811878));
#75194=CARTESIAN_POINT('Ctrl Pts',(-1.55240759882802,0.113654360677632,
8.84772388404581));
#75195=CARTESIAN_POINT('Ctrl Pts',(-1.55448476488467,0.0561904417268394,
8.85183224997284));
#75196=CARTESIAN_POINT('Ctrl Pts',(-1.55517768587606,0.0370210760608892,
8.85320275811399));
#75197=CARTESIAN_POINT('Ctrl Pts',(-1.55551578386882,0.0178439958671598,
8.85457326625514));
#75198=CARTESIAN_POINT('Ctrl Pts',(-1.55549943430708,-0.00132660105165622,
8.8559437743963));
#75199=CARTESIAN_POINT('Origin',(0.,0.,0.));
#75200=CARTESIAN_POINT('',(-1.95399958641728,0.00127133045005693,0.22586969212423));
#75201=CARTESIAN_POINT('',(0.861527884061909,1.75382031718868,3.93409125912768E-5));
#75202=CARTESIAN_POINT('Ctrl Pts',(-1.95399958641728,0.00127133045005693,
0.22586969212423));
#75203=CARTESIAN_POINT('Ctrl Pts',(-1.95395605948788,0.0681710118368687,
0.222037453599974));
#75204=CARTESIAN_POINT('Ctrl Pts',(-1.95047708133558,0.134965857971554,
0.218205215075717));
#75205=CARTESIAN_POINT('Ctrl Pts',(-1.9435932731074,0.201398085223423,0.21437297655146));
#75206=CARTESIAN_POINT('Ctrl Pts',(-1.93654157865274,0.269450499380606,
0.210447275216578));
#75207=CARTESIAN_POINT('Ctrl Pts',(-1.9258976952577,0.337264795747382,0.206521573881697));
#75208=CARTESIAN_POINT('Ctrl Pts',(-1.91168774656432,0.404432886442037,
0.202595872546815));
#75209=CARTESIAN_POINT('Ctrl Pts',(-1.89749924293132,0.471499609862856,
0.198676095716234));
#75210=CARTESIAN_POINT('Ctrl Pts',(-1.87975545668369,0.53792158785195,0.194756318885654));
#75211=CARTESIAN_POINT('Ctrl Pts',(-1.8585342111985,0.603296432779744,0.190836542055074));
#75212=CARTESIAN_POINT('Ctrl Pts',(-1.83733826493252,0.668593340126828,
0.186921438243962));
#75213=CARTESIAN_POINT('Ctrl Pts',(-1.81267324464788,0.732845130317064,
0.18300633443285));
#75214=CARTESIAN_POINT('Ctrl Pts',(-1.78466748745849,0.795661962901718,
0.179091230621739));
#75215=CARTESIAN_POINT('Ctrl Pts',(-1.75667960406991,0.858438704602695,
0.175178625503493));
#75216=CARTESIAN_POINT('Ctrl Pts',(-1.72535541282999,0.919781859271184,
0.171266020385248));
#75217=CARTESIAN_POINT('Ctrl Pts',(-1.69087178125732,0.979320488577508,
0.167353415267004));
#75218=CARTESIAN_POINT('Ctrl Pts',(-1.65639845085757,1.03884133212034,0.163441978947404));
#75219=CARTESIAN_POINT('Ctrl Pts',(-1.61876779934057,1.09655829689135,0.159530542627805));
#75220=CARTESIAN_POINT('Ctrl Pts',(-1.57820231359506,1.15212562568637,0.155619106308205));
#75221=CARTESIAN_POINT('Ctrl Pts',(-1.53763517478325,1.2076952188812,0.151707510595382));
#75222=CARTESIAN_POINT('Ctrl Pts',(-1.49413325513439,1.261114608027,0.147795914882558));
#75223=CARTESIAN_POINT('Ctrl Pts',(-1.44796092155806,1.31206904149161,0.143884319169735));
#75224=CARTESIAN_POINT('Ctrl Pts',(-1.40174135600645,1.36307559877922,0.139968722091207));
#75225=CARTESIAN_POINT('Ctrl Pts',(-1.35284625410977,1.41161180422852,0.13605312501268));
#75226=CARTESIAN_POINT('Ctrl Pts',(-1.30157795883662,1.45739864727216,0.132137527934152));
#75227=CARTESIAN_POINT('Ctrl Pts',(-1.2502800764303,1.5032119140815,0.128219671149278));
#75228=CARTESIAN_POINT('Ctrl Pts',(-1.19660665633888,1.54627235318547,0.124301814364404));
#75229=CARTESIAN_POINT('Ctrl Pts',(-1.14089218940229,1.58634202244058,0.12038395757953));
#75230=CARTESIAN_POINT('Ctrl Pts',(-1.08508447629676,1.62647875404688,0.116459543698166));
#75231=CARTESIAN_POINT('Ctrl Pts',(-1.02722931016663,1.66361446039735,0.112535129816801));
#75232=CARTESIAN_POINT('Ctrl Pts',(-0.967688370463982,1.69755565966738,
0.108610715935436));
#75233=CARTESIAN_POINT('Ctrl Pts',(-0.940634266753058,1.71297779995792,
0.106827547905484));
#75234=CARTESIAN_POINT('Ctrl Pts',(-0.913232427096051,1.72774104823343,
0.105044379875532));
#75235=CARTESIAN_POINT('Ctrl Pts',(-0.885518136927234,1.74183053974057,
0.103261211845581));
#75236=CARTESIAN_POINT('Ctrl Pts',(-0.82518277812167,1.77250404861606,0.0993791682412745));
#75237=CARTESIAN_POINT('Ctrl Pts',(-0.763123230766267,1.80010409723702,
0.0954971246369682));
#75238=CARTESIAN_POINT('Ctrl Pts',(-0.699688390744016,1.82443200910805,
0.0916150810326619));
#75239=CARTESIAN_POINT('Ctrl Pts',(-0.636359874122095,1.84871914486438,
0.0877395441378561));
#75240=CARTESIAN_POINT('Ctrl Pts',(-0.57166110601235,1.8697448547059,0.0838640072430504));
#75241=CARTESIAN_POINT('Ctrl Pts',(-0.505964393620445,1.88735689057165,
0.0799884703482445));
#75242=CARTESIAN_POINT('Ctrl Pts',(-0.440329165750188,1.90495244360956,
0.0761165605075702));
#75243=CARTESIAN_POINT('Ctrl Pts',(-0.37369832685301,1.91914052530666,0.0722446506668958));
#75244=CARTESIAN_POINT('Ctrl Pts',(-0.306461522312016,1.9298179539382,0.0683727408262214));
#75245=CARTESIAN_POINT('Ctrl Pts',(-0.239263532761241,1.94048921861993,
0.0645030661920477));
#75246=CARTESIAN_POINT('Ctrl Pts',(-0.171460765852021,1.94765377033001,
0.060633391557874));
#75247=CARTESIAN_POINT('Ctrl Pts',(-0.103453395172505,1.95125943816482,
0.0567637169237003));
#75248=CARTESIAN_POINT('Ctrl Pts',(-0.0354608995727464,1.95486431734104,
0.0528948886936478));
#75249=CARTESIAN_POINT('Ctrl Pts',(0.0327356099712528,1.95491183184047,
0.0490260604635953));
#75250=CARTESIAN_POINT('Ctrl Pts',(0.10073244876722,1.95140179711031,0.0451572322335428));
#75251=CARTESIAN_POINT('Ctrl Pts',(0.168784262098388,1.947888924564,0.0412852761075839));
#75252=CARTESIAN_POINT('Ctrl Pts',(0.236635579734008,1.94081278028754,0.037413319981625));
#75253=CARTESIAN_POINT('Ctrl Pts',(0.303885490047154,1.93022527414258,0.0335413638556661));
#75254=CARTESIAN_POINT('Ctrl Pts',(0.371160973233011,1.91963374192613,0.0296679353553845));
#75255=CARTESIAN_POINT('Ctrl Pts',(0.43783410146098,1.90552829078888,0.0257945068551029));
#75256=CARTESIAN_POINT('Ctrl Pts',(0.503514718071474,1.88801189844911,0.0219210783548213));
#75257=CARTESIAN_POINT('Ctrl Pts',(0.569310398453004,1.87046481970197,0.0180408641190658));
#75258=CARTESIAN_POINT('Ctrl Pts',(0.634109614849086,1.84949501672137,0.0141606498833103));
#75259=CARTESIAN_POINT('Ctrl Pts',(0.697538648848681,1.82525500502323,0.0102804356475549));
#75260=CARTESIAN_POINT('Ctrl Pts',(0.753341645510678,1.8039293563954,0.00686673740256698));
#75261=CARTESIAN_POINT('Ctrl Pts',(0.808084213811854,1.78007341261458,0.00345303915757911));
#75262=CARTESIAN_POINT('Ctrl Pts',(0.861527884061909,1.75382031718868,3.93409125912768E-5));
#75263=CARTESIAN_POINT('',(-0.861525859670558,1.75382131162753,0.));
#75264=CARTESIAN_POINT('Origin',(0.,0.,0.));
#75265=CARTESIAN_POINT('',(-1.95399890574831,0.00206792998054292,0.124130307921897));
#75266=CARTESIAN_POINT('Ctrl Pts',(-0.861525859670557,1.75382131162753,
1.42247325030098E-15));
#75267=CARTESIAN_POINT('Ctrl Pts',(-0.924646993599216,1.72281445316895,
0.00400966066964642));
#75268=CARTESIAN_POINT('Ctrl Pts',(-0.986139593028611,1.68837280142252,
0.00801932133929142));
#75269=CARTESIAN_POINT('Ctrl Pts',(-1.04562298138973,1.65069336364743,0.0120289820089364));
#75270=CARTESIAN_POINT('Ctrl Pts',(-1.10692437825747,1.61186231799848,0.0161611911312997));
#75271=CARTESIAN_POINT('Ctrl Pts',(-1.16609128060864,1.56959254287446,0.020293400253663));
#75272=CARTESIAN_POINT('Ctrl Pts',(-1.22273578558825,1.5241499921733,0.0244256093760263));
#75273=CARTESIAN_POINT('Ctrl Pts',(-1.27766076881784,1.48008691251414,0.0284323796148805));
#75274=CARTESIAN_POINT('Ctrl Pts',(-1.33021395511449,1.43304126902846,0.0324391498537348));
#75275=CARTESIAN_POINT('Ctrl Pts',(-1.38007385230466,1.38329756819889,0.036445920092589));
#75276=CARTESIAN_POINT('Ctrl Pts',(-1.42993485554633,1.33355276389543,0.0404527792143826));
#75277=CARTESIAN_POINT('Ctrl Pts',(-1.47710212591552,1.28111010739876,0.0444596383361762));
#75278=CARTESIAN_POINT('Ctrl Pts',(-1.52129104438919,1.2262909761803,0.0484664974579699));
#75279=CARTESIAN_POINT('Ctrl Pts',(-1.56549289190009,1.1714558056784,0.0524745289286812));
#75280=CARTESIAN_POINT('Ctrl Pts',(-1.6067143674834,1.11424313578918,0.0564825603993924));
#75281=CARTESIAN_POINT('Ctrl Pts',(-1.64471203692479,1.05500631068952,0.0604905918701037));
#75282=CARTESIAN_POINT('Ctrl Pts',(-1.68273110286472,0.995736129316689,
0.064500880264484));
#75283=CARTESIAN_POINT('Ctrl Pts',(-1.71752250663885,0.934439913118181,
0.0685111686588643));
#75284=CARTESIAN_POINT('Ctrl Pts',(-1.74888764786171,0.871497558893162,
0.0725214570532445));
#75285=CARTESIAN_POINT('Ctrl Pts',(-1.78030155646624,0.808457340169785,
0.0765379807539908));
#75286=CARTESIAN_POINT('Ctrl Pts',(-1.80827836601966,0.743766286772777,
0.080554504454737));
#75287=CARTESIAN_POINT('Ctrl Pts',(-1.83266692769222,0.677825886303518,
0.0845710281554833));
#75288=CARTESIAN_POINT('Ctrl Pts',(-1.85707761604864,0.611825660969874,
0.0885911958739181));
#75289=CARTESIAN_POINT('Ctrl Pts',(-1.8778934365429,0.544574268729266,0.0926113635923529));
#75290=CARTESIAN_POINT('Ctrl Pts',(-1.89501335528528,0.476487547886031,
0.0966315313107877));
#75291=CARTESIAN_POINT('Ctrl Pts',(-1.91216481068738,0.408275404265988,
0.100659104593659));
#75292=CARTESIAN_POINT('Ctrl Pts',(-1.92560668578103,0.339225309972099,
0.104686677876531));
#75293=CARTESIAN_POINT('Ctrl Pts',(-1.93528926100571,0.269761888034572,
0.108714251159402));
#75294=CARTESIAN_POINT('Ctrl Pts',(-1.9372828373484,0.2554598422003,0.109543501088153));
#75295=CARTESIAN_POINT('Ctrl Pts',(-1.93911722566992,0.241140282985028,
0.110372751016905));
#75296=CARTESIAN_POINT('Ctrl Pts',(-1.94079226597546,0.226806923020075,
0.111202000945656));
#75297=CARTESIAN_POINT('Ctrl Pts',(-1.94949709445539,0.152319497479718,
0.115511436589025));
#75298=CARTESIAN_POINT('Ctrl Pts',(-1.95391930711152,0.0772811093863,0.119820872232394));
#75299=CARTESIAN_POINT('Ctrl Pts',(-1.95399890574746,0.00206793078572539,
0.124130307875763));
#75300=CARTESIAN_POINT('',(-1.95389762804932,0.000928492481393378,0.824130263460899));
#75301=CARTESIAN_POINT('Ctrl Pts',(-1.95399890574831,0.00206792998054292,
0.124130307921897));
#75302=CARTESIAN_POINT('Ctrl Pts',(-1.95406955740588,-0.0646912266989078,
0.127955359524064));
#75303=CARTESIAN_POINT('Ctrl Pts',(-1.95071478923537,-0.13160956121342,
0.131780411126231));
#75304=CARTESIAN_POINT('Ctrl Pts',(-1.94391228274796,-0.19829532768475,
0.135605462728398));
#75305=CARTESIAN_POINT('Ctrl Pts',(-1.93712039116072,-0.264877035048702,
0.139424545568767));
#75306=CARTESIAN_POINT('Ctrl Pts',(-1.92689148442229,-0.331226385592703,
0.143243628409135));
#75307=CARTESIAN_POINT('Ctrl Pts',(-1.91325525346835,-0.39695130063495,
0.147062711249504));
#75308=CARTESIAN_POINT('Ctrl Pts',(-1.89963070614838,-0.462619902033525,
0.150878521868523));
#75309=CARTESIAN_POINT('Ctrl Pts',(-1.88260471932677,-0.527664624549438,
0.154694332487542));
#75310=CARTESIAN_POINT('Ctrl Pts',(-1.86225862356753,-0.591699939959745,
0.158510143106561));
#75311=CARTESIAN_POINT('Ctrl Pts',(-1.8419222977489,-0.655704506412813,
0.162324121421064));
#75312=CARTESIAN_POINT('Ctrl Pts',(-1.8182691777226,-0.71870013514503,0.166138099735568));
#75313=CARTESIAN_POINT('Ctrl Pts',(-1.79143085391333,-0.780314997707577,
0.169952078050072));
#75314=CARTESIAN_POINT('Ctrl Pts',(-1.76459531424852,-0.841923468489488,
0.173765660711453));
#75315=CARTESIAN_POINT('Ctrl Pts',(-1.73457543415262,-0.902150985105781,
0.177579243372835));
#75316=CARTESIAN_POINT('Ctrl Pts',(-1.70155067162945,-0.96064629904944,
0.181392826034217));
#75317=CARTESIAN_POINT('Ctrl Pts',(-1.66849454045527,-1.01919717490931,
0.185210031036364));
#75318=CARTESIAN_POINT('Ctrl Pts',(-1.63242808464034,-1.07601211415674,
0.189027236038511));
#75319=CARTESIAN_POINT('Ctrl Pts',(-1.59357574474819,-1.13076626486213,
0.192844441040659));
#75320=CARTESIAN_POINT('Ctrl Pts',(-1.55470355505822,-1.18554838965672,
0.196663596266339));
#75321=CARTESIAN_POINT('Ctrl Pts',(-1.5130429731434,-1.23826722921297,0.200482751492019));
#75322=CARTESIAN_POINT('Ctrl Pts',(-1.46885870121783,-1.28863110154018,
0.204301906717699));
#75323=CARTESIAN_POINT('Ctrl Pts',(-1.42459648896941,-1.33908381490286,
0.208127798869854));
#75324=CARTESIAN_POINT('Ctrl Pts',(-1.37780206632569,-1.38717290575991,
0.211953691022008));
#75325=CARTESIAN_POINT('Ctrl Pts',(-1.32877610474772,-1.43264443022387,
0.215779583174163));
#75326=CARTESIAN_POINT('Ctrl Pts',(-1.30048043891891,-1.45888862859442,
0.217987722746546));
#75327=CARTESIAN_POINT('Ctrl Pts',(-1.27144203572435,-1.48426164641819,
0.220195862318929));
#75328=CARTESIAN_POINT('Ctrl Pts',(-1.24172311025443,-1.50872121926486,
0.222404001891312));
#75329=CARTESIAN_POINT('Ctrl Pts',(-1.18891487557722,-1.55218399063252,
0.226327695325534));
#75330=CARTESIAN_POINT('Ctrl Pts',(-1.13371889692835,-1.59295568107147,
0.230251388759756));
#75331=CARTESIAN_POINT('Ctrl Pts',(-1.076440251592,-1.63076435598542,0.234175082193978));
#75332=CARTESIAN_POINT('Ctrl Pts',(-1.01924776964084,-1.66851615589123,
0.238092873276516));
#75333=CARTESIAN_POINT('Ctrl Pts',(-0.959979245251721,-1.70331351914499,
0.242010664359055));
#75334=CARTESIAN_POINT('Ctrl Pts',(-0.89897254650893,-1.73492488616172,
0.245928455441593));
#75335=CARTESIAN_POINT('Ctrl Pts',(-0.838037968455182,-1.76649888296144,
0.24984161500336));
#75336=CARTESIAN_POINT('Ctrl Pts',(-0.775369730677549,-1.79489414000529,
0.253754774565128));
#75337=CARTESIAN_POINT('Ctrl Pts',(-0.711332838444815,-1.8199235129395,
0.257667934126895));
#75338=CARTESIAN_POINT('Ctrl Pts',(-0.647336410006956,-1.84493707024967,
0.261578621031412));
#75339=CARTESIAN_POINT('Ctrl Pts',(-0.581973498435363,-1.86658878482378,
0.26548930793593));
#75340=CARTESIAN_POINT('Ctrl Pts',(-0.515630360478018,-1.8847390618739,
0.269399994840448));
#75341=CARTESIAN_POINT('Ctrl Pts',(-0.44930657342817,-1.90288404486734,
0.273309541079286));
#75342=CARTESIAN_POINT('Ctrl Pts',(-0.38200360027134,-1.91752948866426,
0.277219087318124));
#75343=CARTESIAN_POINT('Ctrl Pts',(-0.31412246064153,-1.92858577193769,
0.281128633556962));
#75344=CARTESIAN_POINT('Ctrl Pts',(-0.246238028086697,-1.93964259155322,
0.285038369448518));
#75345=CARTESIAN_POINT('Ctrl Pts',(-0.177775857649897,-1.94710982862172,
0.288948105340075));
#75346=CARTESIAN_POINT('Ctrl Pts',(-0.109144972932498,-1.9509493522087,
0.292857841231631));
#75347=CARTESIAN_POINT('Ctrl Pts',(-0.0404427080086257,-1.95479286912883,
0.296771643481305));
#75348=CARTESIAN_POINT('Ctrl Pts',(0.0284281309814633,-1.95500111492118,
0.300685445730979));
#75349=CARTESIAN_POINT('Ctrl Pts',(0.0970566172690447,-1.9515880746316,
0.304599247980653));
#75350=CARTESIAN_POINT('Ctrl Pts',(0.165725237059831,-1.94817303841773,
0.308515338997042));
#75351=CARTESIAN_POINT('Ctrl Pts',(0.234150734215375,-1.94113255080181,
0.312431430013431));
#75352=CARTESIAN_POINT('Ctrl Pts',(0.301928186540551,-1.93053240588505,
0.31634752102982));
#75353=CARTESIAN_POINT('Ctrl Pts',(0.369820574104487,-1.91991428551857,
0.320270252851382));
#75354=CARTESIAN_POINT('Ctrl Pts',(0.437062243846608,-1.90572456052515,
0.324192984672943));
#75355=CARTESIAN_POINT('Ctrl Pts',(0.503260179663232,-1.88807976303051,
0.328115716494505));
#75356=CARTESIAN_POINT('Ctrl Pts',(0.53414389705252,-1.8798478305315,0.329945811941993));
#75357=CARTESIAN_POINT('Ctrl Pts',(0.564800681929095,-1.87086458341792,
0.33177590738948));
#75358=CARTESIAN_POINT('Ctrl Pts',(0.595192097517251,-1.86114544489489,
0.333606002836968));
#75359=CARTESIAN_POINT('Ctrl Pts',(0.660365323478706,-1.84030312482348,
0.337530572384713));
#75360=CARTESIAN_POINT('Ctrl Pts',(0.724566803469462,-1.81599359574741,
0.341455141932458));
#75361=CARTESIAN_POINT('Ctrl Pts',(0.787402665257627,-1.78832688363878,
0.345379711480203));
#75362=CARTESIAN_POINT('Ctrl Pts',(0.850146299341622,-1.76070077950889,
0.349298520718008));
#75363=CARTESIAN_POINT('Ctrl Pts',(0.911527848716609,-1.7297274689731,0.353217329955813));
#75364=CARTESIAN_POINT('Ctrl Pts',(0.971169742846146,-1.69556637457227,
0.357136139193618));
#75365=CARTESIAN_POINT('Ctrl Pts',(1.03074429109471,-1.66144385387925,0.361050523426746));
#75366=CARTESIAN_POINT('Ctrl Pts',(1.088582662301,-1.62414094095966,0.364964907659874));
#75367=CARTESIAN_POINT('Ctrl Pts',(1.14433001772578,-1.58386388636515,0.368879291893001));
#75368=CARTESIAN_POINT('Ctrl Pts',(1.20004397769646,-1.5436109597408,0.372791331214195));
#75369=CARTESIAN_POINT('Ctrl Pts',(1.25366901067057,-1.5003877125148,0.376703370535389));
#75370=CARTESIAN_POINT('Ctrl Pts',(1.30487884291397,-1.45444395055826,0.380615409856583));
#75371=CARTESIAN_POINT('Ctrl Pts',(1.35607539351088,-1.40851210445415,0.384526434561618));
#75372=CARTESIAN_POINT('Ctrl Pts',(1.40485762252771,-1.35986147163389,0.388437459266652));
#75373=CARTESIAN_POINT('Ctrl Pts',(1.45093335970032,-1.30878125968732,0.392348483971687));
#75374=CARTESIAN_POINT('Ctrl Pts',(1.49701279774398,-1.25769694490293,0.396259822815984));
#75375=CARTESIAN_POINT('Ctrl Pts',(1.54038498602521,-1.20418302905568,0.40017116166028));
#75376=CARTESIAN_POINT('Ctrl Pts',(1.58079677904237,-1.14856325179298,0.404082500504577));
#75377=CARTESIAN_POINT('Ctrl Pts',(1.62125243037714,-1.09288311121367,0.407998084266718));
#75378=CARTESIAN_POINT('Ctrl Pts',(1.65874098605547,-1.03509294534008,0.41191366802886));
#75379=CARTESIAN_POINT('Ctrl Pts',(1.69305213268919,-0.975546244929774,
0.415829251791001));
#75380=CARTESIAN_POINT('Ctrl Pts',(1.72738425196474,-0.915963146679629,
0.419747228948405));
#75381=CARTESIAN_POINT('Ctrl Pts',(1.75853487473283,-0.854621813839973,
0.42366520610581));
#75382=CARTESIAN_POINT('Ctrl Pts',(1.78634054088466,-0.791898650075812,
0.427583183263214));
#75383=CARTESIAN_POINT('Ctrl Pts',(1.81419434865803,-0.729066889927195,
0.431507943850027));
#75384=CARTESIAN_POINT('Ctrl Pts',(1.83869146635988,-0.664848981323484,
0.435432704436839));
#75385=CARTESIAN_POINT('Ctrl Pts',(1.85971756427337,-0.599638708834834,
0.439357465023652));
#75386=CARTESIAN_POINT('Ctrl Pts',(1.86945094453038,-0.569451634589951,
0.441174311276643));
#75387=CARTESIAN_POINT('Ctrl Pts',(1.87844121977373,-0.539052075038428,
0.442991157529633));
#75388=CARTESIAN_POINT('Ctrl Pts',(1.88668076778593,-0.508479773901289,
0.444808003782624));
#75389=CARTESIAN_POINT('Ctrl Pts',(1.9044236565005,-0.442645951946244,0.448720366551869));
#75390=CARTESIAN_POINT('Ctrl Pts',(1.91875277173103,-0.375748034148455,
0.452632729321114));
#75391=CARTESIAN_POINT('Ctrl Pts',(1.9295452933751,-0.308173588767728,0.456545092090358));
#75392=CARTESIAN_POINT('Ctrl Pts',(1.94032129714163,-0.240702565594617,
0.460451467016235));
#75393=CARTESIAN_POINT('Ctrl Pts',(1.94757137127701,-0.172557552819724,
0.464357841942112));
#75394=CARTESIAN_POINT('Ctrl Pts',(1.95122293739034,-0.104139563095908,
0.46826421686799));
#75395=CARTESIAN_POINT('Ctrl Pts',(1.95487010940956,-0.0358039038233925,
0.47216589107682));
#75396=CARTESIAN_POINT('Ctrl Pts',(1.95492734649464,0.0328035896702445,
0.47606756528565));
#75397=CARTESIAN_POINT('Ctrl Pts',(1.95137369834605,0.101275314876119,0.479969239494481));
#75398=CARTESIAN_POINT('Ctrl Pts',(1.94782233509269,0.169703014699623,0.483868405037166));
#75399=CARTESIAN_POINT('Ctrl Pts',(1.94066471706783,0.237994627663291,0.487767570579851));
#75400=CARTESIAN_POINT('Ctrl Pts',(1.92993197530334,0.30574265437089,0.491666736122537));
#75401=CARTESIAN_POINT('Ctrl Pts',(1.91920242318858,0.373470547129496,0.495564742877225));
#75402=CARTESIAN_POINT('Ctrl Pts',(1.90489993343761,0.440654687062428,0.499462749631914));
#75403=CARTESIAN_POINT('Ctrl Pts',(1.88710726506204,0.506894634169728,0.503360756386602));
#75404=CARTESIAN_POINT('Ctrl Pts',(1.86931373221155,0.573137799612361,0.507258952529921));
#75405=CARTESIAN_POINT('Ctrl Pts',(1.84802981460086,0.63843620516231,0.51115714867324));
#75406=CARTESIAN_POINT('Ctrl Pts',(1.82338849546918,0.702403299102889,0.515055344816559));
#75407=CARTESIAN_POINT('Ctrl Pts',(1.79872096906624,0.766438425236626,0.518957686885801));
#75408=CARTESIAN_POINT('Ctrl Pts',(1.77068909265435,0.829138952520078,0.522860028955043));
#75409=CARTESIAN_POINT('Ctrl Pts',(1.73947412521829,0.890138061031027,0.526762371024285));
#75410=CARTESIAN_POINT('Ctrl Pts',(1.7082406204775,0.951173394441619,0.530667030536409));
#75411=CARTESIAN_POINT('Ctrl Pts',(1.67382051073079,1.01050487141279,0.534571690048533));
#75412=CARTESIAN_POINT('Ctrl Pts',(1.63643976155116,1.06779253922023,0.538476349560657));
#75413=CARTESIAN_POINT('Ctrl Pts',(1.59899385409424,1.12518006499805,0.542387815273642));
#75414=CARTESIAN_POINT('Ctrl Pts',(1.55857729832838,1.18051627299139,0.546299280986626));
#75415=CARTESIAN_POINT('Ctrl Pts',(1.51545734802895,1.23349301834468,0.550210746699611));
#75416=CARTESIAN_POINT('Ctrl Pts',(1.49414703144356,1.25967466297327,0.552143832709167));
#75417=CARTESIAN_POINT('Ctrl Pts',(1.47217701434554,1.28528057601971,0.554076918718724));
#75418=CARTESIAN_POINT('Ctrl Pts',(1.44958276974344,1.31027699119802,0.55601000472828));
#75419=CARTESIAN_POINT('Ctrl Pts',(1.40377828829966,1.36095130473934,0.559928878928912));
#75420=CARTESIAN_POINT('Ctrl Pts',(1.35522274662966,1.40932119078568,0.563847753129544));
#75421=CARTESIAN_POINT('Ctrl Pts',(1.30417707256363,1.45507325018343,0.567766627330176));
#75422=CARTESIAN_POINT('Ctrl Pts',(1.25320829705278,1.50075638567472,0.57167959788139));
#75423=CARTESIAN_POINT('Ctrl Pts',(1.19975719741317,1.54382919586173,0.575592568432604));
#75424=CARTESIAN_POINT('Ctrl Pts',(1.14412310761945,1.58401335682854,0.579505538983818));
#75425=CARTESIAN_POINT('Ctrl Pts',(1.08855453628523,1.62415019421492,0.583413901356782));
#75426=CARTESIAN_POINT('Ctrl Pts',(1.03080847727012,1.66140485211139,0.587322263729745));
#75427=CARTESIAN_POINT('Ctrl Pts',(0.9712176677035,1.69553892374683,0.591230626102709));
#75428=CARTESIAN_POINT('Ctrl Pts',(0.911664288785019,1.72965155482065,0.595136533524349));
#75429=CARTESIAN_POINT('Ctrl Pts',(0.850268883585566,1.76064724411937,0.59904244094599));
#75430=CARTESIAN_POINT('Ctrl Pts',(0.787392215127153,1.78833148480844,0.60294834836763));
#75431=CARTESIAN_POINT('Ctrl Pts',(0.72453349817706,1.81600782155016,0.606853140639068));
#75432=CARTESIAN_POINT('Ctrl Pts',(0.660194807281561,1.84037438850214,0.610757932910506));
#75433=CARTESIAN_POINT('Ctrl Pts',(0.594758853395274,1.86128394027025,0.614662725181944));
#75434=CARTESIAN_POINT('Ctrl Pts',(0.529319162480106,1.88219468617697,0.618567740454967));
#75435=CARTESIAN_POINT('Ctrl Pts',(0.462782553274368,1.89964787770071,0.622472755727991));
#75436=CARTESIAN_POINT('Ctrl Pts',(0.395547203749737,1.9135460301769,0.626377771001015));
#75437=CARTESIAN_POINT('Ctrl Pts',(0.328240393553435,1.92745895421772,0.630286936695153));
#75438=CARTESIAN_POINT('Ctrl Pts',(0.260233843326273,1.93780919873518,0.634196102389291));
#75439=CARTESIAN_POINT('Ctrl Pts',(0.191935248663222,1.94455055483795,0.638105268083429));
#75440=CARTESIAN_POINT('Ctrl Pts',(0.123595941658968,1.95129592941857,0.64201676400542));
#75441=CARTESIAN_POINT('Ctrl Pts',(0.0549647349864728,1.9544281116713,0.64592825992741));
#75442=CARTESIAN_POINT('Ctrl Pts',(-0.0135490597968924,1.95395302476252,
0.6498397558494));
#75443=CARTESIAN_POINT('Ctrl Pts',(-0.0821811566735969,1.95347711752587,
0.6537580057128));
#75444=CARTESIAN_POINT('Ctrl Pts',(-0.15069494646004,1.94938153877401,0.657676255576199));
#75445=CARTESIAN_POINT('Ctrl Pts',(-0.218685496651521,1.94172414455666,
0.661594505439598));
#75446=CARTESIAN_POINT('Ctrl Pts',(-0.251177633442923,1.93806473748206,
0.663467005517711));
#75447=CARTESIAN_POINT('Ctrl Pts',(-0.283550413865308,1.93359263600638,
0.665339505595823));
#75448=CARTESIAN_POINT('Ctrl Pts',(-0.315760658977315,1.92831823261676,
0.667212005673936));
#75449=CARTESIAN_POINT('Ctrl Pts',(-0.383166145740961,1.91728063490121,
0.671130534663431));
#75450=CARTESIAN_POINT('Ctrl Pts',(-0.450125490731316,1.90268265935469,
0.675049063652926));
#75451=CARTESIAN_POINT('Ctrl Pts',(-0.516233959946512,1.88457382413052,
0.678967592642421));
#75452=CARTESIAN_POINT('Ctrl Pts',(-0.582243056814569,1.86649220958597,
0.682880231411985));
#75453=CARTESIAN_POINT('Ctrl Pts',(-0.647403345824134,1.84491033813827,
0.686792870181548));
#75454=CARTESIAN_POINT('Ctrl Pts',(-0.711318768867144,1.81992901209287,
0.690705508951112));
#75455=CARTESIAN_POINT('Ctrl Pts',(-0.775159268726725,1.79497696975372,
0.694613561232184));
#75456=CARTESIAN_POINT('Ctrl Pts',(-0.837757344874346,1.76663356510626,
0.698521613513256));
#75457=CARTESIAN_POINT('Ctrl Pts',(-0.898732394159872,1.73504930295587,
0.702429665794328));
#75458=CARTESIAN_POINT('Ctrl Pts',(-0.959669353667418,1.70348477080239,
0.706335276800723));
#75459=CARTESIAN_POINT('Ctrl Pts',(-1.0189848618327,1.66868362279679,0.710240887807119));
#75460=CARTESIAN_POINT('Ctrl Pts',(-1.07632003494276,1.63084370262169,0.714146498813514));
#75461=CARTESIAN_POINT('Ctrl Pts',(-1.13363904553076,1.59301444934635,0.718051008846098));
#75462=CARTESIAN_POINT('Ctrl Pts',(-1.18897841904067,1.55214839518999,0.721955518878682));
#75463=CARTESIAN_POINT('Ctrl Pts',(-1.24200711024413,1.50848743385652,0.725860028911266));
#75464=CARTESIAN_POINT('Ctrl Pts',(-1.2950390296435,1.46482381460082,0.729764776636372));
#75465=CARTESIAN_POINT('Ctrl Pts',(-1.3457596094451,1.4183652649158,0.733669524361477));
#75466=CARTESIAN_POINT('Ctrl Pts',(-1.39387125524627,1.36939363361971,0.737574272086583));
#75467=CARTESIAN_POINT('Ctrl Pts',(-1.44203433832124,1.32036964561942,0.741483194467836));
#75468=CARTESIAN_POINT('Ctrl Pts',(-1.48758257552104,1.26882756542321,0.745392116849089));
#75469=CARTESIAN_POINT('Ctrl Pts',(-1.53025631837195,1.21508501763569,0.749301039230342));
#75470=CARTESIAN_POINT('Ctrl Pts',(-1.57295564752691,1.16131024691491,0.753212305321565));
#75471=CARTESIAN_POINT('Ctrl Pts',(-1.61277676715721,1.10533278360485,0.757123571412787));
#75472=CARTESIAN_POINT('Ctrl Pts',(-1.64950297744994,1.04749984600657,0.76103483750401));
#75473=CARTESIAN_POINT('Ctrl Pts',(-1.68629282591488,0.989566697076561,
0.764952880930088));
#75474=CARTESIAN_POINT('Ctrl Pts',(-1.71997682037156,0.92977208513841,0.768870924356166));
#75475=CARTESIAN_POINT('Ctrl Pts',(-1.75038428830772,0.868487675931825,
0.772788967782244));
#75476=CARTESIAN_POINT('Ctrl Pts',(-1.76493604024832,0.839159501600691,
0.774663980728026));
#75477=CARTESIAN_POINT('Ctrl Pts',(-1.77873812108614,0.809490427406177,
0.776538993673809));
#75478=CARTESIAN_POINT('Ctrl Pts',(-1.79177582235983,0.77952254772185,0.778414006619591));
#75479=CARTESIAN_POINT('Ctrl Pts',(-1.82180013066274,0.710510009396372,
0.782731943161803));
#75480=CARTESIAN_POINT('Ctrl Pts',(-1.84787001263996,0.639676840066979,
0.787049879704015));
#75481=CARTESIAN_POINT('Ctrl Pts',(-1.86978437594614,0.567470164385505,
0.791367816246227));
#75482=CARTESIAN_POINT('Ctrl Pts',(-1.89163136933685,0.49548546903576,0.795672478434275));
#75483=CARTESIAN_POINT('Ctrl Pts',(-1.9093481871965,0.422135977045125,0.799977140622323));
#75484=CARTESIAN_POINT('Ctrl Pts',(-1.92278189205019,0.347887619216186,
0.80428180281037));
#75485=CARTESIAN_POINT('Ctrl Pts',(-1.93614789390559,0.274013457225047,
0.808564770421985));
#75486=CARTESIAN_POINT('Ctrl Pts',(-1.94527371417388,0.19924976401323,0.812847738033601));
#75487=CARTESIAN_POINT('Ctrl Pts',(-1.95005683809791,0.124073881971984,
0.817130705645216));
#75488=CARTESIAN_POINT('Ctrl Pts',(-1.95266248815594,0.0831211396816443,
0.819463891024273));
#75489=CARTESIAN_POINT('Ctrl Pts',(-1.95398023955751,0.0420463704976374,
0.82179707640333));
#75490=CARTESIAN_POINT('Ctrl Pts',(-1.95399977936455,0.000928570563274659,
0.824130261782387));
#75491=CARTESIAN_POINT('',(-1.9539992614335,-0.00169891651796276,1.52413032658075));
#75492=CARTESIAN_POINT('Ctrl Pts',(-1.95119461725619,0.00092642636832007,
0.824130307875761));
#75493=CARTESIAN_POINT('Ctrl Pts',(-1.94958058750438,-0.38320769809472,
0.845958874438923));
#75494=CARTESIAN_POINT('Ctrl Pts',(-1.65406893488018,-1.42195455262908,
0.904854774650637));
#75495=CARTESIAN_POINT('Ctrl Pts',(0.0349978082279151,-2.30969445268954,
1.0008180085109));
#75496=CARTESIAN_POINT('Ctrl Pts',(1.96019660501107,-1.22214099283921,1.11202000945656));
#75497=CARTESIAN_POINT('Ctrl Pts',(2.08932028008313,0.985264718230409,1.22322201040221));
#75498=CARTESIAN_POINT('Ctrl Pts',(0.304039107037155,2.28987742561639,1.33442401134788));
#75499=CARTESIAN_POINT('Ctrl Pts',(-1.55753832107891,1.5741108521456,1.43472677717238));
#75500=CARTESIAN_POINT('Ctrl Pts',(-1.94902381498454,0.457824381443284,
1.49796220934835));
#75501=CARTESIAN_POINT('Ctrl Pts',(-1.95283689833027,-0.00169757742976787,
1.52413030787576));
#75502=CARTESIAN_POINT('',(-1.95399999997531,9.82336242309353E-6,2.22413030790917));
#75503=CARTESIAN_POINT('Ctrl Pts',(-1.9539992614335,-0.00169891651796276,
1.52413032658075));
#75504=CARTESIAN_POINT('Ctrl Pts',(-1.95392695442445,-0.0848624156019545,
1.52886340490957));
#75505=CARTESIAN_POINT('Ctrl Pts',(-1.94854160179058,-0.167792826350324,
1.53359648323839));
#75506=CARTESIAN_POINT('Ctrl Pts',(-1.93795475085125,-0.249894745149011,
1.53832956156721));
#75507=CARTESIAN_POINT('Ctrl Pts',(-1.92720840960645,-0.333233524670808,
1.54313394345104));
#75508=CARTESIAN_POINT('Ctrl Pts',(-1.91110273860045,-0.415718692889136,
1.54793832533488));
#75509=CARTESIAN_POINT('Ctrl Pts',(-1.88980307899214,-0.496749758562415,
1.55274270721872));
#75510=CARTESIAN_POINT('Ctrl Pts',(-1.88376583842472,-0.519717451281494,
1.55410447589221));
#75511=CARTESIAN_POINT('Ctrl Pts',(-1.87731160600884,-0.542568454780191,
1.55546624456569));
#75512=CARTESIAN_POINT('Ctrl Pts',(-1.8704448365791,-0.565289406688817,
1.55682801323918));
#75513=CARTESIAN_POINT('Ctrl Pts',(-1.85068959414275,-0.630656085726513,
1.56074573183483));
#75514=CARTESIAN_POINT('Ctrl Pts',(-1.82746439869295,-0.695115839472794,
1.56466345043049));
#75515=CARTESIAN_POINT('Ctrl Pts',(-1.80087105238586,-0.758273995781628,
1.56858116902614));
#75516=CARTESIAN_POINT('Ctrl Pts',(-1.77431781679637,-0.821336890706583,
1.57249297853076));
#75517=CARTESIAN_POINT('Ctrl Pts',(-1.74440670199538,-0.883101634631058,
1.57640478803539));
#75518=CARTESIAN_POINT('Ctrl Pts',(-1.71128922679017,-0.943188837016162,
1.58031659754001));
#75519=CARTESIAN_POINT('Ctrl Pts',(-1.67821078334524,-1.00320522152445,
1.58422379664453));
#75520=CARTESIAN_POINT('Ctrl Pts',(-1.64193372088679,-1.06154756222763,
1.58813099574906));
#75521=CARTESIAN_POINT('Ctrl Pts',(-1.60265682155651,-1.11785827022855,
1.59203819485359));
#75522=CARTESIAN_POINT('Ctrl Pts',(-1.56340460731049,-1.17413358759033,
1.59594293832794));
#75523=CARTESIAN_POINT('Ctrl Pts',(-1.52115657694202,-1.22837940247629,
1.5998476818023));
#75524=CARTESIAN_POINT('Ctrl Pts',(-1.47615561562483,-1.28026583116917,
1.60375242527665));
#75525=CARTESIAN_POINT('Ctrl Pts',(-1.43116749310002,-1.33213745664305,
1.60765605472612));
#75526=CARTESIAN_POINT('Ctrl Pts',(-1.383428320985,-1.38165066067867,1.61155968417558));
#75527=CARTESIAN_POINT('Ctrl Pts',(-1.33322102711829,-1.42850890541489,
1.61546331362505));
#75528=CARTESIAN_POINT('Ctrl Pts',(-1.28301082739003,-1.47536986217882,
1.61936716900597));
#75529=CARTESIAN_POINT('Ctrl Pts',(-1.23033258373456,-1.51957522074296,
1.62327102438689));
#75530=CARTESIAN_POINT('Ctrl Pts',(-1.17550447248529,-1.56086682172666,
1.62717487976781));
#75531=CARTESIAN_POINT('Ctrl Pts',(-1.12061789490383,-1.60220245429206,
1.63108289805167));
#75532=CARTESIAN_POINT('Ctrl Pts',(-1.06357726827144,-1.64061783182154,
1.63499091633552));
#75533=CARTESIAN_POINT('Ctrl Pts',(-1.00473128432354,-1.6758970870258,1.63889893461938));
#75534=CARTESIAN_POINT('Ctrl Pts',(-0.94585013040328,-1.71119742727864,
1.64280928857486));
#75535=CARTESIAN_POINT('Ctrl Pts',(-0.885161906579292,-1.74335768452249,
1.64671964253035));
#75536=CARTESIAN_POINT('Ctrl Pts',(-0.823039035615062,-1.77220843747394,
1.65062999648583));
#75537=CARTESIAN_POINT('Ctrl Pts',(-0.760808540287798,-1.80110917272436,
1.65454712490855));
#75538=CARTESIAN_POINT('Ctrl Pts',(-0.697138893503489,-1.82668877696017,
1.65846425333126));
#75539=CARTESIAN_POINT('Ctrl Pts',(-0.632420742890022,-1.84882665600711,
1.66238138175398));
#75540=CARTESIAN_POINT('Ctrl Pts',(-0.601312151342819,-1.8594678475502,
1.66426425923093));
#75541=CARTESIAN_POINT('Ctrl Pts',(-0.569961498234108,-1.86931457355083,
1.66614713670789));
#75542=CARTESIAN_POINT('Ctrl Pts',(-0.538413007585896,-1.87835764253305,
1.66803001418484));
#75543=CARTESIAN_POINT('Ctrl Pts',(-0.472769903991052,-1.89717360176971,
1.67194772684673));
#75544=CARTESIAN_POINT('Ctrl Pts',(-0.40600881106407,-1.91258176029287,
1.67586543950862));
#75545=CARTESIAN_POINT('Ctrl Pts',(-0.338516599480537,-1.9244538217053,
1.67978315217051));
#75546=CARTESIAN_POINT('Ctrl Pts',(-0.271126187234549,-1.93630797634066,
1.68369495569794));
#75547=CARTESIAN_POINT('Ctrl Pts',(-0.203007325537228,-1.94463653440483,
1.68760675922537));
#75548=CARTESIAN_POINT('Ctrl Pts',(-0.134560980986145,-1.94936126523435,
1.69151856275279));
#75549=CARTESIAN_POINT('Ctrl Pts',(-0.0661953069987432,-1.95408042751667,
1.69542575584561));
#75550=CARTESIAN_POINT('Ctrl Pts',(0.00249659480716174,-1.95520416429194,
1.69933294893843));
#75551=CARTESIAN_POINT('Ctrl Pts',(0.0711064711692457,-1.95270578166755,
1.70324014203125));
#75552=CARTESIAN_POINT('Ctrl Pts',(0.139673226624597,-1.95020896926205,
1.70714487947602));
#75553=CARTESIAN_POINT('Ctrl Pts',(0.20815756833239,-1.94409457108146,1.71104961692079));
#75554=CARTESIAN_POINT('Ctrl Pts',(0.276150630565734,-1.93438797278058,
1.71495435436556));
#75555=CARTESIAN_POINT('Ctrl Pts',(0.344124294171014,-1.9246841438018,1.71885797777683));
#75556=CARTESIAN_POINT('Ctrl Pts',(0.411606469711573,-1.91139021870064,
1.7227616011881));
#75557=CARTESIAN_POINT('Ctrl Pts',(0.478194619982706,-1.89458330653988,
1.72666522459936));
#75558=CARTESIAN_POINT('Ctrl Pts',(0.544786624211529,-1.87777542163656,
1.73056907394271));
#75559=CARTESIAN_POINT('Ctrl Pts',(0.610484024023804,-1.85745426888696,
1.73447292328606));
#75560=CARTESIAN_POINT('Ctrl Pts',(0.674897438294774,-1.83374737839844,
1.73837677262941));
#75561=CARTESIAN_POINT('Ctrl Pts',(0.739379541061065,-1.81001520760682,
1.74228478491833));
#75562=CARTESIAN_POINT('Ctrl Pts',(0.802574463128006,-1.78289026391186,
1.74619279720724));
#75563=CARTESIAN_POINT('Ctrl Pts',(0.864111833408501,-1.75254864108344,
1.75010080949616));
#75564=CARTESIAN_POINT('Ctrl Pts',(0.92568598249944,-1.72218888409053,1.7540111574722));
#75565=CARTESIAN_POINT('Ctrl Pts',(0.985600178950291,-1.68860886242822,
1.75792150544823));
#75566=CARTESIAN_POINT('Ctrl Pts',(1.04351022916227,-1.65202978230833,1.76183185342427));
#75567=CARTESIAN_POINT('Ctrl Pts',(1.10152060670916,-1.61538733008622,1.7657489759548));
#75568=CARTESIAN_POINT('Ctrl Pts',(1.15751950676532,-1.57573573348381,1.76966609848533));
#75569=CARTESIAN_POINT('Ctrl Pts',(1.21119389803979,-1.53333797362198,1.77358322101587));
#75570=CARTESIAN_POINT('Ctrl Pts',(1.23699477467599,-1.51295768898583,1.77546615238741));
#75571=CARTESIAN_POINT('Ctrl Pts',(1.2622590616211,-1.49194343294059,1.77734908375895));
#75572=CARTESIAN_POINT('Ctrl Pts',(1.28695506774092,-1.47032739674399,1.77923201513049));
#75573=CARTESIAN_POINT('Ctrl Pts',(1.33833866502721,-1.42535212043969,1.7831497250162));
#75574=CARTESIAN_POINT('Ctrl Pts',(1.3874639142744,-1.37759065900973,1.7870674349019));
#75575=CARTESIAN_POINT('Ctrl Pts',(1.43401335636865,-1.32729864527781,1.79098514478761));
#75576=CARTESIAN_POINT('Ctrl Pts',(1.48049258647854,-1.27708248856851,1.79489694546854));
#75577=CARTESIAN_POINT('Ctrl Pts',(1.52440338854723,-1.2243437128594,1.79880874614948));
#75578=CARTESIAN_POINT('Ctrl Pts',(1.56546274401249,-1.16937692687554,1.80272054683041));
#75579=CARTESIAN_POINT('Ctrl Pts',(1.60647370611654,-1.11447492582312,1.80662773698638));
#75580=CARTESIAN_POINT('Ctrl Pts',(1.64463960306984,-1.05735052198329,1.81053492714236));
#75581=CARTESIAN_POINT('Ctrl Pts',(1.6797167829136,-0.998332374111145,1.81444211729833));
#75582=CARTESIAN_POINT('Ctrl Pts',(1.71477191644938,-0.939351319650439,
1.81834685175182));
#75583=CARTESIAN_POINT('Ctrl Pts',(1.74674193291708,-0.878479304161515,
1.82225158620531));
#75584=CARTESIAN_POINT('Ctrl Pts',(1.77542661964497,-0.81607372109144,1.82615632065881));
#75585=CARTESIAN_POINT('Ctrl Pts',(1.80410312217094,-0.753685943336723,
1.83005994102883));
#75586=CARTESIAN_POINT('Ctrl Pts',(1.82949595035479,-0.689765913428525,
1.83396356139886));
#75587=CARTESIAN_POINT('Ctrl Pts',(1.85145179255203,-0.624693732845057,
1.83786718176888));
#75588=CARTESIAN_POINT('Ctrl Pts',(1.87340890524395,-0.559617786800943,
1.84177102802544));
#75589=CARTESIAN_POINT('Ctrl Pts',(1.89192848221934,-0.493390024716284,
1.84567487428199));
#75590=CARTESIAN_POINT('Ctrl Pts',(1.90690671786495,-0.426406812048687,
1.84957872053854));
#75591=CARTESIAN_POINT('Ctrl Pts',(1.92190092567108,-0.359352171300337,
1.85348672969255));
#75592=CARTESIAN_POINT('Ctrl Pts',(1.93334614807582,-0.291540953333802,
1.85739473884656));
#75593=CARTESIAN_POINT('Ctrl Pts',(1.94118969646704,-0.223379861066723,
1.86130274800057));
#75594=CARTESIAN_POINT('Ctrl Pts',(1.94903793262193,-0.155178031740894,
1.86521309280962));
#75595=CARTESIAN_POINT('Ctrl Pts',(1.95328018036679,-0.0866264030986778,
1.86912343761867));
#75596=CARTESIAN_POINT('Ctrl Pts',(1.95391585121788,-0.0181341214158713,
1.87303378242772));
#75597=CARTESIAN_POINT('Ctrl Pts',(1.95455262334687,0.0504768207916181,
1.87695090177479));
#75598=CARTESIAN_POINT('Ctrl Pts',(1.95157036920284,0.119027719528215,1.88086802112186));
#75599=CARTESIAN_POINT('Ctrl Pts',(1.94502049642343,0.187112983228721,1.88478514046894));
#75600=CARTESIAN_POINT('Ctrl Pts',(1.94187197380637,0.219841556724618,1.88666809900467));
#75601=CARTESIAN_POINT('Ctrl Pts',(1.93789983737931,0.25246266519304,1.88855105754041));
#75602=CARTESIAN_POINT('Ctrl Pts',(1.93311397113303,0.284932228100443,1.89043401607615));
#75603=CARTESIAN_POINT('Ctrl Pts',(1.92315642265863,0.352488910622552,1.89435172917762));
#75604=CARTESIAN_POINT('Ctrl Pts',(1.90963345760212,0.419657244532697,1.89826944227908));
#75605=CARTESIAN_POINT('Ctrl Pts',(1.8925879093297,0.486031897573641,1.90218715538055));
#75606=CARTESIAN_POINT('Ctrl Pts',(1.87556807114542,0.552306436605199,1.90609895932922));
#75607=CARTESIAN_POINT('Ctrl Pts',(1.85503631580055,0.61778919792082,1.91001076327789));
#75608=CARTESIAN_POINT('Ctrl Pts',(1.83108689664052,0.682082676038163,1.91392256722657));
#75609=CARTESIAN_POINT('Ctrl Pts',(1.80716570433876,0.746300377666639,1.91782976071121));
#75610=CARTESIAN_POINT('Ctrl Pts',(1.77983501889488,0.809331120999531,1.92173695419585));
#75611=CARTESIAN_POINT('Ctrl Pts',(1.74923904282111,0.870792036636921,1.9256441476805));
#75612=CARTESIAN_POINT('Ctrl Pts',(1.71866229628285,0.932214324160061,1.92954888549856));
#75613=CARTESIAN_POINT('Ctrl Pts',(1.68482454880486,0.992068301683998,1.93345362331663));
#75614=CARTESIAN_POINT('Ctrl Pts',(1.64791769151329,1.04999203901625,1.93735836113469));
#75615=CARTESIAN_POINT('Ctrl Pts',(1.61102136404073,1.10789925024699,1.9412619849001));
#75616=CARTESIAN_POINT('Ctrl Pts',(1.57105792927715,1.1638768997892,1.94516560866551));
#75617=CARTESIAN_POINT('Ctrl Pts',(1.52826377752397,1.21759017173602,1.94906923243091));
#75618=CARTESIAN_POINT('Ctrl Pts',(1.48546714916836,1.27130655220153,1.95297308210859));
#75619=CARTESIAN_POINT('Ctrl Pts',(1.43983978715841,1.32275791168654,1.95687693178628));
#75620=CARTESIAN_POINT('Ctrl Pts',(1.39165857650034,1.37164222975711,1.96078078146396));
#75621=CARTESIAN_POINT('Ctrl Pts',(1.34342598727786,1.42057867615841,1.96468879405472));
#75622=CARTESIAN_POINT('Ctrl Pts',(1.29263446046224,1.46694226699872,1.96859680664548));
#75623=CARTESIAN_POINT('Ctrl Pts',(1.23959726763818,1.51046834262224,1.97250481923624));
#75624=CARTESIAN_POINT('Ctrl Pts',(1.18652837652109,1.55402043210934,1.97641516749602));
#75625=CARTESIAN_POINT('Ctrl Pts',(1.13121154459855,1.59473133961202,1.98032551575581));
#75626=CARTESIAN_POINT('Ctrl Pts',(1.07399032801683,1.6323788700318,1.98423586401559));
#75627=CARTESIAN_POINT('Ctrl Pts',(1.01666997794584,1.67009162330555,1.98815298679872));
#75628=CARTESIAN_POINT('Ctrl Pts',(0.957439082795922,1.70473015878866,1.99207010958184));
#75629=CARTESIAN_POINT('Ctrl Pts',(0.896666385734625,1.73611790863801,1.99598723236496));
#75630=CARTESIAN_POINT('Ctrl Pts',(0.867453457630535,1.75120573794355,1.99787016058391));
#75631=CARTESIAN_POINT('Ctrl Pts',(0.837884578362065,1.76554313899271,1.99975308880286));
#75632=CARTESIAN_POINT('Ctrl Pts',(0.808002149859811,1.77911453420569,2.0016360170218));
#75633=CARTESIAN_POINT('Ctrl Pts',(0.745827315652347,1.80735183919136,2.00555372905879));
#75634=CARTESIAN_POINT('Ctrl Pts',(0.682046917070363,1.83238209596217,2.00947144109577));
#75635=CARTESIAN_POINT('Ctrl Pts',(0.617024832475356,1.85402167088434,2.01338915313276));
#75636=CARTESIAN_POINT('Ctrl Pts',(0.552100821983804,1.87562860640526,2.01730095600676));
#75637=CARTESIAN_POINT('Ctrl Pts',(0.4859393054637,1.89385485581639,2.02121275888075));
#75638=CARTESIAN_POINT('Ctrl Pts',(0.418925445613308,1.90856424335617,2.02512456175475));
#75639=CARTESIAN_POINT('Ctrl Pts',(0.351990568690836,1.92325629432559,2.02903175415496));
#75640=CARTESIAN_POINT('Ctrl Pts',(0.284205821803741,1.93443961040337,2.03293894655517));
#75641=CARTESIAN_POINT('Ctrl Pts',(0.215971132001531,1.94202792723019,2.03684613895537));
#75642=CARTESIAN_POINT('Ctrl Pts',(0.147779327729397,1.94961147479682,2.04075087568358));
#75643=CARTESIAN_POINT('Ctrl Pts',(0.0791386293835333,1.95360445084957,
2.04465561241179));
#75644=CARTESIAN_POINT('Ctrl Pts',(0.010457205880532,1.95397201792789,2.04856034914));
#75645=CARTESIAN_POINT('Ctrl Pts',(-0.0582046221962698,1.95433948013602,
2.05246397181179));
#75646=CARTESIAN_POINT('Ctrl Pts',(-0.126906660601441,1.95108358408695,
2.05636759448358));
#75647=CARTESIAN_POINT('Ctrl Pts',(-0.195239416744181,1.94422158463211,
2.06027121715538));
#75648=CARTESIAN_POINT('Ctrl Pts',(-0.263576127435452,1.93735918806011,
2.06417506573735));
#75649=CARTESIAN_POINT('Ctrl Pts',(-0.331543024149646,1.92689032545489,
2.06807891431933));
#75650=CARTESIAN_POINT('Ctrl Pts',(-0.39873623534906,1.91288405676341,2.0719827629013));
#75651=CARTESIAN_POINT('Ctrl Pts',(-0.466001098864394,1.89886285231323,
2.07589077440073));
#75652=CARTESIAN_POINT('Ctrl Pts',(-0.532490147758416,1.88129681421564,
2.07979878590016));
#75653=CARTESIAN_POINT('Ctrl Pts',(-0.597811194576149,1.86030582852375,
2.0837067973996));
#75654=CARTESIAN_POINT('Ctrl Pts',(-0.663171281300395,1.83930229731769,
2.08761714456894));
#75655=CARTESIAN_POINT('Ctrl Pts',(-0.727361516769884,1.81486991974442,
2.09152749173828));
#75656=CARTESIAN_POINT('Ctrl Pts',(-0.790008993625948,1.78717704494829,
2.09543783890762));
#75657=CARTESIAN_POINT('Ctrl Pts',(-0.852765004988979,1.75943619323972,
2.0993549606132));
#75658=CARTESIAN_POINT('Ctrl Pts',(-0.913972484550015,1.72842379249747,
2.10327208231878));
#75659=CARTESIAN_POINT('Ctrl Pts',(-0.973283225352221,1.69435408437787,
2.10718920402436));
#75660=CARTESIAN_POINT('Ctrl Pts',(-1.00179355894251,1.67797697071051,2.10907214200539));
#75661=CARTESIAN_POINT('Ctrl Pts',(-1.0298660529186,1.66089405636913,2.11095507998643));
#75662=CARTESIAN_POINT('Ctrl Pts',(-1.05746463830973,1.64313253839259,2.11283801796746));
#75663=CARTESIAN_POINT('Ctrl Pts',(-1.11489578162405,1.60617179312489,2.1167563086881));
#75664=CARTESIAN_POINT('Ctrl Pts',(-1.17050077078353,1.56612305683658,2.12067459940874));
#75665=CARTESIAN_POINT('Ctrl Pts',(-1.22392803543809,1.52319275341916,2.12459289012938));
#75666=CARTESIAN_POINT('Ctrl Pts',(-1.27727472049635,1.48032719796406,2.12850527124026));
#75667=CARTESIAN_POINT('Ctrl Pts',(-1.32844981924711,1.43458900625428,2.13241765235114));
#75668=CARTESIAN_POINT('Ctrl Pts',(-1.37713012110195,1.38622820255314,2.13633003346202));
#75669=CARTESIAN_POINT('Ctrl Pts',(-1.42575303011744,1.33792441501117,2.14023780197495));
#75670=CARTESIAN_POINT('Ctrl Pts',(-1.47188663644957,1.2870045012155,2.14414557048788));
#75671=CARTESIAN_POINT('Ctrl Pts',(-1.51524168221546,1.23375793593268,2.14805333900081));
#75672=CARTESIAN_POINT('Ctrl Pts',(-1.55856945797604,1.18054486234828,2.15195864955605));
#75673=CARTESIAN_POINT('Ctrl Pts',(-1.59912183018387,1.12500842081584,2.15586396011129));
#75674=CARTESIAN_POINT('Ctrl Pts',(-1.63664829953451,1.06747287723427,2.15976927066653));
#75675=CARTESIAN_POINT('Ctrl Pts',(-1.67416403321688,1.00995379356806,2.16367346398054));
#75676=CARTESIAN_POINT('Ctrl Pts',(-1.70865531393348,0.950437154933405,
2.16757765729456));
#75677=CARTESIAN_POINT('Ctrl Pts',(-1.73991470740603,0.889276566064914,
2.17148185060857));
#75678=CARTESIAN_POINT('Ctrl Pts',(-1.77117587693582,0.828112502250339,
2.17538626574618));
#75679=CARTESIAN_POINT('Ctrl Pts',(-1.79920457307696,0.765304741865069,
2.17929068088378));
#75680=CARTESIAN_POINT('Ctrl Pts',(-1.82383994727051,0.701230238039046,
2.18319509602138));
#75681=CARTESIAN_POINT('Ctrl Pts',(-1.84850158070921,0.637087436159569,
2.18710367293844));
#75682=CARTESIAN_POINT('Ctrl Pts',(-1.86976249674088,0.571675656065409,
2.1910122498555));
#75683=CARTESIAN_POINT('Ctrl Pts',(-1.88751089425965,0.505389576516129,
2.19492082677256));
#75684=CARTESIAN_POINT('Ctrl Pts',(-1.9052698733566,0.439063977267521,2.19883173397957));
#75685=CARTESIAN_POINT('Ctrl Pts',(-1.91951206409704,0.371863522385234,
2.20274264118657));
#75686=CARTESIAN_POINT('Ctrl Pts',(-1.93017684355697,0.304192952903994,
2.20665354839357));
#75687=CARTESIAN_POINT('Ctrl Pts',(-1.94086012054759,0.236405012178415,
2.21057123887503));
#75688=CARTESIAN_POINT('Ctrl Pts',(-1.94795355107944,0.168145818399277,
2.21448892935649));
#75689=CARTESIAN_POINT('Ctrl Pts',(-1.95144846778218,0.0998242334835162,
2.21840661983795));
#75690=CARTESIAN_POINT('Ctrl Pts',(-1.9531504750421,0.0665519573676903,
2.22031451585055));
#75691=CARTESIAN_POINT('Ctrl Pts',(-1.953999832782,0.0332648680386802,2.22222241186316));
#75692=CARTESIAN_POINT('Ctrl Pts',(-1.9539999999753,9.82394477163224E-6,
2.22413030787576));
#75693=CARTESIAN_POINT('',(-1.95399926641343,0.00169317918818195,2.92413028879048));
#75694=CARTESIAN_POINT('Ctrl Pts',(-1.95399999997531,9.82336241918865E-6,
2.22413030790917));
#75695=CARTESIAN_POINT('Ctrl Pts',(-1.95400034322258,-0.0682667145672286,
2.22804744403147));
#75696=CARTESIAN_POINT('Ctrl Pts',(-1.95041780549391,-0.136679161354171,
2.23196458015376));
#75697=CARTESIAN_POINT('Ctrl Pts',(-1.9432356042465,-0.204820375911999,
2.23588171627606));
#75698=CARTESIAN_POINT('Ctrl Pts',(-1.93606423675079,-0.272858805129577,
2.23979294372515));
#75699=CARTESIAN_POINT('Ctrl Pts',(-1.92530403292758,-0.340626328588442,
2.24370417117423));
#75700=CARTESIAN_POINT('Ctrl Pts',(-1.91099022196807,-0.407716042782765,
2.24761539862331));
#75701=CARTESIAN_POINT('Ctrl Pts',(-1.89669327592396,-0.474726710079095,
2.25152201775947));
#75702=CARTESIAN_POINT('Ctrl Pts',(-1.87885114017296,-0.541060675100519,
2.25542863689563));
#75703=CARTESIAN_POINT('Ctrl Pts',(-1.85755059422337,-0.606318224944963,
2.25933525603178));
#75704=CARTESIAN_POINT('Ctrl Pts',(-1.83626342508014,-0.671534792853558,
2.26323942179948));
#75705=CARTESIAN_POINT('Ctrl Pts',(-1.81152230636717,-0.735675819692555,
2.26714358756717));
#75706=CARTESIAN_POINT('Ctrl Pts',(-1.78346425066129,-0.798355351089442,
2.27104775333486));
#75707=CARTESIAN_POINT('Ctrl Pts',(-1.75541417838837,-0.861017048113155,
2.27495080823992));
#75708=CARTESIAN_POINT('Ctrl Pts',(-1.72404924363516,-0.92221762619541,
2.27885386314499));
#75709=CARTESIAN_POINT('Ctrl Pts',(-1.68955443659765,-0.981591465821289,
2.28275691805005));
#75710=CARTESIAN_POINT('Ctrl Pts',(-1.65505759687093,-1.04096880419303,
2.28666020295198));
#75711=CARTESIAN_POINT('Ctrl Pts',(-1.61743076815678,-1.09851876612914,
2.29056348785391));
#75712=CARTESIAN_POINT('Ctrl Pts',(-1.57690378390483,-1.15390227329121,
2.29446677275583));
#75713=CARTESIAN_POINT('Ctrl Pts',(-1.53633356553099,-1.20934486349002,
2.29837422167585));
#75714=CARTESIAN_POINT('Ctrl Pts',(-1.49285730840736,-1.26261598859572,
2.30228167059586));
#75715=CARTESIAN_POINT('Ctrl Pts',(-1.44674628823888,-1.31340822955661,
2.30618911951587));
#75716=CARTESIAN_POINT('Ctrl Pts',(-1.40060764199253,-1.36423090121278,
2.31009890947036));
#75717=CARTESIAN_POINT('Ctrl Pts',(-1.35183144081067,-1.41257138658037,
2.31400869942485));
#75718=CARTESIAN_POINT('Ctrl Pts',(-1.30072510863043,-1.45815986495938,
2.31791848937934));
#75719=CARTESIAN_POINT('Ctrl Pts',(-1.24953033896871,-1.50382723239265,
2.32183504507033));
#75720=CARTESIAN_POINT('Ctrl Pts',(-1.19599777456993,-1.54673278059923,
2.32575160076131));
#75721=CARTESIAN_POINT('Ctrl Pts',(-1.14046639934664,-1.58664816262501,
2.3296681564523));
#75722=CARTESIAN_POINT('Ctrl Pts',(-1.11412315929172,-1.6055834129472,2.33152611092112));
#75723=CARTESIAN_POINT('Ctrl Pts',(-1.08733050185621,-1.62384640243154,
2.33338406538995));
#75724=CARTESIAN_POINT('Ctrl Pts',(-1.06012654717021,-1.64141637130406,
2.33524201985877));
#75725=CARTESIAN_POINT('Ctrl Pts',(-1.00276386025002,-1.67846468414182,
2.33915973188768));
#75726=CARTESIAN_POINT('Ctrl Pts',(-0.943342738039523,-1.71257601910822,
2.34307744391659));
#75727=CARTESIAN_POINT('Ctrl Pts',(-0.882196201650275,-1.74351537469385,
2.34699515594549));
#75728=CARTESIAN_POINT('Ctrl Pts',(-0.821141893843108,-1.77440806381127,
2.35090695880853));
#75729=CARTESIAN_POINT('Ctrl Pts',(-0.758367772261743,-1.80213804838734,
2.35481876167158));
#75730=CARTESIAN_POINT('Ctrl Pts',(-0.694234870682419,-1.8265141511438,
2.35873056453462));
#75731=CARTESIAN_POINT('Ctrl Pts',(-0.630177556586263,-1.85086152405628,
2.36263775691964));
#75732=CARTESIAN_POINT('Ctrl Pts',(-0.564765100721728,-1.87186269165573,
2.36654494930467));
#75733=CARTESIAN_POINT('Ctrl Pts',(-0.4983804597485,-1.88937368388069,2.37045214168969));
#75734=CARTESIAN_POINT('Ctrl Pts',(-0.432037541593535,-1.90687367042819,
2.3743568784001));
#75735=CARTESIAN_POINT('Ctrl Pts',(-0.364724125039669,-1.92088770770785,
2.37826161511051));
#75736=CARTESIAN_POINT('Ctrl Pts',(-0.296838859841856,-1.93132148833067,
2.38216635182091));
#75737=CARTESIAN_POINT('Ctrl Pts',(-0.228972962964415,-1.94175229209533,
2.38606997447231));
#75738=CARTESIAN_POINT('Ctrl Pts',(-0.160536027388258,-1.94860479227721,
2.3899735971237));
#75739=CARTESIAN_POINT('Ctrl Pts',(-0.0919356501021985,-1.95183601673918,
2.3938772197751));
#75740=CARTESIAN_POINT('Ctrl Pts',(-0.0233313028251302,-1.95506742819622,
2.39778106833409));
#75741=CARTESIAN_POINT('Ctrl Pts',(0.0454360133624638,-1.95467712726879,
2.40168491689309));
#75742=CARTESIAN_POINT('Ctrl Pts',(0.113956666023218,-1.95067421120721,
2.40558876545209));
#75743=CARTESIAN_POINT('Ctrl Pts',(0.182550386467686,-1.94666702659018,
2.40949677692476));
#75744=CARTESIAN_POINT('Ctrl Pts',(0.250896426330908,-1.93903956738392,
2.41340478839744));
#75745=CARTESIAN_POINT('Ctrl Pts',(0.31858925877276,-1.92785292078899,2.41731279987011));
#75746=CARTESIAN_POINT('Ctrl Pts',(0.38632254860938,-1.9166595883669,2.42122314701049));
#75747=CARTESIAN_POINT('Ctrl Pts',(0.453401373476329,-1.90190294079295,
2.42513349415088));
#75748=CARTESIAN_POINT('Ctrl Pts',(0.519432172520297,-1.88369483148169,
2.42904384129126));
#75749=CARTESIAN_POINT('Ctrl Pts',(0.585577367504033,-1.86545517728826,
2.43296096296478));
#75750=CARTESIAN_POINT('Ctrl Pts',(0.650670446306053,-1.8437522825183,2.4368780846383));
#75751=CARTESIAN_POINT('Ctrl Pts',(0.71433555268926,-1.81874701873684,2.44079520631182));
#75752=CARTESIAN_POINT('Ctrl Pts',(0.74493900811613,-1.80672713030742,2.44267814447602));
#75753=CARTESIAN_POINT('Ctrl Pts',(0.775212841443383,-1.79394487209788,
2.44456108264023));
#75754=CARTESIAN_POINT('Ctrl Pts',(0.805117385821651,-1.78042185873116,
2.44644402080443));
#75755=CARTESIAN_POINT('Ctrl Pts',(0.867337906277968,-1.75228536819742,
2.45036173281107));
#75756=CARTESIAN_POINT('Ctrl Pts',(0.928205375409723,-1.72082739507311,
2.45427944481772));
#75757=CARTESIAN_POINT('Ctrl Pts',(0.987341830831477,-1.68620049492649,
2.45819715682436));
#75758=CARTESIAN_POINT('Ctrl Pts',(1.04638908950262,-1.65162582325645,2.46210895966417));
#75759=CARTESIAN_POINT('Ctrl Pts',(1.10371009503318,-1.61389195719953,2.46602076250398));
#75760=CARTESIAN_POINT('Ctrl Pts',(1.15894853894812,-1.57319874271181,2.4699325653438));
#75761=CARTESIAN_POINT('Ctrl Pts',(1.21412187843032,-1.53255348954338,2.47383975770426));
#75762=CARTESIAN_POINT('Ctrl Pts',(1.26721713674452,-1.4889561053604,2.47774695006472));
#75763=CARTESIAN_POINT('Ctrl Pts',(1.31790580243201,-1.44265044134608,2.48165414242519));
#75764=CARTESIAN_POINT('Ctrl Pts',(1.36856261022785,-1.39637388050121,2.48555887911022));
#75765=CARTESIAN_POINT('Ctrl Pts',(1.41681546334458,-1.34739274741358,2.48946361579526));
#75766=CARTESIAN_POINT('Ctrl Pts',(1.46236908675021,-1.29599099306954,2.49336835248029));
#75767=CARTESIAN_POINT('Ctrl Pts',(1.50790971325896,-1.24460390415165,2.49727197510554));
#75768=CARTESIAN_POINT('Ctrl Pts',(1.55075231267688,-1.1907979330058,2.50117559773079));
#75769=CARTESIAN_POINT('Ctrl Pts',(1.59063990746642,-1.13489236704421,2.50507922035604));
#75770=CARTESIAN_POINT('Ctrl Pts',(1.63052981059415,-1.07898356576715,2.50898306888814));
#75771=CARTESIAN_POINT('Ctrl Pts',(1.66746408590047,-1.02097533043663,2.51288691742025));
#75772=CARTESIAN_POINT('Ctrl Pts',(1.70122841558543,-0.961216873553878,
2.51679076595235));
#75773=CARTESIAN_POINT('Ctrl Pts',(1.73502875024273,-0.90139469256917,2.5206987773972));
#75774=CARTESIAN_POINT('Ctrl Pts',(1.7656521506494,-0.839818994476754,2.52460678884205));
#75775=CARTESIAN_POINT('Ctrl Pts',(1.79293021957056,-0.776863712468706,
2.5285148002869));
#75776=CARTESIAN_POINT('Ctrl Pts',(1.82022459153739,-0.713870804526047,
2.53242514739889));
#75777=CARTESIAN_POINT('Ctrl Pts',(1.84416948134966,-0.649497132924647,
2.53633549451087));
#75778=CARTESIAN_POINT('Ctrl Pts',(1.86464564306295,-0.584134082044838,
2.54024584162286));
#75779=CARTESIAN_POINT('Ctrl Pts',(1.88515727897323,-0.51865779208363,2.54416296326738));
#75780=CARTESIAN_POINT('Ctrl Pts',(1.90218807064011,-0.452189178170086,
2.5480800849119));
#75781=CARTESIAN_POINT('Ctrl Pts',(1.91566956375596,-0.385131305529756,
2.55199720655642));
#75782=CARTESIAN_POINT('Ctrl Pts',(1.92215004186012,-0.352896962373318,
2.55388014495431));
#75783=CARTESIAN_POINT('Ctrl Pts',(1.92781116286614,-0.320526557816258,
2.55576308335219));
#75784=CARTESIAN_POINT('Ctrl Pts',(1.93264959926769,-0.288065142720263,
2.55764602175008));
#75785=CARTESIAN_POINT('Ctrl Pts',(1.94271663104477,-0.220524708129425,
2.56156373381916));
#75786=CARTESIAN_POINT('Ctrl Pts',(1.94925889654111,-0.152321689154477,
2.56548144588824));
#75787=CARTESIAN_POINT('Ctrl Pts',(1.95219981089288,-0.0838564150783238,
2.56939915795732));
#75788=CARTESIAN_POINT('Ctrl Pts',(1.95513628940303,-0.0154944085837447,
2.57331096086068));
#75789=CARTESIAN_POINT('Ctrl Pts',(1.95448217630384,0.0531285803865306,
2.57722276376404));
#75790=CARTESIAN_POINT('Ctrl Pts',(1.95021236620661,0.121604797170189,2.5811345666674));
#75791=CARTESIAN_POINT('Ctrl Pts',(1.94594758853717,0.190000307410026,2.58504175909274));
#75792=CARTESIAN_POINT('Ctrl Pts',(1.93807560765553,0.2582489003026,2.58894895151807));
#75793=CARTESIAN_POINT('Ctrl Pts',(1.92662336528264,0.325942338991097,2.59285614394341));
#75794=CARTESIAN_POINT('Ctrl Pts',(1.91517832065641,0.393593232280572,2.59676088069411));
#75795=CARTESIAN_POINT('Ctrl Pts',(1.90015756004841,0.460689179480282,2.6006656174448));
#75796=CARTESIAN_POINT('Ctrl Pts',(1.88163973730727,0.526828149386717,2.6045703541955));
#75797=CARTESIAN_POINT('Ctrl Pts',(1.86312719787978,0.592948249206345,2.60847397688709));
#75798=CARTESIAN_POINT('Ctrl Pts',(1.84111970956889,0.658111440185297,2.61237759957869));
#75799=CARTESIAN_POINT('Ctrl Pts',(1.8157463772773,0.721928731527132,2.61628122227028));
#75800=CARTESIAN_POINT('Ctrl Pts',(1.79037157659979,0.785749716054033,2.62018507086932));
#75801=CARTESIAN_POINT('Ctrl Pts',(1.76163072937231,0.8482241900587,2.62408891946835));
#75802=CARTESIAN_POINT('Ctrl Pts',(1.72970120722305,0.90898280166961,2.62799276806739));
#75803=CARTESIAN_POINT('Ctrl Pts',(1.69773763666605,0.969806203914456,2.63190077957961));
#75804=CARTESIAN_POINT('Ctrl Pts',(1.66257883451267,1.02890965577615,2.63580879109183));
#75805=CARTESIAN_POINT('Ctrl Pts',(1.62444783189962,1.08594900498901,2.63971680260406));
#75806=CARTESIAN_POINT('Ctrl Pts',(1.5862940398596,1.14302244441704,2.64362714978377));
#75807=CARTESIAN_POINT('Ctrl Pts',(1.54516480673797,1.19802893194669,2.64753749696348));
#75808=CARTESIAN_POINT('Ctrl Pts',(1.50132446399708,1.2506561692983,2.65144784414318));
#75809=CARTESIAN_POINT('Ctrl Pts',(1.45740816947832,1.3033745813988,2.65536496585525));
#75810=CARTESIAN_POINT('Ctrl Pts',(1.41077172517221,1.35370515568967,2.65928208756731));
#75811=CARTESIAN_POINT('Ctrl Pts',(1.36171680191587,1.40137195325867,2.66319920927938));
#75812=CARTESIAN_POINT('Ctrl Pts',(1.33813638335019,1.42428510781584,2.66508214708483));
#75813=CARTESIAN_POINT('Ctrl Pts',(1.31399763238744,1.44658334545152,2.66696508489029));
#75814=CARTESIAN_POINT('Ctrl Pts',(1.28933660976701,1.46823945823374,2.66884802269575));
#75815=CARTESIAN_POINT('Ctrl Pts',(1.23802594780508,1.51329799045605,2.67276573473544));
#75816=CARTESIAN_POINT('Ctrl Pts',(1.18424847215195,1.55575309701275,2.67668344677512));
#75817=CARTESIAN_POINT('Ctrl Pts',(1.12829914852506,1.59532348802292,2.68060115881481));
#75818=CARTESIAN_POINT('Ctrl Pts',(1.07243421441997,1.63483419419405,2.68451296168842));
#75819=CARTESIAN_POINT('Ctrl Pts',(1.01440433211291,1.67146853828116,2.68842476456203));
#75820=CARTESIAN_POINT('Ctrl Pts',(0.954538602825627,1.70498447374623,2.69233656743563));
#75821=CARTESIAN_POINT('Ctrl Pts',(0.89474343170841,1.73846090709376,2.69624375983083));
#75822=CARTESIAN_POINT('Ctrl Pts',(0.833117138063596,1.76882599192038,2.70015095222602));
#75823=CARTESIAN_POINT('Ctrl Pts',(0.770017430669509,1.79588116434945,2.70405814462122));
#75824=CARTESIAN_POINT('Ctrl Pts',(0.706957381513432,1.82291933257181,2.70796288134154));
#75825=CARTESIAN_POINT('Ctrl Pts',(0.642426206728058,1.84665152152243,2.71186761806186));
#75826=CARTESIAN_POINT('Ctrl Pts',(0.576804420210808,1.86692599232676,2.71577235478218));
#75827=CARTESIAN_POINT('Ctrl Pts',(0.511201356225879,1.88719467862789,2.71967597744324));
#75828=CARTESIAN_POINT('Ctrl Pts',(0.44450876806408,1.90400745999413,2.72357960010429));
#75829=CARTESIAN_POINT('Ctrl Pts',(0.377123547021885,1.91726206614579,2.72748322276534));
#75830=CARTESIAN_POINT('Ctrl Pts',(0.309734426316387,1.93051743935736,2.73138707133371));
#75831=CARTESIAN_POINT('Ctrl Pts',(0.241653076395766,1.94021413608686,2.73529091990207));
#75832=CARTESIAN_POINT('Ctrl Pts',(0.173286036508639,1.94630109426859,2.73919476847044));
#75833=CARTESIAN_POINT('Ctrl Pts',(0.104846092653275,1.9523945433472,2.74310277995199));
#75834=CARTESIAN_POINT('Ctrl Pts',(0.0361203418520083,1.95487052808008,
2.74701079143354));
#75835=CARTESIAN_POINT('Ctrl Pts',(-0.0324811150189426,1.95373001644729,
2.7509188029151));
#75836=CARTESIAN_POINT('Ctrl Pts',(-0.101123572329707,1.95258882317477,
2.75482915006409));
#75837=CARTESIAN_POINT('Ctrl Pts',(-0.169641096972235,1.94782686600023,
2.75873949721309));
#75838=CARTESIAN_POINT('Ctrl Pts',(-0.237627981308397,1.9394970849422,2.76264984436209));
#75839=CARTESIAN_POINT('Ctrl Pts',(-0.305732650421314,1.93115287284484,
2.76656696604371));
#75840=CARTESIAN_POINT('Ctrl Pts',(-0.373304360108464,1.9192285855885,2.77048408772534));
#75841=CARTESIAN_POINT('Ctrl Pts',(-0.43994772888382,1.90382824746613,2.77440120940696));
#75842=CARTESIAN_POINT('Ctrl Pts',(-0.471982816614628,1.89642539266002,
2.77628414748511));
#75843=CARTESIAN_POINT('Ctrl Pts',(-0.50380362454953,1.88822007760216,2.77816708556325));
#75844=CARTESIAN_POINT('Ctrl Pts',(-0.535367745366362,1.87922786729586,
2.7800500236414));
#75845=CARTESIAN_POINT('Ctrl Pts',(-0.601041246564359,1.86051833511056,
2.7839677356806));
#75846=CARTESIAN_POINT('Ctrl Pts',(-0.665863320672553,1.83832483006667,
2.7878854477198));
#75847=CARTESIAN_POINT('Ctrl Pts',(-0.729437722121871,1.81274284153756,
2.791803159759));
#75848=CARTESIAN_POINT('Ctrl Pts',(-0.792916232985298,1.78719943885136,
2.79571496263202));
#75849=CARTESIAN_POINT('Ctrl Pts',(-0.855150353294405,1.75827787813295,
2.79962676550505));
#75850=CARTESIAN_POINT('Ctrl Pts',(-0.915758323573785,1.72612360299178,
2.80353856837807));
#75851=CARTESIAN_POINT('Ctrl Pts',(-0.976294860870307,1.69400722510694,
2.80744576077253));
#75852=CARTESIAN_POINT('Ctrl Pts',(-1.03520862193264,1.65866592914393,2.81135295316699));
#75853=CARTESIAN_POINT('Ctrl Pts',(-1.09213889176975,1.62029276400407,2.81526014556146));
#75854=CARTESIAN_POINT('Ctrl Pts',(-1.14903338086615,1.58194371644306,2.81916488228096));
#75855=CARTESIAN_POINT('Ctrl Pts',(-1.20394644456238,1.54056685400413,2.82306961900046));
#75856=CARTESIAN_POINT('Ctrl Pts',(-1.25654436559627,1.49639976519921,2.82697435571997));
#75857=CARTESIAN_POINT('Ctrl Pts',(-1.3091272799316,1.45224527769441,2.8308779783801));
#75858=CARTESIAN_POINT('Ctrl Pts',(-1.35939598624797,1.40530246038736,2.83478160104023));
#75859=CARTESIAN_POINT('Ctrl Pts',(-1.40704946979724,1.35584947156508,2.83868522370036));
#75860=CARTESIAN_POINT('Ctrl Pts',(-1.45470571110967,1.30639362084016,2.84258907226773));
#75861=CARTESIAN_POINT('Ctrl Pts',(-1.49974608962532,1.25442766625078,2.8464929208351));
#75862=CARTESIAN_POINT('Ctrl Pts',(-1.54190740162807,1.20026562260384,2.85039676940246));
#75863=CARTESIAN_POINT('Ctrl Pts',(-1.5841136728226,1.14604582264923,2.85430478088289));
#75864=CARTESIAN_POINT('Ctrl Pts',(-1.62343444760295,1.08962564901291,2.85821279236332));
#75865=CARTESIAN_POINT('Ctrl Pts',(-1.65964832194906,1.03135030297744,2.86212080384375));
#75866=CARTESIAN_POINT('Ctrl Pts',(-1.69588383992779,0.973040128020652,
2.86603115099155));
#75867=CARTESIAN_POINT('Ctrl Pts',(-1.7290085246365,0.912873005093201,2.86994149813935));
#75868=CARTESIAN_POINT('Ctrl Pts',(-1.75884703342753,0.851218604709267,
2.87385184528715));
#75869=CARTESIAN_POINT('Ctrl Pts',(-1.78873723633691,0.789457390345678,
2.87776896696748));
#75870=CARTESIAN_POINT('Ctrl Pts',(-1.8153297098807,0.726204209186377,2.8816860886478));
#75871=CARTESIAN_POINT('Ctrl Pts',(-1.83849764145948,0.661847733506674,
2.88560321032813));
#75872=CARTESIAN_POINT('Ctrl Pts',(-1.84963433424332,0.630911942115114,
2.88748614841444));
#75873=CARTESIAN_POINT('Ctrl Pts',(-1.85998047482828,0.599721424360237,
2.88936908650075));
#75874=CARTESIAN_POINT('Ctrl Pts',(-1.86952616624135,0.568320256315866,
2.89125202458706));
#75875=CARTESIAN_POINT('Ctrl Pts',(-1.89385394953268,0.48829244290548,2.89605080842916));
#75876=CARTESIAN_POINT('Ctrl Pts',(-1.91305798426404,0.406639111708275,
2.90084959227126));
#75877=CARTESIAN_POINT('Ctrl Pts',(-1.92695885244266,0.323953053686572,
2.90564837611336));
#75878=CARTESIAN_POINT('Ctrl Pts',(-1.94065975646689,0.242456435594826,
2.91037812939271));
#75879=CARTESIAN_POINT('Ctrl Pts',(-1.94920892492174,0.159956562486602,
2.91510788267205));
#75880=CARTESIAN_POINT('Ctrl Pts',(-1.95248061093239,0.0770419621574774,
2.9198376359514));
#75881=CARTESIAN_POINT('Ctrl Pts',(-1.9534703885813,0.0519579480110874,
2.9212685202311));
#75882=CARTESIAN_POINT('Ctrl Pts',(-1.9539774795513,0.0268361250322783,
2.92269940451079));
#75883=CARTESIAN_POINT('Ctrl Pts',(-1.95399926641343,0.00169317918818195,
2.92413028879048));
#75884=CARTESIAN_POINT('',(-1.95389457769654,-0.000928448540882686,3.62413035263971));
#75885=CARTESIAN_POINT('Ctrl Pts',(-1.95280791655641,0.00169181170498602,
2.92413030787576));
#75886=CARTESIAN_POINT('Ctrl Pts',(-1.94902086284632,-0.456790150037774,
2.95023821376141));
#75887=CARTESIAN_POINT('Ctrl Pts',(-1.55897155685892,-1.57201467073545,
3.01341345329561));
#75888=CARTESIAN_POINT('Ctrl Pts',(0.300327974436277,-2.29036964049045,
3.11365602647836));
#75889=CARTESIAN_POINT('Ctrl Pts',(2.08771894852419,-0.988645322604532,
3.22485802742402));
#75890=CARTESIAN_POINT('Ctrl Pts',(1.96217801545985,1.21895341072494,3.33606002836968));
#75891=CARTESIAN_POINT('Ctrl Pts',(0.0387356283802723,2.30965138778674,
3.44726202931533));
#75892=CARTESIAN_POINT('Ctrl Pts',(-1.65281353681269,1.42405341209699,3.54328545581736));
#75893=CARTESIAN_POINT('Ctrl Pts',(-1.94956657085447,0.384252923937107,
3.60224154867084));
#75894=CARTESIAN_POINT('Ctrl Pts',(-1.95121488712599,-0.000926387452031019,
3.62413030787576));
#75895=CARTESIAN_POINT('',(-1.95399960711636,-0.0012391081865255,4.32413030787576));
#75896=CARTESIAN_POINT('Ctrl Pts',(-1.95399977938408,-0.000928529456951041,
3.62413035439709));
#75897=CARTESIAN_POINT('Ctrl Pts',(-1.95396384512653,-0.0765486735560237,
3.62842153969855));
#75898=CARTESIAN_POINT('Ctrl Pts',(-1.94953396892489,-0.152021773335561,
3.63271272500001));
#75899=CARTESIAN_POINT('Ctrl Pts',(-1.94078603975606,-0.22686019458684,
3.63700391030146));
#75900=CARTESIAN_POINT('Ctrl Pts',(-1.93200861573635,-0.301950943907116,
3.64130956392658));
#75901=CARTESIAN_POINT('Ctrl Pts',(-1.91888410869524,-0.376402426202599,
3.6456152175517));
#75902=CARTESIAN_POINT('Ctrl Pts',(-1.90153921339991,-0.449738390514354,
3.64992087117681));
#75903=CARTESIAN_POINT('Ctrl Pts',(-1.88411335654505,-0.523416668454385,
3.6542466224979));
#75904=CARTESIAN_POINT('Ctrl Pts',(-1.86242776661361,-0.595968697856712,
3.65857237381899));
#75905=CARTESIAN_POINT('Ctrl Pts',(-1.83665921822363,-0.666932467431417,
3.66289812514008));
#75906=CARTESIAN_POINT('Ctrl Pts',(-1.82322038783094,-0.703941539456255,
3.66515409382894));
#75907=CARTESIAN_POINT('Ctrl Pts',(-1.80867184087001,-0.740519002767186,
3.66741006251779));
#75908=CARTESIAN_POINT('Ctrl Pts',(-1.79304361189968,-0.77660196099787,
3.66966603120665));
#75909=CARTESIAN_POINT('Ctrl Pts',(-1.76590365150813,-0.839263575378505,
3.67358374325044));
#75910=CARTESIAN_POINT('Ctrl Pts',(-1.73542103874449,-0.900625316628146,
3.67750145529423));
#75911=CARTESIAN_POINT('Ctrl Pts',(-1.70174227804019,-0.960306835928284,
3.68141916733802));
#75912=CARTESIAN_POINT('Ctrl Pts',(-1.6681143157071,-1.01989833635871,3.68533097021571));
#75913=CARTESIAN_POINT('Ctrl Pts',(-1.63130001279988,-1.07781421948387,
3.68924277309341));
#75914=CARTESIAN_POINT('Ctrl Pts',(-1.59149350367943,-1.13369503295471,
3.69315457597111));
#75915=CARTESIAN_POINT('Ctrl Pts',(-1.55173391079101,-1.18950998490518,
3.69706176837038));
#75916=CARTESIAN_POINT('Ctrl Pts',(-1.50898939968645,-1.24329423189826,
3.70096896076966));
#75917=CARTESIAN_POINT('Ctrl Pts',(-1.46349854794866,-1.29471541280398,
3.70487615316893));
#75918=CARTESIAN_POINT('Ctrl Pts',(-1.41803628726312,-1.34610427543879,
3.70878088989332));
#75919=CARTESIAN_POINT('Ctrl Pts',(-1.36983143515774,-1.39513265042968,
3.71268562661771));
#75920=CARTESIAN_POINT('Ctrl Pts',(-1.31916319431565,-1.4415007689082,3.7165903633421));
#75921=CARTESIAN_POINT('Ctrl Pts',(-1.26850940961461,-1.48785565811232,
3.72049398600719));
#75922=CARTESIAN_POINT('Ctrl Pts',(-1.21539399417526,-1.53155146551823,
3.72439760867228));
#75923=CARTESIAN_POINT('Ctrl Pts',(-1.16013209377737,-1.57232615095843,
3.72830123133736));
#75924=CARTESIAN_POINT('Ctrl Pts',(-1.10486699530747,-1.61310319607824,
3.73220507990975));
#75925=CARTESIAN_POINT('Ctrl Pts',(-1.04745556267513,-1.6509584935525,3.73610892848213));
#75926=CARTESIAN_POINT('Ctrl Pts',(-0.988243543724006,-1.68567217995903,
3.74001277705452));
#75927=CARTESIAN_POINT('Ctrl Pts',(-0.928968383366187,-1.72042288369802,
3.74392078854002));
#75928=CARTESIAN_POINT('Ctrl Pts',(-0.867889230025287,-1.75202504122151,
3.74782880002552));
#75929=CARTESIAN_POINT('Ctrl Pts',(-0.805377281911555,-1.78030430931927,
3.75173681151102));
#75930=CARTESIAN_POINT('Ctrl Pts',(-0.742827972822654,-1.80860047884251,
3.75564715866393));
#75931=CARTESIAN_POINT('Ctrl Pts',(-0.678844623129316,-1.83356962762598,
3.75955750581684));
#75932=CARTESIAN_POINT('Ctrl Pts',(-0.613816664389189,-1.8550862789957,
3.76346785296976));
#75933=CARTESIAN_POINT('Ctrl Pts',(-0.548676047103823,-1.87664020717203,
3.7673849746552));
#75934=CARTESIAN_POINT('Ctrl Pts',(-0.48248768311705,-1.89472957032568,
3.77130209634063));
#75935=CARTESIAN_POINT('Ctrl Pts',(-0.415653493903269,-1.90927949054244,
3.77521921802607));
#75936=CARTESIAN_POINT('Ctrl Pts',(-0.383526680521459,-1.91627355416501,
3.77710215606815));
#75937=CARTESIAN_POINT('Ctrl Pts',(-0.351250747401493,-1.9224505366792,
3.77898509411023));
#75938=CARTESIAN_POINT('Ctrl Pts',(-0.318870686539781,-1.92780639205955,
3.7808680321523));
#75939=CARTESIAN_POINT('Ctrl Pts',(-0.251499508315918,-1.93894998715381,
3.78478574419611));
#75940=CARTESIAN_POINT('Ctrl Pts',(-0.183409580024177,-1.94657983874897,
3.78870345623992));
#75941=CARTESIAN_POINT('Ctrl Pts',(-0.114999957780594,-1.95061298306724,
3.79262116828373));
#75942=CARTESIAN_POINT('Ctrl Pts',(-0.0466935191847929,-1.95464004411053,
3.79653297116146));
#75943=CARTESIAN_POINT('Ctrl Pts',(0.021931169193035,-1.95508113573335,
3.80044477403918));
#75944=CARTESIAN_POINT('Ctrl Pts',(0.0904668052660995,-1.95190464857916,
3.80435657691691));
#75945=CARTESIAN_POINT('Ctrl Pts',(0.158921664755669,-1.94873190525511,
3.80826376931621));
#75946=CARTESIAN_POINT('Ctrl Pts',(0.22728719125003,-1.94195007354239,3.8121709617155));
#75947=CARTESIAN_POINT('Ctrl Pts',(0.29515476993388,-1.93157957687103,3.8160781541148));
#75948=CARTESIAN_POINT('Ctrl Pts',(0.362979693767063,-1.92121559806867,
3.81998289083921));
#75949=CARTESIAN_POINT('Ctrl Pts',(0.430306805337967,-1.90726750255992,
3.82388762756362));
#75950=CARTESIAN_POINT('Ctrl Pts',(0.49673286944478,-1.88980751835026,3.82779236428803));
#75951=CARTESIAN_POINT('Ctrl Pts',(0.563139981550571,-1.87235251564361,
3.83169598695315));
#75952=CARTESIAN_POINT('Ctrl Pts',(0.628646080911884,-1.85138773830943,
3.83559960961826));
#75953=CARTESIAN_POINT('Ctrl Pts',(0.692860165948776,-1.82703606708829,
3.83950323228338));
#75954=CARTESIAN_POINT('Ctrl Pts',(0.757077967131214,-1.80268298660694,
3.84340708085578));
#75955=CARTESIAN_POINT('Ctrl Pts',(0.820003146414706,-1.77494279994659,
3.84731092942819));
#75956=CARTESIAN_POINT('Ctrl Pts',(0.88126356837749,-1.74398696183503,3.85121477800059));
#75957=CARTESIAN_POINT('Ctrl Pts',(0.942589316084718,-1.71299811361507,
3.85512278948612));
#75958=CARTESIAN_POINT('Ctrl Pts',(1.00224632363735,-1.67878699286616,3.85903080097164));
#75959=CARTESIAN_POINT('Ctrl Pts',(1.05988692335203,-1.64157111015861,3.86293881245716));
#75960=CARTESIAN_POINT('Ctrl Pts',(1.11756197262524,-1.60433298495644,3.8668491596101));
#75961=CARTESIAN_POINT('Ctrl Pts',(1.17321781688942,-1.56408681211669,3.87075950676304));
#75962=CARTESIAN_POINT('Ctrl Pts',(1.22653797929859,-1.5210919056185,3.87466985391597));
#75963=CARTESIAN_POINT('Ctrl Pts',(1.27995051692673,-1.4780225120272,3.87858697560143));
#75964=CARTESIAN_POINT('Ctrl Pts',(1.33101893042946,-1.43219520871446,3.88250409728689));
#75965=CARTESIAN_POINT('Ctrl Pts',(1.3794625018168,-1.38390722452097,3.88642121897235));
#75966=CARTESIAN_POINT('Ctrl Pts',(1.4027490501484,-1.36069546606563,3.88830415701422));
#75967=CARTESIAN_POINT('Ctrl Pts',(1.42542966987338,-1.33691563300483,3.89018709505609));
#75968=CARTESIAN_POINT('Ctrl Pts',(1.44747658103796,-1.31260334730133,3.89207003309796));
#75969=CARTESIAN_POINT('Ctrl Pts',(1.49334821753265,-1.26201828693525,3.89598774514179));
#75970=CARTESIAN_POINT('Ctrl Pts',(1.53665612658425,-1.20892518019095,3.89990545718561));
#75971=CARTESIAN_POINT('Ctrl Pts',(1.57711434691632,-1.15361446625409,3.90382316922944));
#75972=CARTESIAN_POINT('Ctrl Pts',(1.61751154327807,-1.09838717861076,3.90773497210718));
#75973=CARTESIAN_POINT('Ctrl Pts',(1.6550672932089,-1.0409493159769,3.91164677498492));
#75974=CARTESIAN_POINT('Ctrl Pts',(1.68953432902574,-0.981626074961098,
3.91555857786266));
#75975=CARTESIAN_POINT('Ctrl Pts',(1.72396074175136,-0.922372752735072,
3.91946577026197));
#75976=CARTESIAN_POINT('Ctrl Pts',(1.75530542416981,-0.861238888646867,
3.92337296266128));
#75977=CARTESIAN_POINT('Ctrl Pts',(1.78336412918788,-0.798578977137478,
3.9272801550606));
#75978=CARTESIAN_POINT('Ctrl Pts',(1.81140519927783,-0.735958447453981,
3.93118489178502));
#75979=CARTESIAN_POINT('Ctrl Pts',(1.83616418807734,-0.671814220944769,
3.93508962850945));
#75980=CARTESIAN_POINT('Ctrl Pts',(1.85748330359643,-0.606524341523494,
3.93899436523388));
#75981=CARTESIAN_POINT('Ctrl Pts',(1.87879633656486,-0.541253089938719,
3.94289798789901));
#75982=CARTESIAN_POINT('Ctrl Pts',(1.89667129187766,-0.474837301794581,
3.94680161056414));
#75983=CARTESIAN_POINT('Ctrl Pts',(1.91099957848101,-0.40767218576375,3.95070523322927));
#75984=CARTESIAN_POINT('Ctrl Pts',(1.92532869427938,-0.340503182807664,
3.9546090818017));
#75985=CARTESIAN_POINT('Ctrl Pts',(1.93611063372278,-0.27258524757927,3.95851293037412));
#75986=CARTESIAN_POINT('Ctrl Pts',(1.94328785348326,-0.204324052682056,
3.96241677894654));
#75987=CARTESIAN_POINT('Ctrl Pts',(1.95047272675328,-0.135990066686953,
3.96632479043208));
#75988=CARTESIAN_POINT('Ctrl Pts',(1.95404515739319,-0.0673125807662448,
3.97023280191762));
#75989=CARTESIAN_POINT('Ctrl Pts',(1.95399956865673,0.00129834098001337,
3.97414081340316));
#75990=CARTESIAN_POINT('Ctrl Pts',(1.95395395267365,0.0699502688222659,
3.97805116055612));
#75991=CARTESIAN_POINT('Ctrl Pts',(1.95028604012803,0.138535061937052,3.98196150770907));
#75992=CARTESIAN_POINT('Ctrl Pts',(1.94304228980324,0.206646219506102,3.98587185486202));
#75993=CARTESIAN_POINT('Ctrl Pts',(1.93578598994762,0.274875377148873,3.9897889765475));
#75994=CARTESIAN_POINT('Ctrl Pts',(1.92494156558795,0.342628775934079,3.99370609823298));
#75995=CARTESIAN_POINT('Ctrl Pts',(1.91060671806678,0.409509424651126,3.99762321991846));
#75996=CARTESIAN_POINT('Ctrl Pts',(1.9037160386631,0.441658570844584,3.99950615796018));
#75997=CARTESIAN_POINT('Ctrl Pts',(1.89601958163991,0.473606270615025,4.00138909600189));
#75998=CARTESIAN_POINT('Ctrl Pts',(1.88753223325937,0.505309873648744,4.00327203404361));
#75999=CARTESIAN_POINT('Ctrl Pts',(1.86987313549098,0.571273588165984,4.00718974608742));
#76000=CARTESIAN_POINT('Ctrl Pts',(1.84871692100692,0.63644158306265,4.01110745813123));
#76001=CARTESIAN_POINT('Ctrl Pts',(1.82415274352892,0.70041613935997,4.01502517017505));
#76002=CARTESIAN_POINT('Ctrl Pts',(1.79962561670774,0.764294201511163,4.01893697305277));
#76003=CARTESIAN_POINT('Ctrl Pts',(1.7717009034081,0.826981941970619,4.0228487759305));
#76004=CARTESIAN_POINT('Ctrl Pts',(1.740517936403,0.888095328812978,4.02676057880823));
#76005=CARTESIAN_POINT('Ctrl Pts',(1.70937172186249,0.949136686987083,4.03066777120753));
#76006=CARTESIAN_POINT('Ctrl Pts',(1.67497510280882,1.00860694049179,4.03457496360682));
#76007=CARTESIAN_POINT('Ctrl Pts',(1.6375153470833,1.0661423394963,4.03848215600612));
#76008=CARTESIAN_POINT('Ctrl Pts',(1.60007913485701,1.12364157743689,4.04238689273054));
#76009=CARTESIAN_POINT('Ctrl Pts',(1.55958387270889,1.17920796173859,4.04629162945495));
#76010=CARTESIAN_POINT('Ctrl Pts',(1.51626179326266,1.23250402607533,4.05019636617937));
#76011=CARTESIAN_POINT('Ctrl Pts',(1.47295207402633,1.28578488452744,4.05409998884449));
#76012=CARTESIAN_POINT('Ctrl Pts',(1.42681744872955,1.33679632727251,4.0580036115096));
#76013=CARTESIAN_POINT('Ctrl Pts',(1.37813123648841,1.3852329389005,4.06190723417472));
#76014=CARTESIAN_POINT('Ctrl Pts',(1.32944220671819,1.43367235361289,4.06581108274713));
#76015=CARTESIAN_POINT('Ctrl Pts',(1.27820164743175,1.47953629618033,4.06971493131954));
#76016=CARTESIAN_POINT('Ctrl Pts',(1.22471933310697,1.52255658519282,4.07361877989194));
#76017=CARTESIAN_POINT('Ctrl Pts',(1.17117998731088,1.5656227493775,4.07752679137747));
#76018=CARTESIAN_POINT('Ctrl Pts',(1.11539449978614,1.60583889930092,4.081434802863));
#76019=CARTESIAN_POINT('Ctrl Pts',(1.05770449457606,1.64297815023621,4.08534281434852));
#76020=CARTESIAN_POINT('Ctrl Pts',(0.999980010279702,1.68013959786628,4.08925316150146));
#76021=CARTESIAN_POINT('Ctrl Pts',(0.940349170190319,1.71422024250868,4.0931635086544));
#76022=CARTESIAN_POINT('Ctrl Pts',(0.879178799538057,1.74503886445054,4.09707385580733));
#76023=CARTESIAN_POINT('Ctrl Pts',(0.817902453469941,1.77591087852067,4.1009909774928));
#76024=CARTESIAN_POINT('Ctrl Pts',(0.755081703720956,1.80350939274851,4.10490809917826));
#76025=CARTESIAN_POINT('Ctrl Pts',(0.691103149330296,1.8277014080494,4.10882522086373));
#76026=CARTESIAN_POINT('Ctrl Pts',(0.66034902331689,1.83933037175712,4.11070815890558));
#76027=CARTESIAN_POINT('Ctrl Pts',(0.629327587348807,1.85017294903199,4.11259109694742));
#76028=CARTESIAN_POINT('Ctrl Pts',(0.598082753942746,1.86021854077317,4.11447403498927));
#76029=CARTESIAN_POINT('Ctrl Pts',(0.533073572853702,1.88111977856061,4.11839174703309));
#76030=CARTESIAN_POINT('Ctrl Pts',(0.466838218501822,1.89865063147875,4.12230945907691));
#76031=CARTESIAN_POINT('Ctrl Pts',(0.39975926997196,1.91267052208986,4.12622717112072));
#76032=CARTESIAN_POINT('Ctrl Pts',(0.33278149800723,1.92666926621005,4.13013897399845));
#76033=CARTESIAN_POINT('Ctrl Pts',(0.264963134829249,1.93716745808514,4.13405077687618));
#76034=CARTESIAN_POINT('Ctrl Pts',(0.196702446048127,1.94407411065491,4.13796257975391));
#76035=CARTESIAN_POINT('Ctrl Pts',(0.12852220979567,1.95097262299531,4.14186977215321));
#76036=CARTESIAN_POINT('Ctrl Pts',(0.0599011704720178,1.95428795350473,
4.14577696455251));
#76037=CARTESIAN_POINT('Ctrl Pts',(-0.00875347863661003,1.95398039309809,
4.14968415695182));
#76038=CARTESIAN_POINT('Ctrl Pts',(-0.0773649782199373,1.95367302599351,
4.15358889367624));
#76039=CARTESIAN_POINT('Ctrl Pts',(-0.146009554799158,1.94974728694482,
4.15749363040066));
#76040=CARTESIAN_POINT('Ctrl Pts',(-0.214277740888109,1.94221550033973,
4.16139836712508));
#76041=CARTESIAN_POINT('Ctrl Pts',(-0.282526449400711,1.93468586262648,
4.16530198979019));
#76042=CARTESIAN_POINT('Ctrl Pts',(-0.350398491798432,1.92355227367332,
4.16920561245531));
#76043=CARTESIAN_POINT('Ctrl Pts',(-0.417489075214589,1.90887895689498,
4.17310923512043));
#76044=CARTESIAN_POINT('Ctrl Pts',(-0.484583541242724,1.89420479095432,
4.17701308369285));
#76045=CARTESIAN_POINT('Ctrl Pts',(-0.55089597840766,1.87599059810718,4.18091693226526));
#76046=CARTESIAN_POINT('Ctrl Pts',(-0.616033134107817,1.85435141698689,
4.18482078083767));
#76047=CARTESIAN_POINT('Ctrl Pts',(-0.681239749551307,1.83268916068087,
4.1887287923232));
#76048=CARTESIAN_POINT('Ctrl Pts',(-0.745268114533601,1.8075947826105,4.19263680380873));
#76049=CARTESIAN_POINT('Ctrl Pts',(-0.807742426974779,1.77923246701068,
4.19654481529426));
#76050=CARTESIAN_POINT('Ctrl Pts',(-0.870254077897779,1.75085320035106,
4.2004551624472));
#76051=CARTESIAN_POINT('Ctrl Pts',(-0.931209391090382,1.71920233586662,
4.20436550960015));
#76052=CARTESIAN_POINT('Ctrl Pts',(-0.990257288933346,1.68448998266964,
4.20827585675309));
#76053=CARTESIAN_POINT('Ctrl Pts',(-1.04940748508609,1.64971749159833,4.21219297843856));
#76054=CARTESIAN_POINT('Ctrl Pts',(-1.10664326026723,1.61187319710062,4.21611010012403));
#76055=CARTESIAN_POINT('Ctrl Pts',(-1.16164335011394,1.5712099564145,4.22002722180949));
#76056=CARTESIAN_POINT('Ctrl Pts',(-1.18808157945453,1.5516633686546,4.2219101598513));
#76057=CARTESIAN_POINT('Ctrl Pts',(-1.21400372073073,1.53146600340324,4.22379309789311));
#76058=CARTESIAN_POINT('Ctrl Pts',(-1.23937707126458,1.51064902450028,4.22567603593492));
#76059=CARTESIAN_POINT('Ctrl Pts',(-1.29146188795,1.4679172406683,4.22954121261338));
#76060=CARTESIAN_POINT('Ctrl Pts',(-1.34145104924453,1.42239238310119,4.23340638929184));
#76061=CARTESIAN_POINT('Ctrl Pts',(-1.38902358462359,1.37431054764177,4.23727156597029));
#76062=CARTESIAN_POINT('Ctrl Pts',(-1.43651415424535,1.32631155544527,4.24113008308917));
#76063=CARTESIAN_POINT('Ctrl Pts',(-1.48159601034897,1.27576468746548,4.24498860020805));
#76064=CARTESIAN_POINT('Ctrl Pts',(-1.52398108062412,1.22294630540336,4.24884711732693));
#76065=CARTESIAN_POINT('Ctrl Pts',(-1.56632550140521,1.17017857892573,4.25270193392656));
#76066=CARTESIAN_POINT('Ctrl Pts',(-1.6059779459253,1.11514404786349,4.25655675052618));
#76067=CARTESIAN_POINT('Ctrl Pts',(-1.64268815047333,1.05815482812985,4.26041156712581));
#76068=CARTESIAN_POINT('Ctrl Pts',(-1.67937654991031,1.00119945882773,4.26426409404317));
#76069=CARTESIAN_POINT('Ctrl Pts',(-1.71312590054591,0.942292127623766,
4.26811662096054));
#76070=CARTESIAN_POINT('Ctrl Pts',(-1.74372832408474,0.881775216131987,
4.27196914787791));
#76071=CARTESIAN_POINT('Ctrl Pts',(-1.77432373987696,0.821272162600879,
4.27582079259284));
#76072=CARTESIAN_POINT('Ctrl Pts',(-1.80177343135669,0.759160712600748,
4.27967243730778));
#76073=CARTESIAN_POINT('Ctrl Pts',(-1.82591566516403,0.695807432921341,
4.28352408202271));
#76074=CARTESIAN_POINT('Ctrl Pts',(-1.85007491702172,0.632409495017186,
4.28737844179227));
#76075=CARTESIAN_POINT('Ctrl Pts',(-1.87092187371776,0.567768453060736,
4.29123280156184));
#76076=CARTESIAN_POINT('Ctrl Pts',(-1.88834363426166,0.502269169811835,
4.2950871613314));
#76077=CARTESIAN_POINT('Ctrl Pts',(-1.90577213426105,0.436744548738803,
4.29894301212629));
#76078=CARTESIAN_POINT('Ctrl Pts',(-1.91977269465477,0.370361521168322,
4.30279886292118));
#76079=CARTESIAN_POINT('Ctrl Pts',(-1.93028347373097,0.303515586158412,
4.30665471371606));
#76080=CARTESIAN_POINT('Ctrl Pts',(-1.94080991109656,0.236570068331005,
4.31051630871194));
#76081=CARTESIAN_POINT('Ctrl Pts',(-1.94783613896308,0.16916077050416,4.31437790370782));
#76082=CARTESIAN_POINT('Ctrl Pts',(-1.95135225678392,0.101687609590854,
4.31823949870369));
#76083=CARTESIAN_POINT('Ctrl Pts',(-1.95314018630796,0.0673778217440355,
4.32020310176105));
#76084=CARTESIAN_POINT('Ctrl Pts',(-1.9540213521528,0.033051515596815,4.3221667048184));
#76085=CARTESIAN_POINT('Ctrl Pts',(-1.95399960711636,-0.0012391081865255,
4.32413030787576));
#76086=CARTESIAN_POINT('',(-1.95503514488101,0.00166188402949293,5.02413030787576));
#76087=CARTESIAN_POINT('Ctrl Pts',(-1.95619906720822,-0.0012405029508829,
4.32413030787576));
#76088=CARTESIAN_POINT('Ctrl Pts',(-1.95674893362639,-0.0755294225214843,
4.32837955087737));
#76089=CARTESIAN_POINT('Ctrl Pts',(-1.91917105279229,-0.797299711222014,
4.36969612752756));
#76090=CARTESIAN_POINT('Ctrl Pts',(-1.0218363276303,-2.07167577132427,4.44808003782619));
#76091=CARTESIAN_POINT('Ctrl Pts',(1.18748472594414,-1.9813808335618,4.55928203877191));
#76092=CARTESIAN_POINT('Ctrl Pts',(2.30873910126256,-0.0755893131216004,
4.67048403971755));
#76093=CARTESIAN_POINT('Ctrl Pts',(1.31454556387366,1.89946306688404,4.7816860406632));
#76094=CARTESIAN_POINT('Ctrl Pts',(-0.884137760921009,2.13407834946856,
4.89288804160887));
#76095=CARTESIAN_POINT('Ctrl Pts',(-1.89326256884871,0.88351086131374,4.97370279734637));
#76096=CARTESIAN_POINT('Ctrl Pts',(-1.95609296160575,0.118629928772321,
5.01745021943535));
#76097=CARTESIAN_POINT('Ctrl Pts',(-1.95503514488101,0.00166188402949293,
5.02413030787576));
#76098=CARTESIAN_POINT('',(-1.95369680431385,0.000267557090813054,5.72413028758448));
#76099=CARTESIAN_POINT('Ctrl Pts',(-1.95503514488101,0.00166188402949293,
5.02413030787576));
#76100=CARTESIAN_POINT('Ctrl Pts',(-1.95022321215187,-0.530417397378261,
5.0545175530839));
#76101=CARTESIAN_POINT('Ctrl Pts',(-1.4502565862486,-1.71950099814147,5.12197213194059));
#76102=CARTESIAN_POINT('Ctrl Pts',(0.561680408542795,-2.24064836612449,
5.22649404444583));
#76103=CARTESIAN_POINT('Ctrl Pts',(2.18754642622138,-0.742044887511754,
5.33769604539148));
#76104=CARTESIAN_POINT('Ctrl Pts',(1.80901076907705,1.43647833931448,5.44889804633715));
#76105=CARTESIAN_POINT('Ctrl Pts',(-0.22708249317601,2.29878740279546,5.56010004728279));
#76106=CARTESIAN_POINT('Ctrl Pts',(-1.73523991140407,1.27244417468795,5.65184406350195));
#76107=CARTESIAN_POINT('Ctrl Pts',(-1.95119622568095,0.3103015106477,5.70652074607255));
#76108=CARTESIAN_POINT('Ctrl Pts',(-1.95081926741735,0.000270554286225176,
5.72413009499459));
#76109=CARTESIAN_POINT('',(-1.95399918195666,-0.00178799124785366,6.42413030787577));
#76110=CARTESIAN_POINT('Ctrl Pts',(-1.9539999817252,0.000267241306175345,
5.72413030787576));
#76111=CARTESIAN_POINT('Ctrl Pts',(-1.95400974747832,-0.0711374442006378,
5.72817939860468));
#76112=CARTESIAN_POINT('Ctrl Pts',(-1.95010119842815,-0.142484142639079,
5.73222848933361));
#76113=CARTESIAN_POINT('Ctrl Pts',(-1.94231926826411,-0.213335088839061,
5.73627758006253));
#76114=CARTESIAN_POINT('Ctrl Pts',(-1.93451919732893,-0.284351198536104,
5.74033610979009));
#76115=CARTESIAN_POINT('Ctrl Pts',(-1.92282775581061,-0.354868811322742,
5.74439463951765));
#76116=CARTESIAN_POINT('Ctrl Pts',(-1.90734149414534,-0.42445780086063,
5.74845316924521));
#76117=CARTESIAN_POINT('Ctrl Pts',(-1.89183676010772,-0.494129797760376,
5.75251654008123));
#76118=CARTESIAN_POINT('Ctrl Pts',(-1.87252830400951,-0.562870543064802,
5.75657991091725));
#76119=CARTESIAN_POINT('Ctrl Pts',(-1.84956251433186,-0.630265424704857,
5.76064328175326));
#76120=CARTESIAN_POINT('Ctrl Pts',(-1.82653669710265,-0.69783646182618,
5.76471727335198));
#76121=CARTESIAN_POINT('Ctrl Pts',(-1.79983460214371,-0.764054196930572,
5.7687912649507));
#76122=CARTESIAN_POINT('Ctrl Pts',(-1.76965082572354,-0.828523961642621,
5.77286525654942));
#76123=CARTESIAN_POINT('Ctrl Pts',(-1.74584655788662,-0.879367683953132,
5.77607818742431));
#76124=CARTESIAN_POINT('Ctrl Pts',(-1.71987779756399,-0.929124638781733,
5.77929111829921));
#76125=CARTESIAN_POINT('Ctrl Pts',(-1.69185916877391,-0.977613703379642,
5.7825040491741));
#76126=CARTESIAN_POINT('Ctrl Pts',(-1.65769443764956,-1.0367392182958,5.78642176121791));
#76127=CARTESIAN_POINT('Ctrl Pts',(-1.62035868086182,-1.09418914636563,
5.79033947326172));
#76128=CARTESIAN_POINT('Ctrl Pts',(-1.58004116331142,-1.14960250619137,
5.79425718530553));
#76129=CARTESIAN_POINT('Ctrl Pts',(-1.53978445750642,-1.20493228490067,
5.79816898818325));
#76130=CARTESIAN_POINT('Ctrl Pts',(-1.49655520382515,-1.25823119711222,
5.80208079106098));
#76131=CARTESIAN_POINT('Ctrl Pts',(-1.45058757855937,-1.30916449574882,
5.8059925939387));
#76132=CARTESIAN_POINT('Ctrl Pts',(-1.40467413106055,-1.36003776404084,
5.80989978633799));
#76133=CARTESIAN_POINT('Ctrl Pts',(-1.35602904979169,-1.40855059247393,
5.81380697873729));
#76134=CARTESIAN_POINT('Ctrl Pts',(-1.30492754459694,-1.45440025555285,
5.81771417113658));
#76135=CARTESIAN_POINT('Ctrl Pts',(-1.25385815675652,-1.5002211020662,5.821618907861));
#76136=CARTESIAN_POINT('Ctrl Pts',(-1.20033577287194,-1.54338177564893,
5.82552364458541));
#76137=CARTESIAN_POINT('Ctrl Pts',(-1.14467221103605,-1.5836165979434,5.82942838130982));
#76138=CARTESIAN_POINT('Ctrl Pts',(-1.08902453055477,-1.62383994085245,
5.83333200397494));
#76139=CARTESIAN_POINT('Ctrl Pts',(-1.03123728339406,-1.66113880152937,
5.83723562664006));
#76140=CARTESIAN_POINT('Ctrl Pts',(-0.971653654361067,-1.69528911279663,
5.84113924930517));
#76141=CARTESIAN_POINT('Ctrl Pts',(-0.912066577152505,-1.72944140038307,
5.84504309787758));
#76142=CARTESIAN_POINT('Ctrl Pts',(-0.850683339807656,-1.76044453436794,
5.84894694644999));
#76143=CARTESIAN_POINT('Ctrl Pts',(-0.787872676805905,-1.78811986319226,
5.8528507950224));
#76144=CARTESIAN_POINT('Ctrl Pts',(-0.72499503494271,-1.81582470391673,
5.85675880650792));
#76145=CARTESIAN_POINT('Ctrl Pts',(-0.66068738074735,-1.84019445863267,
5.86066681799344));
#76146=CARTESIAN_POINT('Ctrl Pts',(-0.595338496412384,-1.86109862035558,
5.86457482947896));
#76147=CARTESIAN_POINT('Ctrl Pts',(-0.529950555575004,-1.882015275688,5.8684851766319));
#76148=CARTESIAN_POINT('Ctrl Pts',(-0.46352062204288,-1.89946209086813,
5.87239552378484));
#76149=CARTESIAN_POINT('Ctrl Pts',(-0.396449971809546,-1.91335919781211,
5.87630587093778));
#76150=CARTESIAN_POINT('Ctrl Pts',(-0.329263124143222,-1.92728038098239,
5.88022299262325));
#76151=CARTESIAN_POINT('Ctrl Pts',(-0.261433830450867,-1.93763950757668,
5.88414011430871));
#76152=CARTESIAN_POINT('Ctrl Pts',(-0.193369956017992,-1.94440840877363,
5.88805723599417));
#76153=CARTESIAN_POINT('Ctrl Pts',(-0.160652039972154,-1.94766218095351,
5.88994017403604));
#76154=CARTESIAN_POINT('Ctrl Pts',(-0.127879940264592,-1.95008714533632,
5.8918231120779));
#76155=CARTESIAN_POINT('Ctrl Pts',(-0.0950988157093481,-1.95168445586132,
5.89370605011976));
#76156=CARTESIAN_POINT('Ctrl Pts',(-0.026893169201801,-1.95500788050001,
5.89762376216355));
#76157=CARTESIAN_POINT('Ctrl Pts',(0.0416224541382525,-1.95475822391928,
5.90154147420734));
#76158=CARTESIAN_POINT('Ctrl Pts',(0.110042105676551,-1.95089895560438,
5.90545918625112));
#76159=CARTESIAN_POINT('Ctrl Pts',(0.178358558439678,-1.94704550830369,
5.90937098912883));
#76160=CARTESIAN_POINT('Ctrl Pts',(0.246578839436212,-1.93959328196012,
5.91328279200653));
#76161=CARTESIAN_POINT('Ctrl Pts',(0.314294713424914,-1.92855770800698,
5.91719459488423));
#76162=CARTESIAN_POINT('Ctrl Pts',(0.381930777007469,-1.91753514065906,
5.9211017872835));
#76163=CARTESIAN_POINT('Ctrl Pts',(0.449063130968994,-1.90293769205455,
5.92500897968277));
#76164=CARTESIAN_POINT('Ctrl Pts',(0.515288218719501,-1.88483263226444,
5.92891617208205));
#76165=CARTESIAN_POINT('Ctrl Pts',(0.581471683926788,-1.86673895152506,
5.93282090880644));
#76166=CARTESIAN_POINT('Ctrl Pts',(0.646748540525457,-1.84514216210282,
5.93672564553083));
#76167=CARTESIAN_POINT('Ctrl Pts',(0.710726532295221,-1.82016037653049,
5.94063038225522));
#76168=CARTESIAN_POINT('Ctrl Pts',(0.774686270522744,-1.79518571850414,
5.94453400492031));
#76169=CARTESIAN_POINT('Ctrl Pts',(0.837347421484593,-1.76682816038839,
5.9484376275854));
#76170=CARTESIAN_POINT('Ctrl Pts',(0.898335705444953,-1.73525472491007,
5.95234125025049));
#76171=CARTESIAN_POINT('Ctrl Pts',(0.959327518870092,-1.70367946223935,
5.95624509882288));
#76172=CARTESIAN_POINT('Ctrl Pts',(1.01864583733957,-1.66888818118021,5.96014894739527));
#76173=CARTESIAN_POINT('Ctrl Pts',(1.07594070713876,-1.63109398709018,5.96405279596766));
#76174=CARTESIAN_POINT('Ctrl Pts',(1.13329667397083,-1.59325949073353,5.96796080745317));
#76175=CARTESIAN_POINT('Ctrl Pts',(1.18862447442876,-1.55241596212164,5.97186881893867));
#76176=CARTESIAN_POINT('Ctrl Pts',(1.2416037557157,-1.50881944373496,5.97577683042417));
#76177=CARTESIAN_POINT('Ctrl Pts',(1.29461470067135,-1.46519686939429,5.97968717757709));
#76178=CARTESIAN_POINT('Ctrl Pts',(1.34527397005212,-1.41881836300644,5.98359752473));
#76179=CARTESIAN_POINT('Ctrl Pts',(1.3932970015496,-1.36997790692876,5.98750787188292));
#76180=CARTESIAN_POINT('Ctrl Pts',(1.44140323118165,-1.32105283655849,5.99142499356836));
#76181=CARTESIAN_POINT('Ctrl Pts',(1.4868637815959,-1.26965767197482,5.9953421152538));
#76182=CARTESIAN_POINT('Ctrl Pts',(1.52943397159461,-1.21611994742802,5.99925923693924));
#76183=CARTESIAN_POINT('Ctrl Pts',(1.54989721901025,-1.19038466873877,6.0011421749813));
#76184=CARTESIAN_POINT('Ctrl Pts',(1.56969323977391,-1.16415475197086,6.00302511302336));
#76185=CARTESIAN_POINT('Ctrl Pts',(1.58879853394519,-1.13746877694889,6.00490805106542));
#76186=CARTESIAN_POINT('Ctrl Pts',(1.62854973096024,-1.08194492889261,6.00882576310932));
#76187=CARTESIAN_POINT('Ctrl Pts',(1.66546583088142,-1.0242244426078,6.01274347515322));
#76188=CARTESIAN_POINT('Ctrl Pts',(1.69929616333118,-0.964628710586589,
6.01666118719712));
#76189=CARTESIAN_POINT('Ctrl Pts',(1.73307546879098,-0.905122868040263,
6.02057299007493));
#76190=CARTESIAN_POINT('Ctrl Pts',(1.76377800295952,-0.843747817632082,
6.02448479295275));
#76191=CARTESIAN_POINT('Ctrl Pts',(1.79119552880505,-0.780855029815905,
6.02839659583057));
#76192=CARTESIAN_POINT('Ctrl Pts',(1.81858074016145,-0.718036367882554,
6.03230378822995));
#76193=CARTESIAN_POINT('Ctrl Pts',(1.84268843678239,-0.653703969994269,
6.03621098062933));
#76194=CARTESIAN_POINT('Ctrl Pts',(1.86335648554363,-0.588233463671093,
6.04011817302872));
#76195=CARTESIAN_POINT('Ctrl Pts',(1.88401154441264,-0.522804105635826,
6.04402290975322));
#76196=CARTESIAN_POINT('Ctrl Pts',(1.90123109596156,-0.456238526201307,
6.04792764647772));
#76197=CARTESIAN_POINT('Ctrl Pts',(1.91490186176886,-0.388930404820886,
6.05183238320223));
#76198=CARTESIAN_POINT('Ctrl Pts',(1.92856872717395,-0.321641487101036,
6.05573600586743));
#76199=CARTESIAN_POINT('Ctrl Pts',(1.93868871891055,-0.253610929925255,
6.05963962853263));
#76200=CARTESIAN_POINT('Ctrl Pts',(1.94519940677486,-0.185243806597507,
6.06354325119783));
#76201=CARTESIAN_POINT('Ctrl Pts',(1.95171047142043,-0.116872726782948,
6.06744709977033));
#76202=CARTESIAN_POINT('Ctrl Pts',(1.95461177340225,-0.0481655321755956,
6.07135094834282));
#76203=CARTESIAN_POINT('Ctrl Pts',(1.95389279482182,0.0204681787997021,
6.07525479691531));
#76204=CARTESIAN_POINT('Ctrl Pts',(1.95317304955044,0.0891750781096338,
6.07916280840092));
#76205=CARTESIAN_POINT('Ctrl Pts',(1.94882532436429,0.157807844474764,6.08307081988653));
#76206=CARTESIAN_POINT('Ctrl Pts',(1.94089122823017,0.225958492159874,6.08697883137214));
#76207=CARTESIAN_POINT('Ctrl Pts',(1.93295239019346,0.294149870852989,6.09088917852517));
#76208=CARTESIAN_POINT('Ctrl Pts',(1.92142299799078,0.361858072310764,6.09479952567819));
#76209=CARTESIAN_POINT('Ctrl Pts',(1.90639594131311,0.42868463343688,6.09870987283122));
#76210=CARTESIAN_POINT('Ctrl Pts',(1.89134285081281,0.495626969120597,6.10262699451676));
#76211=CARTESIAN_POINT('Ctrl Pts',(1.87278013473514,0.561684142528404,6.10654411620231));
#76212=CARTESIAN_POINT('Ctrl Pts',(1.85085049208168,0.626473028917459,6.11046123788786));
#76213=CARTESIAN_POINT('Ctrl Pts',(1.84030903800031,0.657616676884984,6.11234417592893));
#76214=CARTESIAN_POINT('Ctrl Pts',(1.82899031236449,0.688467566994951,6.11422711397));
#76215=CARTESIAN_POINT('Ctrl Pts',(1.81691400659672,0.718985043399842,6.11611005201107));
#76216=CARTESIAN_POINT('Ctrl Pts',(1.7917875884574,0.782480858051353,6.12002776405482));
#76217=CARTESIAN_POINT('Ctrl Pts',(1.7632787377027,0.844784135642975,6.12394547609856));
#76218=CARTESIAN_POINT('Ctrl Pts',(1.73152174607975,0.905510045694094,6.12786318814231));
#76219=CARTESIAN_POINT('Ctrl Pts',(1.69981265418395,0.966144361599376,6.13177499101997));
#76220=CARTESIAN_POINT('Ctrl Pts',(1.66486537073897,1.02520559928078,6.13568679389763));
#76221=CARTESIAN_POINT('Ctrl Pts',(1.62686246002969,1.08232829407078,6.13959859677529));
#76222=CARTESIAN_POINT('Ctrl Pts',(1.58890433981864,1.13938366365035,6.14350578917452));
#76223=CARTESIAN_POINT('Ctrl Pts',(1.54789801591874,1.19450462023064,6.14741298157376));
#76224=CARTESIAN_POINT('Ctrl Pts',(1.50407133776116,1.24735135824889,6.15132017397299));
#76225=CARTESIAN_POINT('Ctrl Pts',(1.46027220472077,1.30016488203206,6.15522491069735));
#76226=CARTESIAN_POINT('Ctrl Pts',(1.41365654701226,1.35070664473475,6.15912964742171));
#76227=CARTESIAN_POINT('Ctrl Pts',(1.36449385859073,1.39866811998708,6.16303438414607));
#76228=CARTESIAN_POINT('Ctrl Pts',(1.31534519676154,1.44661591136485,6.16693800681113));
#76229=CARTESIAN_POINT('Ctrl Pts',(1.26365129881092,1.49198453330514,6.17084162947618));
#76230=CARTESIAN_POINT('Ctrl Pts',(1.20971878751819,1.53450202187078,6.17474525214124));
#76231=CARTESIAN_POINT('Ctrl Pts',(1.15578315508681,1.57702197097412,6.17864910071359));
#76232=CARTESIAN_POINT('Ctrl Pts',(1.09960904006529,1.61669015652933,6.18255294928594));
#76233=CARTESIAN_POINT('Ctrl Pts',(1.04153499769514,1.653275793259,6.18645679785829));
#76234=CARTESIAN_POINT('Ctrl Pts',(0.983399027412527,1.68990044349655,6.19036480934376));
#76235=CARTESIAN_POINT('Ctrl Pts',(0.92335950353096,1.72343572200999,6.19427282082922));
#76236=CARTESIAN_POINT('Ctrl Pts',(0.861781871380804,1.75369552835132,6.19818083231469));
#76237=CARTESIAN_POINT('Ctrl Pts',(0.800167436659958,1.78397341980932,6.20209117946757));
#76238=CARTESIAN_POINT('Ctrl Pts',(0.737013516630954,1.81097174964362,6.20600152662045));
#76239=CARTESIAN_POINT('Ctrl Pts',(0.672705340160985,1.83455267717198,6.20991187377334));
#76240=CARTESIAN_POINT('Ctrl Pts',(0.608285752142004,1.85817445778945,6.21382899545875));
#76241=CARTESIAN_POINT('Ctrl Pts',(0.542708386512292,1.87836687477056,6.21774611714416));
#76242=CARTESIAN_POINT('Ctrl Pts',(0.476372570451038,1.89504226183003,6.22166323882957));
#76243=CARTESIAN_POINT('Ctrl Pts',(0.444485322194318,1.9030580252368,6.22354617687196));
#76244=CARTESIAN_POINT('Ctrl Pts',(0.412422954664156,1.91026188256864,6.22542911491434));
#76245=CARTESIAN_POINT('Ctrl Pts',(0.380230307819654,1.91664835403247,6.22731205295673));
#76246=CARTESIAN_POINT('Ctrl Pts',(0.313249070295753,1.92993628789278,6.23122976500039));
#76247=CARTESIAN_POINT('Ctrl Pts',(0.245437314789097,1.93973520542814,6.23514747704405));
#76248=CARTESIAN_POINT('Ctrl Pts',(0.177191246535985,1.94594945005029,6.23906518908771));
#76249=CARTESIAN_POINT('Ctrl Pts',(0.109048115238776,1.95215432159878,6.24297699196528));
#76250=CARTESIAN_POINT('Ctrl Pts',(0.0404724573062881,1.9547852065334,6.24688879484285));
#76251=CARTESIAN_POINT('Ctrl Pts',(-0.0281296413821285,1.95379751337638,
6.25080059772042));
#76252=CARTESIAN_POINT('Ctrl Pts',(-0.0966508851536292,1.95281098432147,
6.25470779011956));
#76253=CARTESIAN_POINT('Ctrl Pts',(-0.165198018180031,1.94821435428103,
6.2586149825187));
#76254=CARTESIAN_POINT('Ctrl Pts',(-0.233361982001063,1.94001499616795,
6.26252217491784));
#76255=CARTESIAN_POINT('Ctrl Pts',(-0.301483104693047,1.9318207913608,6.26642691164209));
#76256=CARTESIAN_POINT('Ctrl Pts',(-0.369221048510593,1.92002840874236,
6.27033164836635));
#76257=CARTESIAN_POINT('Ctrl Pts',(-0.436170478628699,1.90469717109382,
6.27423638509061));
#76258=CARTESIAN_POINT('Ctrl Pts',(-0.503100807424284,1.88937030759626,
6.27814000775556));
#76259=CARTESIAN_POINT('Ctrl Pts',(-0.569242589755988,1.87050670317321,
6.28204363042051));
#76260=CARTESIAN_POINT('Ctrl Pts',(-0.634201101710008,1.84821669795233,
6.28594725308546));
#76261=CARTESIAN_POINT('Ctrl Pts',(-0.69916337289066,1.82592540278223,6.28985110165772));
#76262=CARTESIAN_POINT('Ctrl Pts',(-0.762941773203437,1.80020747524087,
6.29375495022997));
#76263=CARTESIAN_POINT('Ctrl Pts',(-0.82515888514281,1.77122240677727,6.29765879880223));
#76264=CARTESIAN_POINT('Ctrl Pts',(-0.887442343003711,1.74220642975785,
6.3015668102876));
#76265=CARTESIAN_POINT('Ctrl Pts',(-0.948160742984259,1.70991656700681,
6.30547482177296));
#76266=CARTESIAN_POINT('Ctrl Pts',(-1.00695965307578,1.67455912319557,6.30938283325833));
#76267=CARTESIAN_POINT('Ctrl Pts',(-1.06579370500315,1.63918054760681,6.31329318041111));
#76268=CARTESIAN_POINT('Ctrl Pts',(-1.12270557615092,1.60073101768641,6.31720352756388));
#76269=CARTESIAN_POINT('Ctrl Pts',(-1.17737067538964,1.55945961561451,6.32111387471666));
#76270=CARTESIAN_POINT('Ctrl Pts',(-1.23213047990089,1.51811671235747,6.32503099640197));
#76271=CARTESIAN_POINT('Ctrl Pts',(-1.2846353673682,1.47394249614177,6.32894811808727));
#76272=CARTESIAN_POINT('Ctrl Pts',(-1.33459527732834,1.42722508586869,6.33286523977257));
#76273=CARTESIAN_POINT('Ctrl Pts',(-1.35861072097803,1.40476829331708,6.33474817781584));
#76274=CARTESIAN_POINT('Ctrl Pts',(-1.38203867359999,1.38172437852258,6.33663111585911));
#76275=CARTESIAN_POINT('Ctrl Pts',(-1.40485023258728,1.35812805876304,6.33851405390238));
#76276=CARTESIAN_POINT('Ctrl Pts',(-1.45168051628269,1.30968672473925,6.34237957325581));
#76277=CARTESIAN_POINT('Ctrl Pts',(-1.49610723096855,1.25871160704438,6.34624509260924));
#76278=CARTESIAN_POINT('Ctrl Pts',(-1.53783880507626,1.20547410158893,6.35011061196267));
#76279=CARTESIAN_POINT('Ctrl Pts',(-1.57951346580268,1.15230920126548,6.35397085953373));
#76280=CARTESIAN_POINT('Ctrl Pts',(-1.61849995954832,1.09688842053841,6.35783110710478));
#76281=CARTESIAN_POINT('Ctrl Pts',(-1.65454370561901,1.03951966128425,6.36169135467584));
#76282=CARTESIAN_POINT('Ctrl Pts',(-1.69055144198506,0.982208216607538,
6.36554774564513));
#76283=CARTESIAN_POINT('Ctrl Pts',(-1.72362199059012,0.922953077188807,
6.36940413661441));
#76284=CARTESIAN_POINT('Ctrl Pts',(-1.753542463168,0.862093283738307,6.3732605275837));
#76285=CARTESIAN_POINT('Ctrl Pts',(-1.7834439502011,0.801272107870848,6.37711447154339));
#76286=CARTESIAN_POINT('Ctrl Pts',(-1.81019910352668,0.738848750838604,
6.38096841550308));
#76287=CARTESIAN_POINT('Ctrl Pts',(-1.83364062917215,0.675187413278106,
6.38482235946277));
#76288=CARTESIAN_POINT('Ctrl Pts',(-1.85708378576909,0.611521646460108,
6.38867657156182));
#76289=CARTESIAN_POINT('Ctrl Pts',(-1.87721266552031,0.546618196918323,
6.39253078366087));
#76290=CARTESIAN_POINT('Ctrl Pts',(-1.89390847856224,0.480860348573328,
6.39638499575992));
#76291=CARTESIAN_POINT('Ctrl Pts',(-1.9106049567987,0.415099880304359,6.40023936141848));
#76292=CARTESIAN_POINT('Ctrl Pts',(-1.92386798326764,0.348485439130104,
6.40409372707703));
#76293=CARTESIAN_POINT('Ctrl Pts',(-1.93362954546735,0.281412119312107,
6.40794809273559));
#76294=CARTESIAN_POINT('Ctrl Pts',(-1.94339988590562,0.214278482754805,
6.41180592449317));
#76295=CARTESIAN_POINT('Ctrl Pts',(-1.94966242192901,0.146685647235719,
6.41566375625076));
#76296=CARTESIAN_POINT('Ctrl Pts',(-1.95240098832497,0.0790340482809151,
6.41952158800834));
#76297=CARTESIAN_POINT('Ctrl Pts',(-1.95349152191573,0.0520942810957384,
6.42105782796415));
#76298=CARTESIAN_POINT('Ctrl Pts',(-1.95402382695803,0.0251452012775251,
6.42259406791996));
#76299=CARTESIAN_POINT('Ctrl Pts',(-1.95399918195666,-0.00178799124785366,
6.42413030787577));
#76300=CARTESIAN_POINT('',(-1.95414064801411,0.000755162503876828,7.12413030787577));
#76301=CARTESIAN_POINT('Ctrl Pts',(-1.954054516794,-0.00178804188155213,
6.42413030787577));
#76302=CARTESIAN_POINT('Ctrl Pts',(-1.95543262626536,-0.151315844023487,
6.43265889019986));
#76303=CARTESIAN_POINT('Ctrl Pts',(-1.87143461050528,-0.949196308976276,
6.47825480617249));
#76304=CARTESIAN_POINT('Ctrl Pts',(-0.776860394673377,-2.17542591450428,
6.56091805579371));
#76305=CARTESIAN_POINT('Ctrl Pts',(1.40742627626055,-1.8317044680295,6.67212005673936));
#76306=CARTESIAN_POINT('Ctrl Pts',(2.30211856357103,0.190368330558137,6.78332205768501));
#76307=CARTESIAN_POINT('Ctrl Pts',(1.08742919413144,2.03801072910203,6.89452405863067));
#76308=CARTESIAN_POINT('Ctrl Pts',(-1.12364812450813,2.01826778932502,7.00572605957632));
#76309=CARTESIAN_POINT('Ctrl Pts',(-1.936824180042,0.731891475031694,7.08226147599136));
#76310=CARTESIAN_POINT('Ctrl Pts',(-1.95706302779737,0.0426910058065101,
7.12172955875784));
#76311=CARTESIAN_POINT('Ctrl Pts',(-1.95685604123946,0.000756211846537467,
7.12413030787577));
#76312=CARTESIAN_POINT('',(-1.95399953930486,0.00134178850078647,7.82413028070635));
#76313=CARTESIAN_POINT('Ctrl Pts',(-1.95399985409717,0.000755108095159142,
7.12413030787577));
#76314=CARTESIAN_POINT('Ctrl Pts',(-1.9540260066976,-0.066920205871119,
7.12801036203239));
#76315=CARTESIAN_POINT('Ctrl Pts',(-1.95053207911632,-0.134738559516202,
7.13189041618902));
#76316=CARTESIAN_POINT('Ctrl Pts',(-1.94349970506361,-0.202299027228677,
7.13577047034564));
#76317=CARTESIAN_POINT('Ctrl Pts',(-1.93647868148827,-0.269750450178347,
7.13964426197035));
#76318=CARTESIAN_POINT('Ctrl Pts',(-1.92593060117903,-0.33694431819104,
7.14351805359506));
#76319=CARTESIAN_POINT('Ctrl Pts',(-1.91188909971567,-0.403479950416863,
7.14739184521977));
#76320=CARTESIAN_POINT('Ctrl Pts',(-1.89786021818198,-0.46995578312616,
7.15126215523833));
#76321=CARTESIAN_POINT('Ctrl Pts',(-1.88034424118874,-0.535774063500215,
7.15513246525689));
#76322=CARTESIAN_POINT('Ctrl Pts',(-1.85942639198367,-0.600541000094582,
7.15900277527546));
#76323=CARTESIAN_POINT('Ctrl Pts',(-1.83851983101935,-0.665272985448707,
7.16287099669538));
#76324=CARTESIAN_POINT('Ctrl Pts',(-1.81421519195131,-0.728954274905217,
7.16673921811531));
#76325=CARTESIAN_POINT('Ctrl Pts',(-1.78664791545218,-0.791204920491756,
7.17060743953524));
#76326=CARTESIAN_POINT('Ctrl Pts',(-1.75908561662076,-0.85344432583018,
7.17447496249223));
#76327=CARTESIAN_POINT('Ctrl Pts',(-1.72826205366677,-0.914253141235299,
7.17834248544923));
#76328=CARTESIAN_POINT('Ctrl Pts',(-1.69436055598944,-0.97327195906754,
7.18221000840622));
#76329=CARTESIAN_POINT('Ctrl Pts',(-1.66042884852077,-1.03234336885866,
7.18608097773194));
#76330=CARTESIAN_POINT('Ctrl Pts',(-1.62341397617838,-1.08962115703652,
7.18995194705767));
#76331=CARTESIAN_POINT('Ctrl Pts',(-1.58354441879559,-1.14477206189762,
7.1938229163834));
#76332=CARTESIAN_POINT('Ctrl Pts',(-1.54365840156346,-1.19994573539838,
7.19769548380993));
#76333=CARTESIAN_POINT('Ctrl Pts',(-1.50091566732535,-1.25299038469823,
7.20156805123646));
#76334=CARTESIAN_POINT('Ctrl Pts',(-1.45558526447401,-1.30360559136808,
7.205440618663));
#76335=CARTESIAN_POINT('Ctrl Pts',(-1.41017027373367,-1.35431524752911,
7.2093204124163));
#76336=CARTESIAN_POINT('Ctrl Pts',(-1.36215832235579,-1.40258604666527,
7.21320020616961));
#76337=CARTESIAN_POINT('Ctrl Pts',(-1.31185514347887,-1.44815471636426,
7.21707999992292));
#76338=CARTESIAN_POINT('Ctrl Pts',(-1.26409889165823,-1.49141617446416,
7.22076335377115));
#76339=CARTESIAN_POINT('Ctrl Pts',(-1.21427813020722,-1.53224230292097,
7.2244467076194));
#76340=CARTESIAN_POINT('Ctrl Pts',(-1.16267879803052,-1.57044389030946,
7.22813006146763));
#76341=CARTESIAN_POINT('Ctrl Pts',(-1.1077963911698,-1.61107610342805,7.23204777349962));
#76342=CARTESIAN_POINT('Ctrl Pts',(-1.05067238186761,-1.64890863561676,
7.23596548553161));
#76343=CARTESIAN_POINT('Ctrl Pts',(-0.99162412135517,-1.68368571946981,
7.23988319756359));
#76344=CARTESIAN_POINT('Ctrl Pts',(-0.932664924562514,-1.71841034832379,
7.24379500042902));
#76345=CARTESIAN_POINT('Ctrl Pts',(-0.871787657231446,-1.7500884275218,
7.24770680329444));
#76346=CARTESIAN_POINT('Ctrl Pts',(-0.809340421898512,-1.77850613760008,
7.25161860615986));
#76347=CARTESIAN_POINT('Ctrl Pts',(-0.746966787327428,-1.80689035436034,
7.25552579854622));
#76348=CARTESIAN_POINT('Ctrl Pts',(-0.683027305285058,-1.83202163077789,
7.25943299093258));
#76349=CARTESIAN_POINT('Ctrl Pts',(-0.617894968048404,-1.85373185991407,
7.26334018331894));
#76350=CARTESIAN_POINT('Ctrl Pts',(-0.552803566566573,-1.87542844414427,
7.26724492003003));
#76351=CARTESIAN_POINT('Ctrl Pts',(-0.486521262762922,-1.89370809099178,
7.27114965674113));
#76352=CARTESIAN_POINT('Ctrl Pts',(-0.419439878198159,-1.90845125391693,
7.27505439345222));
#76353=CARTESIAN_POINT('Ctrl Pts',(-0.35237763261,-1.92319021047318,7.27895801610365));
#76354=CARTESIAN_POINT('Ctrl Pts',(-0.284517239149783,-1.93439458053492,
7.28286163875509));
#76355=CARTESIAN_POINT('Ctrl Pts',(-0.216262723240614,-1.94199547747582,
7.28676526140652));
#76356=CARTESIAN_POINT('Ctrl Pts',(-0.148004257367238,-1.94959681428902,
7.2906691099649));
#76357=CARTESIAN_POINT('Ctrl Pts',(-0.0793521130250479,-1.95359421204594,
7.29457295852329));
#76358=CARTESIAN_POINT('Ctrl Pts',(-0.0107156686257376,-1.95397061760045,
7.29847680708168));
#76359=CARTESIAN_POINT('Ctrl Pts',(0.0579939670161398,-1.95434742453926,
7.30238481855277));
#76360=CARTESIAN_POINT('Ctrl Pts',(0.126687376355374,-1.95109553054233,
7.30629283002387));
#76361=CARTESIAN_POINT('Ctrl Pts',(0.194955961596583,-1.94425002842689,
7.31020084149497));
#76362=CARTESIAN_POINT('Ctrl Pts',(0.263265348328256,-1.93740043501985,
7.31411118863323));
#76363=CARTESIAN_POINT('Ctrl Pts',(0.331148919299421,-1.92695303391652,
7.31802153577148));
#76364=CARTESIAN_POINT('Ctrl Pts',(0.398206779776185,-1.91299434409522,
7.32193188290974));
#76365=CARTESIAN_POINT('Ctrl Pts',(0.465380815524651,-1.89901147135828,
7.32584900458029));
#76366=CARTESIAN_POINT('Ctrl Pts',(0.531725810164595,-1.88150529411959,
7.32976612625084));
#76367=CARTESIAN_POINT('Ctrl Pts',(0.59685641047922,-1.86061237910261,7.33368324792139));
#76368=CARTESIAN_POINT('Ctrl Pts',(0.628164320544014,-1.85056927338604,
7.33556618608536));
#76369=CARTESIAN_POINT('Ctrl Pts',(0.659191914101623,-1.83974432301109,
7.33744912424932));
#76370=CARTESIAN_POINT('Ctrl Pts',(0.689898226227635,-1.82815656808928,
7.33933206241329));
#76371=CARTESIAN_POINT('Ctrl Pts',(0.753786938260937,-1.80404664781379,
7.34324977462961));
#76372=CARTESIAN_POINT('Ctrl Pts',(0.816537243537038,-1.77653569426117,
7.34716748684593));
#76373=CARTESIAN_POINT('Ctrl Pts',(0.877762217461966,-1.74575184078272,
7.35108519906224));
#76374=CARTESIAN_POINT('Ctrl Pts',(0.938894844507095,-1.71501441921978,
7.35499700211314));
#76375=CARTESIAN_POINT('Ctrl Pts',(0.998506270194983,-1.68101411423343,
7.35890880516403));
#76376=CARTESIAN_POINT('Ctrl Pts',(1.05622816292326,-1.64392763461405,7.36282060821492));
#76377=CARTESIAN_POINT('Ctrl Pts',(1.11388202422737,-1.60688486537746,7.36672780078754));
#76378=CARTESIAN_POINT('Ctrl Pts',(1.16965036346901,-1.56676341004483,7.37063499336015));
#76379=CARTESIAN_POINT('Ctrl Pts',(1.22318978220132,-1.52378566626619,7.37454218593276));
#76380=CARTESIAN_POINT('Ctrl Pts',(1.27669555134924,-1.48083493404745,7.37844692283049));
#76381=CARTESIAN_POINT('Ctrl Pts',(1.32797479604209,-1.4350317817024,7.38235165972821));
#76382=CARTESIAN_POINT('Ctrl Pts',(1.37671472845914,-1.38664074527027,7.38625639662593));
#76383=CARTESIAN_POINT('Ctrl Pts',(1.42544075489747,-1.33826351527342,7.39016001946408));
#76384=CARTESIAN_POINT('Ctrl Pts',(1.47162855829193,-1.28730021339475,7.39406364230224));
#76385=CARTESIAN_POINT('Ctrl Pts',(1.51500131607822,-1.23405308325098,7.39796726514039));
#76386=CARTESIAN_POINT('Ctrl Pts',(1.55837658389168,-1.18080287163973,7.4018711138853));
#76387=CARTESIAN_POINT('Ctrl Pts',(1.59893617391789,-1.12526895244265,7.40577496263022));
#76388=CARTESIAN_POINT('Ctrl Pts',(1.6364439274139,-1.06778615482229,7.40967881137514));
#76389=CARTESIAN_POINT('Ctrl Pts',(1.67399167770678,-1.01024205980162,7.4135868230312));
#76390=CARTESIAN_POINT('Ctrl Pts',(1.70848082731213,-0.950745351687654,
7.41749483468727));
#76391=CARTESIAN_POINT('Ctrl Pts',(1.73971946749999,-0.889658459410997,
7.42140284634334));
#76392=CARTESIAN_POINT('Ctrl Pts',(1.77097677780789,-0.828535057875143,
7.42531319366595));
#76393=CARTESIAN_POINT('Ctrl Pts',(1.79897951174431,-0.765820030051449,
7.42922354098856));
#76394=CARTESIAN_POINT('Ctrl Pts',(1.82358369848309,-0.70189635604321,7.43313388831117));
#76395=CARTESIAN_POINT('Ctrl Pts',(1.84823051104832,-0.637861936678382,
7.43705101016318));
#76396=CARTESIAN_POINT('Ctrl Pts',(1.86946687280628,-0.572615159524416,
7.44096813201518));
#76397=CARTESIAN_POINT('Ctrl Pts',(1.88719875594981,-0.506553901911217,
7.44488525386719));
#76398=CARTESIAN_POINT('Ctrl Pts',(1.89572236363867,-0.47479865974266,7.44676819036444));
#76399=CARTESIAN_POINT('Ctrl Pts',(1.90343696461329,-0.442855364101904,
7.44865112686169));
#76400=CARTESIAN_POINT('Ctrl Pts',(1.91033636421216,-0.410768761675791,
7.45053406335894));
#76401=CARTESIAN_POINT('Ctrl Pts',(1.92469152636594,-0.344008114725301,
7.45445177508964));
#76402=CARTESIAN_POINT('Ctrl Pts',(1.93557137089309,-0.276361376031788,
7.45836948682035));
#76403=CARTESIAN_POINT('Ctrl Pts',(1.94287393052167,-0.20822317378063,7.46228719855105));
#76404=CARTESIAN_POINT('Ctrl Pts',(1.95016547554831,-0.140187745791203,
7.46619900111601));
#76405=CARTESIAN_POINT('Ctrl Pts',(1.95389039210975,-0.0716628106656136,
7.47011080368096));
#76406=CARTESIAN_POINT('Ctrl Pts',(1.95399761386033,-0.00305369090163639,
7.47402260624592));
#76407=CARTESIAN_POINT('Ctrl Pts',(1.95410470923865,0.0654745656992405,
7.47792979833446));
#76408=CARTESIAN_POINT('Ctrl Pts',(1.95060257702726,0.134086320225401,7.48183699042299));
#76409=CARTESIAN_POINT('Ctrl Pts',(1.94349206121551,0.202372448698611,7.48574418251153));
#76410=CARTESIAN_POINT('Ctrl Pts',(1.93638601436886,0.270615659283433,7.4896489189266));
#76411=CARTESIAN_POINT('Ctrl Pts',(1.92567613344655,0.338533161531557,7.49355365534167));
#76412=CARTESIAN_POINT('Ctrl Pts',(1.91141526511457,0.405718725580928,7.49745839175673));
#76413=CARTESIAN_POINT('Ctrl Pts',(1.89715846554027,0.472885120967215,7.50136201411437));
#76414=CARTESIAN_POINT('Ctrl Pts',(1.8793527918653,0.539319511655636,7.50526563647201));
#76415=CARTESIAN_POINT('Ctrl Pts',(1.85810227093987,0.604625463182053,7.50916925882965));
#76416=CARTESIAN_POINT('Ctrl Pts',(1.83685052020874,0.669935194080809,7.51307310709691));
#76417=CARTESIAN_POINT('Ctrl Pts',(1.81215368109625,0.734115889098009,7.51697695536416));
#76418=CARTESIAN_POINT('Ctrl Pts',(1.78416520169937,0.796787633591946,7.52088080363141));
#76419=CARTESIAN_POINT('Ctrl Pts',(1.75614687642862,0.859526208904175,7.52478881481732));
#76420=CARTESIAN_POINT('Ctrl Pts',(1.72483010675834,0.920752172299416,7.52869682600323));
#76421=CARTESIAN_POINT('Ctrl Pts',(1.69041551486067,0.980107844636662,7.53260483718913));
#76422=CARTESIAN_POINT('Ctrl Pts',(1.65598035466613,1.03949899160902,7.53651518404517));
#76423=CARTESIAN_POINT('Ctrl Pts',(1.61844395645568,1.09701721080549,7.5404255309012));
#76424=CARTESIAN_POINT('Ctrl Pts',(1.5780501906774,1.15233397750089,7.54433587775724));
#76425=CARTESIAN_POINT('Ctrl Pts',(1.53758644410584,1.20774657856925,7.5482529991531));
#76426=CARTESIAN_POINT('Ctrl Pts',(1.49425576036724,1.2609497336927,7.55217012054896));
#76427=CARTESIAN_POINT('Ctrl Pts',(1.44834159271625,1.31164882144885,7.55608724194482));
#76428=CARTESIAN_POINT('Ctrl Pts',(1.42627088052338,1.33601962095484,7.55797018273142));
#76429=CARTESIAN_POINT('Ctrl Pts',(1.40360374362322,1.35981237217978,7.55985312351801));
#76430=CARTESIAN_POINT('Ctrl Pts',(1.38037443378564,1.38299762203373,7.5617360643046));
#76431=CARTESIAN_POINT('Ctrl Pts',(1.33204272412895,1.43123765895668,7.56565377636901));
#76432=CARTESIAN_POINT('Ctrl Pts',(1.28108314388008,1.47703693965468,7.56957148843341));
#76433=CARTESIAN_POINT('Ctrl Pts',(1.22777211348501,1.52009593031116,7.57348920049781));
#76434=CARTESIAN_POINT('Ctrl Pts',(1.17454149326189,1.56308997416738,7.57740100339297));
#76435=CARTESIAN_POINT('Ctrl Pts',(1.11896684151028,1.60335162427363,7.58131280628814));
#76436=CARTESIAN_POINT('Ctrl Pts',(1.06136114812037,1.64061833259921,7.58522460918331));
#76437=CARTESIAN_POINT('Ctrl Pts',(1.0038233492746,1.67784111807578,7.5891318015954));
#76438=CARTESIAN_POINT('Ctrl Pts',(0.944259674013049,1.71207570611015,7.59303899400749));
#76439=CARTESIAN_POINT('Ctrl Pts',(0.883014435422671,1.7431011177884,7.59694618641958));
#76440=CARTESIAN_POINT('Ctrl Pts',(0.821807689579798,1.77410702993714,7.6008509231539));
#76441=CARTESIAN_POINT('Ctrl Pts',(0.758921914777607,1.80190754488188,7.60475565988822));
#76442=CARTESIAN_POINT('Ctrl Pts',(0.694727169901249,1.82632695851564,7.60866039662254));
#76443=CARTESIAN_POINT('Ctrl Pts',(0.630550740456051,1.85073940503566,7.61256401929469));
#76444=CARTESIAN_POINT('Ctrl Pts',(0.565066541949429,1.87177249038891,7.61646764196684));
#76445=CARTESIAN_POINT('Ctrl Pts',(0.498664133081241,1.88929883353014,7.62037126463899));
#76446=CARTESIAN_POINT('Ctrl Pts',(0.43225788147548,1.9068261909288,7.62427511321556));
#76447=CARTESIAN_POINT('Ctrl Pts',(0.364933790374975,1.92084628012294,7.62817896179212));
#76448=CARTESIAN_POINT('Ctrl Pts',(0.297094313530838,1.93128220849974,7.63208281036869));
#76449=CARTESIAN_POINT('Ctrl Pts',(0.229182495367473,1.94172926533539,7.63599082185407));
#76450=CARTESIAN_POINT('Ctrl Pts',(0.160754681865166,1.94858445876277,7.63989883333945));
#76451=CARTESIAN_POINT('Ctrl Pts',(0.0922202003259246,1.95182259302731,
7.64380684482484));
#76452=CARTESIAN_POINT('Ctrl Pts',(0.0236447584190841,1.9550626625975,7.64771719197518));
#76453=CARTESIAN_POINT('Ctrl Pts',(-0.0450369863285532,1.95468137341821,
7.65162753912552));
#76454=CARTESIAN_POINT('Ctrl Pts',(-0.113416775426539,1.95070567617256,
7.65553788627586));
#76455=CARTESIAN_POINT('Ctrl Pts',(-0.181915029927715,1.94672309118152,
7.65945500795501));
#76456=CARTESIAN_POINT('Ctrl Pts',(-0.250109795935364,1.93913372386523,
7.66337212963417));
#76457=CARTESIAN_POINT('Ctrl Pts',(-0.31759986123396,1.92801616387005,7.66728925131333));
#76458=CARTESIAN_POINT('Ctrl Pts',(-0.350041949471986,1.92267201639057,
7.66917218929231));
#76459=CARTESIAN_POINT('Ctrl Pts',(-0.382321386102698,1.91651337360227,
7.67105512727128));
#76460=CARTESIAN_POINT('Ctrl Pts',(-0.414394857243163,1.90955306349167,
7.67293806525026));
#76461=CARTESIAN_POINT('Ctrl Pts',(-0.481128154164906,1.89507117472934,
7.67685577838726));
#76462=CARTESIAN_POINT('Ctrl Pts',(-0.547234011966056,1.87705809216585,
7.68077349152426));
#76463=CARTESIAN_POINT('Ctrl Pts',(-0.612310900416118,1.855583832984,7.68469120466126));
#76464=CARTESIAN_POINT('Ctrl Pts',(-0.677289632163757,1.83414196383368,
7.6886030086374));
#76465=CARTESIAN_POINT('Ctrl Pts',(-0.741242011283347,1.80924943185615,
7.69251481261354));
#76466=CARTESIAN_POINT('Ctrl Pts',(-0.803777777399279,1.78102703083335,
7.69642661658967));
#76467=CARTESIAN_POINT('Ctrl Pts',(-0.866239838478769,1.75283789290502,
7.70033381008971));
#76468=CARTESIAN_POINT('Ctrl Pts',(-0.927288156122975,1.72132688161915,
7.70424100358976));
#76469=CARTESIAN_POINT('Ctrl Pts',(-0.986550434686132,1.68666364157784,
7.7081481970898));
#76470=CARTESIAN_POINT('Ctrl Pts',(-1.04577546686266,1.65202218740894,7.71205293491579));
#76471=CARTESIAN_POINT('Ctrl Pts',(-1.10321626293826,1.61423268231066,7.71595767274178));
#76472=CARTESIAN_POINT('Ctrl Pts',(-1.15852462868117,1.57351094204621,7.71986241056777));
#76473=CARTESIAN_POINT('Ctrl Pts',(-1.21381721440313,1.53280082009495,7.72376603433364));
#76474=CARTESIAN_POINT('Ctrl Pts',(-1.26697818154531,1.48916041530356,7.7276696580995));
#76475=CARTESIAN_POINT('Ctrl Pts',(-1.31768938370035,1.44284811677577,7.73157328186537));
#76476=CARTESIAN_POINT('Ctrl Pts',(-1.36840352053983,1.39653313813045,7.73547713153604));
#76477=CARTESIAN_POINT('Ctrl Pts',(-1.41666724935367,1.34754629243511,7.73938098120671));
#76478=CARTESIAN_POINT('Ctrl Pts',(-1.46219787034241,1.296184164371,7.74328483087737));
#76479=CARTESIAN_POINT('Ctrl Pts',(-1.50777704327967,1.24476726588329,7.74719284344993));
#76480=CARTESIAN_POINT('Ctrl Pts',(-1.55061696493227,1.19097039895722,7.75110085602249));
#76481=CARTESIAN_POINT('Ctrl Pts',(-1.59047466056467,1.13512393777142,7.75500886859505));
#76482=CARTESIAN_POINT('Ctrl Pts',(-1.63035617754554,1.07924409939229,7.75891921683022));
#76483=CARTESIAN_POINT('Ctrl Pts',(-1.66725165695716,1.0213126439139,7.76282956506539));
#76484=CARTESIAN_POINT('Ctrl Pts',(-1.70096253063604,0.961687303322772,
7.76673991330056));
#76485=CARTESIAN_POINT('Ctrl Pts',(-1.73473180698456,0.901958664338918,
7.77065703604944));
#76486=CARTESIAN_POINT('Ctrl Pts',(-1.76530524686167,0.840530723436104,
7.77457415879833));
#76487=CARTESIAN_POINT('Ctrl Pts',(-1.79253150111232,0.777783271560927,
7.77849128154721));
#76488=CARTESIAN_POINT('Ctrl Pts',(-1.80561893432219,0.747621095084287,
7.78037420976345));
#76489=CARTESIAN_POINT('Ctrl Pts',(-1.81793368352772,0.717154282311143,
7.78225713797968));
#76490=CARTESIAN_POINT('Ctrl Pts',(-1.82946306033964,0.686426187475923,
7.78414006619591));
#76491=CARTESIAN_POINT('Ctrl Pts',(-1.85696340883929,0.613132259236415,
7.78863130479371));
#76492=CARTESIAN_POINT('Ctrl Pts',(-1.88008308402579,0.538109812614524,
7.79312254339151));
#76493=CARTESIAN_POINT('Ctrl Pts',(-1.89863218860916,0.461856917645722,
7.79761378198931));
#76494=CARTESIAN_POINT('Ctrl Pts',(-1.91702938031453,0.386228516257064,
7.80206823838136));
#76495=CARTESIAN_POINT('Ctrl Pts',(-1.93093045748714,0.309389931917262,
7.80652269477342));
#76496=CARTESIAN_POINT('Ctrl Pts',(-1.94019647443928,0.231848313716967,
7.81097715116548));
#76497=CARTESIAN_POINT('Ctrl Pts',(-1.94931671348173,0.155526621518631,
7.8153615276791));
#76498=CARTESIAN_POINT('Ctrl Pts',(-1.95394653914743,0.0785240591470384,
7.81974590419272));
#76499=CARTESIAN_POINT('Ctrl Pts',(-1.95399953930486,0.00134178850078647,
7.82413028070635));
#76500=CARTESIAN_POINT('',(-1.95399946858027,-0.00144110652225904,8.52413033454307));
#76501=CARTESIAN_POINT('Ctrl Pts',(-1.95179084094767,0.00133979406531506,
7.82413030787577));
#76502=CARTESIAN_POINT('Ctrl Pts',(-1.94915888327607,-0.416058890402282,
7.84786756096437));
#76503=CARTESIAN_POINT('Ctrl Pts',(-1.61328277704976,-1.48911958067226,
7.90867214770152));
#76504=CARTESIAN_POINT('Ctrl Pts',(0.153605637297869,-2.30486302861762,
8.00654406808722));
#76505=CARTESIAN_POINT('Ctrl Pts',(2.02039752512168,-1.11981505029072,8.11774606903288));
#76506=CARTESIAN_POINT('Ctrl Pts',(2.03594236675928,1.0912978005846,8.22894806997853));
#76507=CARTESIAN_POINT('Ctrl Pts',(0.185997657197315,2.30247329506165,8.34015007092419));
#76508=CARTESIAN_POINT('Ctrl Pts',(-1.60167333631625,1.50744019525351,8.43854415022327));
#76509=CARTESIAN_POINT('Ctrl Pts',(-1.94908776418844,0.42503214287857,8.4998708958738));
#76510=CARTESIAN_POINT('Ctrl Pts',(-1.95199070173634,-0.00143915622514865,
8.52413030787577));
#76511=CARTESIAN_POINT('',(0.0563173628514251,1.95318825376395,9.046));
#76512=CARTESIAN_POINT('Ctrl Pts',(-1.95399946858027,-0.00144110652225904,
8.52413033454307));
#76513=CARTESIAN_POINT('Ctrl Pts',(-1.95394108830595,-0.0805990474803556,
8.52862855434524));
#76514=CARTESIAN_POINT('Ctrl Pts',(-1.94906859332623,-0.15956158622964,
8.5331267741474));
#76515=CARTESIAN_POINT('Ctrl Pts',(-1.93947676251248,-0.237793792337245,
8.53762499394957));
#76516=CARTESIAN_POINT('Ctrl Pts',(-1.92979252801014,-0.316779654816663,
8.542166547721));
#76517=CARTESIAN_POINT('Ctrl Pts',(-1.91529770080219,-0.395020873365993,
8.54670810149244));
#76518=CARTESIAN_POINT('Ctrl Pts',(-1.89613939174724,-0.471986659837334,
8.55124965526387));
#76519=CARTESIAN_POINT('Ctrl Pts',(-1.88024369201979,-0.535845376570965,
8.55501779444775));
#76520=CARTESIAN_POINT('Ctrl Pts',(-1.86113855148694,-0.598826399085066,
8.55878593363163));
#76521=CARTESIAN_POINT('Ctrl Pts',(-1.83893271500536,-0.660637926312909,
8.56255407281551));
#76522=CARTESIAN_POINT('Ctrl Pts',(-1.81584482408034,-0.724904714899271,
8.56647188904098));
#76523=CARTESIAN_POINT('Ctrl Pts',(-1.78933801786655,-0.78808743988942,
8.57038970526645));
#76524=CARTESIAN_POINT('Ctrl Pts',(-1.75953424924607,-0.849797167405293,
8.57430752149192));
#76525=CARTESIAN_POINT('Ctrl Pts',(-1.72977543886373,-0.911413807343544,
8.57821942778979));
#76526=CARTESIAN_POINT('Ctrl Pts',(-1.69672974863648,-0.971561420181686,
8.58213133408766));
#76527=CARTESIAN_POINT('Ctrl Pts',(-1.66056799715565,-1.02986888817096,
8.58604324038552));
#76528=CARTESIAN_POINT('Ctrl Pts',(-1.6244488798736,-1.08810761247168,8.58995053460063));
#76529=CARTESIAN_POINT('Ctrl Pts',(-1.58522125557365,-1.1445100844651,8.59385782881573));
#76530=CARTESIAN_POINT('Ctrl Pts',(-1.54310202347784,-1.19872938778467,
8.59776512303083));
#76531=CARTESIAN_POINT('Ctrl Pts',(-1.50100927399538,-1.25291460052911,
8.60166996052113));
#76532=CARTESIAN_POINT('Ctrl Pts',(-1.45602882436296,-1.3049189798806,8.60557479801144));
#76533=CARTESIAN_POINT('Ctrl Pts',(-1.40842019527807,-1.35442554373908,
8.60947963550174));
#76534=CARTESIAN_POINT('Ctrl Pts',(-1.36082516356631,-1.40391796816034,
8.61338335774186));
#76535=CARTESIAN_POINT('Ctrl Pts',(-1.31060378335576,-1.45091363883351,
8.61728707998198));
#76536=CARTESIAN_POINT('Ctrl Pts',(-1.25805385227626,-1.49513093231759,
8.6211908022221));
#76537=CARTESIAN_POINT('Ctrl Pts',(-1.20550089809209,-1.53935076954442,
8.62509474903646));
#76538=CARTESIAN_POINT('Ctrl Pts',(-1.15061950517139,-1.58079159745433,
8.62899869585082));
#76539=CARTESIAN_POINT('Ctrl Pts',(-1.09374070200118,-1.61921193078175,
8.63290264266518));
#76540=CARTESIAN_POINT('Ctrl Pts',(-1.03680128579549,-1.65767320683119,
8.63681074973));
#76541=CARTESIAN_POINT('Ctrl Pts',(-0.977860619836667,-1.69310728857217,
8.64071885679481));
#76542=CARTESIAN_POINT('Ctrl Pts',(-0.917278035606657,-1.72531649426811,
8.64462696385963));
#76543=CARTESIAN_POINT('Ctrl Pts',(-0.856659265732519,-1.75754493834534,
8.64853740521529));
#76544=CARTESIAN_POINT('Ctrl Pts',(-0.794397071838185,-1.7865444651238,
8.65244784657095));
#76545=CARTESIAN_POINT('Ctrl Pts',(-0.730872100338047,-1.81216499606064,
8.6563582879266));
#76546=CARTESIAN_POINT('Ctrl Pts',(-0.667237127147759,-1.83782989225477,
8.66027550071636));
#76547=CARTESIAN_POINT('Ctrl Pts',(-0.602335477159023,-1.860103954783,8.66419271350611));
#76548=CARTESIAN_POINT('Ctrl Pts',(-0.536563490459429,-1.87888680359036,
8.66810992629587));
#76549=CARTESIAN_POINT('Ctrl Pts',(-0.504962931939731,-1.88791113967457,
8.66999197545097));
#76550=CARTESIAN_POINT('Ctrl Pts',(-0.473161624289845,-1.89613032872838,
8.67187402460607));
#76551=CARTESIAN_POINT('Ctrl Pts',(-0.441204145161111,-1.90353747068259,
8.67375607376116));
#76552=CARTESIAN_POINT('Ctrl Pts',(-0.374677067461068,-1.91895719469579,
8.67767400576925));
#76553=CARTESIAN_POINT('Ctrl Pts',(-0.307208562193932,-1.93091573611139,
8.68159193777734));
#76554=CARTESIAN_POINT('Ctrl Pts',(-0.239191629429316,-1.93930486628868,
8.68550986978543));
#76555=CARTESIAN_POINT('Ctrl Pts',(-0.171277246094544,-1.94768134813736,
8.68942189471013));
#76556=CARTESIAN_POINT('Ctrl Pts',(-0.102816560589667,-1.95249903956177,
8.69333391963483));
#76557=CARTESIAN_POINT('Ctrl Pts',(-0.0342140732766986,-1.95370043691192,
8.69724594455954));
#76558=CARTESIAN_POINT('Ctrl Pts',(0.034307597884766,-1.95490041897358,
8.70115336098079));
#76559=CARTESIAN_POINT('Ctrl Pts',(0.102970249570712,-1.95249255902204,
8.70506077740205));
#76560=CARTESIAN_POINT('Ctrl Pts',(0.171364756157416,-1.94647119689635,
8.70896819382331));
#76561=CARTESIAN_POINT('Ctrl Pts',(0.239716298321133,-1.94045361730178,
8.71287315566305));
#76562=CARTESIAN_POINT('Ctrl Pts',(0.307799540585961,-1.93082708140255,
8.71677811750279));
#76563=CARTESIAN_POINT('Ctrl Pts',(0.375207424648671,-1.91763797117405,
8.72068307934252));
#76564=CARTESIAN_POINT('Ctrl Pts',(0.442596090587038,-1.90445262118759,
8.72458692786973));
#76565=CARTESIAN_POINT('Ctrl Pts',(0.509309297998933,-1.88770680759631,
8.72849077639694));
#76566=CARTESIAN_POINT('Ctrl Pts',(0.574948968527382,-1.86749824192402,
8.73239462492414));
#76567=CARTESIAN_POINT('Ctrl Pts',(0.640592444226431,-1.8472885047492,8.73629869975976));
#76568=CARTESIAN_POINT('Ctrl Pts',(0.705161790076147,-1.82361576414533,
8.74020277459538));
#76569=CARTESIAN_POINT('Ctrl Pts',(0.768274658390884,-1.79662740969695,
8.744106849431));
#76570=CARTESIAN_POINT('Ctrl Pts',(0.831454808481008,-1.76961028418412,
8.74801508622428));
#76571=CARTESIAN_POINT('Ctrl Pts',(0.893174929122545,-1.73927068450819,
8.75192332301756));
#76572=CARTESIAN_POINT('Ctrl Pts',(0.953074153498006,-1.70580352266434,
8.75583155981085));
#76573=CARTESIAN_POINT('Ctrl Pts',(1.01300917198316,-1.67231636177584,8.75974213205769));
#76574=CARTESIAN_POINT('Ctrl Pts',(1.07112071237652,-1.63569818146923,8.76365270430453));
#76575=CARTESIAN_POINT('Ctrl Pts',(1.12707636833054,-1.59618760174073,8.76756327655137));
#76576=CARTESIAN_POINT('Ctrl Pts',(1.18312892098574,-1.55660860274752,8.77148062061679));
#76577=CARTESIAN_POINT('Ctrl Pts',(1.23701775189246,-1.51412751203579,8.7753979646822));
#76578=CARTESIAN_POINT('Ctrl Pts',(1.2884437217572,-1.46902306852699,8.77931530874762));
#76579=CARTESIAN_POINT('Ctrl Pts',(1.3131360224015,-1.44736606366267,8.78119623073402));
#76580=CARTESIAN_POINT('Ctrl Pts',(1.33726107095573,-1.42510479754797,8.78307715272041));
#76581=CARTESIAN_POINT('Ctrl Pts',(1.36078896807282,-1.40227293504914,8.78495807470681));
#76582=CARTESIAN_POINT('Ctrl Pts',(1.40978407058029,-1.35472727306327,8.78887495538142));
#76583=CARTESIAN_POINT('Ctrl Pts',(1.45638193160015,-1.30451597633669,8.79279183605603));
#76584=CARTESIAN_POINT('Ctrl Pts',(1.50027868844302,-1.25191048282363,8.79670871673064));
#76585=CARTESIAN_POINT('Ctrl Pts',(1.544109203753,-1.19938437259032,8.80061968671392));
#76586=CARTESIAN_POINT('Ctrl Pts',(1.58524639139948,-1.1444716106328,8.8045306566972));
#76587=CARTESIAN_POINT('Ctrl Pts',(1.62342277661471,-1.08748079908042,8.80844162668048));
#76588=CARTESIAN_POINT('Ctrl Pts',(1.66155417433965,-1.03055714615416,8.81234798793187));
#76589=CARTESIAN_POINT('Ctrl Pts',(1.6967314261284,-0.971560713876157,8.81625434918325));
#76590=CARTESIAN_POINT('Ctrl Pts',(1.72872811449635,-0.910832095476386,
8.82016071043464));
#76591=CARTESIAN_POINT('Ctrl Pts',(1.7607047013093,-0.850141629139377,8.82406461755906));
#76592=CARTESIAN_POINT('Ctrl Pts',(1.78950445936108,-0.787721569814372,
8.82796852468349));
#76593=CARTESIAN_POINT('Ctrl Pts',(1.81494582571252,-0.723938982048013,
8.83187243180792));
#76594=CARTESIAN_POINT('Ctrl Pts',(1.84037994989638,-0.66017455070387,8.83577522764181));
#76595=CARTESIAN_POINT('Ctrl Pts',(1.86245739786728,-0.595048817847414,
8.8396780234757));
#76596=CARTESIAN_POINT('Ctrl Pts',(1.88104461086103,-0.528949120379897,
8.8435808193096));
#76597=CARTESIAN_POINT('Ctrl Pts',(1.89963291875866,-0.462845529224006,
8.84748384504274));
#76598=CARTESIAN_POINT('Ctrl Pts',(1.91473045271517,-0.395768334100122,
8.85138687077587));
#76599=CARTESIAN_POINT('Ctrl Pts',(1.92625392995489,-0.32811857206403,8.85528989650902));
#76600=CARTESIAN_POINT('Ctrl Pts',(1.93778973221577,-0.260396454719598,
8.85919709675249));
#76601=CARTESIAN_POINT('Ctrl Pts',(1.94574376603604,-0.192101034489606,
8.86310429699595));
#76602=CARTESIAN_POINT('Ctrl Pts',(1.95008432939565,-0.123641045957689,
8.86701149723942));
#76603=CARTESIAN_POINT('Ctrl Pts',(1.95442749349116,-0.0551400382458394,
8.87092103856055));
#76604=CARTESIAN_POINT('Ctrl Pts',(1.95515287313671,0.0135252417277512,
8.87483057988169));
#76605=CARTESIAN_POINT('Ctrl Pts',(1.95228092335384,0.0819463013728634,
8.87874012120282));
#76606=CARTESIAN_POINT('Ctrl Pts',(1.94940398465482,0.150486216483694,8.8826564538592));
#76607=CARTESIAN_POINT('Ctrl Pts',(1.94291729095136,0.218780574760241,8.88657278651558));
#76608=CARTESIAN_POINT('Ctrl Pts',(1.93289304162917,0.286427110486277,8.89048911917197));
#76609=CARTESIAN_POINT('Ctrl Pts',(1.92805457950627,0.319078453278754,8.8923794379988));
#76610=CARTESIAN_POINT('Ctrl Pts',(1.92239271298801,0.351579039383104,8.89426975682563));
#76611=CARTESIAN_POINT('Ctrl Pts',(1.91591973560057,0.383884835251727,8.89616007565247));
#76612=CARTESIAN_POINT('Ctrl Pts',(1.90250125140227,0.450854760439052,8.9000787071862));
#76613=CARTESIAN_POINT('Ctrl Pts',(1.88554057463531,0.517253144766889,8.90399733871994));
#76614=CARTESIAN_POINT('Ctrl Pts',(1.86510139547736,0.582677255938815,8.90791597025368));
#76615=CARTESIAN_POINT('Ctrl Pts',(1.84469306081434,0.648002636449948,8.9118286882324));
#76616=CARTESIAN_POINT('Ctrl Pts',(1.82081678738595,0.712356196166194,8.91574140621112));
#76617=CARTESIAN_POINT('Ctrl Pts',(1.79358721358966,0.775345669522741,8.91965412418983));
#76618=CARTESIAN_POINT('Ctrl Pts',(1.76638980026698,0.838260746882122,8.92356222091138));
#76619=CARTESIAN_POINT('Ctrl Pts',(1.73584714655751,0.899814488352887,8.92747031763293));
#76620=CARTESIAN_POINT('Ctrl Pts',(1.70212301961931,0.959631817981274,8.93137841435447));
#76621=CARTESIAN_POINT('Ctrl Pts',(1.66842014542599,1.01941145108313,8.93528404821663));
#76622=CARTESIAN_POINT('Ctrl Pts',(1.63154001616097,1.07745641564978,8.93918968207879));
#76623=CARTESIAN_POINT('Ctrl Pts',(1.59169294757376,1.13341499930253,8.94309531594095));
#76624=CARTESIAN_POINT('Ctrl Pts',(1.55185733148111,1.18935749983053,8.94699982728012));
#76625=CARTESIAN_POINT('Ctrl Pts',(1.50905675398589,1.2432144094598,8.95090433861929));
#76626=CARTESIAN_POINT('Ctrl Pts',(1.463544578585,1.29466337960663,8.95480884995846));
#76627=CARTESIAN_POINT('Ctrl Pts',(1.41802988360337,1.34611519799864,8.95871357745366));
#76628=CARTESIAN_POINT('Ctrl Pts',(1.36980362041336,1.39515844560795,8.96261830494887));
#76629=CARTESIAN_POINT('Ctrl Pts',(1.31915791157833,1.44150560329133,8.96652303244408));
#76630=CARTESIAN_POINT('Ctrl Pts',(1.26845847522588,1.48790192837268,8.97043190227078));
#76631=CARTESIAN_POINT('Ctrl Pts',(1.21533483432683,1.53159612280881,8.97434077209748));
#76632=CARTESIAN_POINT('Ctrl Pts',(1.16011353387112,1.57233984511271,8.97824964192418));
#76633=CARTESIAN_POINT('Ctrl Pts',(1.10485938495347,1.61310780387248,8.98216083694714));
#76634=CARTESIAN_POINT('Ctrl Pts',(1.04750550368595,1.65092152669452,8.9860720319701));
#76635=CARTESIAN_POINT('Ctrl Pts',(0.988406507414003,1.68557663014817,8.98998322699307));
#76636=CARTESIAN_POINT('Ctrl Pts',(0.929205523574677,1.7202915381657,8.99390117159371));
#76637=CARTESIAN_POINT('Ctrl Pts',(0.868253850527651,1.7518367215787,8.99781911619435));
#76638=CARTESIAN_POINT('Ctrl Pts',(0.80592892480626,1.78005465313867,9.00173706079499));
#76639=CARTESIAN_POINT('Ctrl Pts',(0.7761021722743,1.79355886917842,9.0036120660627));
#76640=CARTESIAN_POINT('Ctrl Pts',(0.745961172374592,1.8063017746176,9.00548707133041));
#76641=CARTESIAN_POINT('Ctrl Pts',(0.715548514393166,1.81827014592159,9.00736207659812));
#76642=CARTESIAN_POINT('Ctrl Pts',(0.641982771868844,1.84722066127355,9.0118975616202));
#76643=CARTESIAN_POINT('Ctrl Pts',(0.566587126936113,1.87173065517956,9.01643304664227));
#76644=CARTESIAN_POINT('Ctrl Pts',(0.489867649121186,1.89159871176328,9.02096853166434));
#76645=CARTESIAN_POINT('Ctrl Pts',(0.413830713534296,1.91129001026686,9.02546366630681));
#76646=CARTESIAN_POINT('Ctrl Pts',(0.336493559382468,1.92642150295744,9.02995880094929));
#76647=CARTESIAN_POINT('Ctrl Pts',(0.258371108637887,1.93684288733527,9.03445393559177));
#76648=CARTESIAN_POINT('Ctrl Pts',(0.191483468276503,1.94576556965883,9.03830262372784));
#76649=CARTESIAN_POINT('Ctrl Pts',(0.124020571038654,1.95123612952076,9.04215131186392));
#76650=CARTESIAN_POINT('Ctrl Pts',(0.0563173628514251,1.95318825376395,
9.046));
#76651=CARTESIAN_POINT('',(1.57931773120857,1.15059615151895,9.04599749618701));
#76652=CARTESIAN_POINT('Origin',(0.,0.,9.046));
#76653=CARTESIAN_POINT('',(-1.95399928911013,-0.00166678046474256,8.62586971036475));
#76654=CARTESIAN_POINT('Ctrl Pts',(1.57931773120857,1.15059615151895,9.04599749618701));
#76655=CARTESIAN_POINT('Ctrl Pts',(1.62180406402798,1.09227906201092,9.04191010737179));
#76656=CARTESIAN_POINT('Ctrl Pts',(1.66100458682741,1.03167794467588,9.03782271855658));
#76657=CARTESIAN_POINT('Ctrl Pts',(1.69670153662891,0.969185170956047,9.03373532974136));
#76658=CARTESIAN_POINT('Ctrl Pts',(1.73250943747722,0.906498161070356,9.02963523675757));
#76659=CARTESIAN_POINT('Ctrl Pts',(1.76479179770922,0.841908110382457,9.02553514377379));
#76660=CARTESIAN_POINT('Ctrl Pts',(1.79337743867541,0.775830756318696,9.02143505079));
#76661=CARTESIAN_POINT('Ctrl Pts',(1.82201159399195,0.709641258542305,9.01732799930044));
#76662=CARTESIAN_POINT('Ctrl Pts',(1.84693637962684,0.641959817168832,9.01322094781089));
#76663=CARTESIAN_POINT('Ctrl Pts',(1.86803029404575,0.573217952028138,9.00911389632133));
#76664=CARTESIAN_POINT('Ctrl Pts',(1.88918515797369,0.504277461689376,9.00499497777065));
#76665=CARTESIAN_POINT('Ctrl Pts',(1.90648693114897,0.434270830524756,9.00087605921997));
#76666=CARTESIAN_POINT('Ctrl Pts',(1.91986493587304,0.363640795298363,8.99675714066929));
#76667=CARTESIAN_POINT('Ctrl Pts',(1.92479612494991,0.337606265830667,8.99523888988491));
#76668=CARTESIAN_POINT('Ctrl Pts',(1.92919470493638,0.311487076162819,8.99372063910054));
#76669=CARTESIAN_POINT('Ctrl Pts',(1.93305891880402,0.28530547914863,8.99220238831617));
#76670=CARTESIAN_POINT('Ctrl Pts',(1.94304653608131,0.217635370908566,8.98827825050065));
#76671=CARTESIAN_POINT('Ctrl Pts',(1.94949596281419,0.149308463994983,8.98435411268513));
#76672=CARTESIAN_POINT('Ctrl Pts',(1.95233174205724,0.0807265071444236,
8.98042997486961));
#76673=CARTESIAN_POINT('Ctrl Pts',(1.95516326323011,0.0122475296727868,
8.97651172935133));
#76674=CARTESIAN_POINT('Ctrl Pts',(1.95439188677818,-0.0564852517374681,
8.97259348383305));
#76675=CARTESIAN_POINT('Ctrl Pts',(1.94999366271435,-0.125062845697096,
8.96867523831477));
#76676=CARTESIAN_POINT('Ctrl Pts',(1.94560062510422,-0.193559571899607,
8.96476161325207));
#76677=CARTESIAN_POINT('Ctrl Pts',(1.93758926597383,-0.261900987293436,
8.96084798818938));
#76678=CARTESIAN_POINT('Ctrl Pts',(1.92598768409354,-0.32967778317626,8.95693436312668));
#76679=CARTESIAN_POINT('Ctrl Pts',(1.91439341097385,-0.39741188105631,8.95302320356816));
#76680=CARTESIAN_POINT('Ctrl Pts',(1.89921348478838,-0.464581583092648,
8.94911204400965));
#76681=CARTESIAN_POINT('Ctrl Pts',(1.88052769958456,-0.530783921285501,
8.94520088445114));
#76682=CARTESIAN_POINT('Ctrl Pts',(1.86184733350569,-0.596967059924311,
8.94129085918065));
#76683=CARTESIAN_POINT('Ctrl Pts',(1.83966326011543,-0.662182920259353,
8.93738083391015));
#76684=CARTESIAN_POINT('Ctrl Pts',(1.81410569602664,-0.726041681753669,
8.93347080863966));
#76685=CARTESIAN_POINT('Ctrl Pts',(1.78854685562587,-0.789903632272646,
8.92956058810752));
#76686=CARTESIAN_POINT('Ctrl Pts',(1.75961437449215,-0.852407895307245,
8.92565036757539));
#76687=CARTESIAN_POINT('Ctrl Pts',(1.72748670324951,-0.91318436807478,8.92174014704325));
#76688=CARTESIAN_POINT('Ctrl Pts',(1.69532565270611,-0.974023985044349,
8.91782586395624));
#76689=CARTESIAN_POINT('Ctrl Pts',(1.65996301624794,-1.03313179501728,8.91391158086924));
#76690=CARTESIAN_POINT('Ctrl Pts',(1.62162286507377,-1.09016296188687,8.90999729778223));
#76691=CARTESIAN_POINT('Ctrl Pts',(1.58326025666247,-1.14722753400914,8.90608072195561));
#76692=CARTESIAN_POINT('Ctrl Pts',(1.54191695645354,-1.2022126498828,8.90216414612899));
#76693=CARTESIAN_POINT('Ctrl Pts',(1.49785831467467,-1.25480535110428,8.89824757030237));
#76694=CARTESIAN_POINT('Ctrl Pts',(1.45372521165557,-1.30748693654013,8.89432437527276));
#76695=CARTESIAN_POINT('Ctrl Pts',(1.40686794153177,-1.35776767867277,8.89040118024314));
#76696=CARTESIAN_POINT('Ctrl Pts',(1.35758916629552,-1.40537100281635,8.88647798521353));
#76697=CARTESIAN_POINT('Ctrl Pts',(1.33503250184569,-1.42716075315522,8.88468219801245));
#76698=CARTESIAN_POINT('Ctrl Pts',(1.31196894094071,-1.44839007968357,8.88288641081136));
#76699=CARTESIAN_POINT('Ctrl Pts',(1.28842968577039,-1.46903537902448,8.88109062361028));
#76700=CARTESIAN_POINT('Ctrl Pts',(1.23698136643587,-1.51415855499429,8.87716568067094));
#76701=CARTESIAN_POINT('Ctrl Pts',(1.18306183933346,-1.55666164634484,8.87324073773159));
#76702=CARTESIAN_POINT('Ctrl Pts',(1.12696846101711,-1.59626379019031,8.86931579479225));
#76703=CARTESIAN_POINT('Ctrl Pts',(1.07095728038006,-1.63580790215363,8.86539660335533));
#76704=CARTESIAN_POINT('Ctrl Pts',(1.0127789686697,-1.67245922405922,8.8614774119184));
#76705=CARTESIAN_POINT('Ctrl Pts',(0.952764807998448,-1.70597632475943,
8.85755822048148));
#76706=CARTESIAN_POINT('Ctrl Pts',(0.892818261479659,-1.73945566386585,
8.85364344454923));
#76707=CARTESIAN_POINT('Ctrl Pts',(0.831040399816556,-1.76980755730277,
8.84972866861699));
#76708=CARTESIAN_POINT('Ctrl Pts',(0.767790916730049,-1.79683419051031,
8.84581389268475));
#76709=CARTESIAN_POINT('Ctrl Pts',(0.704579218113666,-1.82384467833665,
8.84190145539192));
#76710=CARTESIAN_POINT('Ctrl Pts',(0.639898091779485,-1.84753365493355,
8.83798901809909));
#76711=CARTESIAN_POINT('Ctrl Pts',(0.574129832569124,-1.8677502336646,8.83407658080627));
#76712=CARTESIAN_POINT('Ctrl Pts',(0.508378534791603,-1.88796159860184,
8.83016515251905));
#76713=CARTESIAN_POINT('Ctrl Pts',(0.441541128872701,-1.90470219988416,
8.82625372423183));
#76714=CARTESIAN_POINT('Ctrl Pts',(0.374016098171599,-1.91787068341651,
8.82234229594461));
#76715=CARTESIAN_POINT('Ctrl Pts',(0.306485558790806,-1.93104024123134,
8.81843054856379));
#76716=CARTESIAN_POINT('Ctrl Pts',(0.23826776453298,-1.94063701143983,8.81451880118296));
#76717=CARTESIAN_POINT('Ctrl Pts',(0.169770679301235,-1.94661087956725,
8.81060705380214));
#76718=CARTESIAN_POINT('Ctrl Pts',(0.101199340235007,-1.95259122362886,
8.80669106591617));
#76719=CARTESIAN_POINT('Ctrl Pts',(0.0323485949137836,-1.95494078529888,
8.80277507803019));
#76720=CARTESIAN_POINT('Ctrl Pts',(-0.0363701726601297,-1.95366148821659,
8.79885909014422));
#76721=CARTESIAN_POINT('Ctrl Pts',(-0.105131003167084,-1.9523814080733,
8.79494070527207));
#76722=CARTESIAN_POINT('Ctrl Pts',(-0.173759206487808,-1.94746808317336,
8.79102232039991));
#76723=CARTESIAN_POINT('Ctrl Pts',(-0.241847906718193,-1.93897539695996,
8.78710393552776));
#76724=CARTESIAN_POINT('Ctrl Pts',(-0.310054104760477,-1.93046805527445,
8.78317878886331));
#76725=CARTESIAN_POINT('Ctrl Pts',(-0.377718459628762,-1.91836911046163,
8.77925364219886));
#76726=CARTESIAN_POINT('Ctrl Pts',(-0.444444523564576,-1.90278350462512,
8.77532849553441));
#76727=CARTESIAN_POINT('Ctrl Pts',(-0.474758481769812,-1.89570289210187,
8.77354528332441));
#76728=CARTESIAN_POINT('Ctrl Pts',(-0.504878998460603,-1.88790333932249,
8.77176207111441));
#76729=CARTESIAN_POINT('Ctrl Pts',(-0.534770152701521,-1.87939801100767,
8.76997885890441));
#76730=CARTESIAN_POINT('Ctrl Pts',(-0.600358020416365,-1.86073542127,8.76606609308766));
#76731=CARTESIAN_POINT('Ctrl Pts',(-0.665101228545049,-1.83859735094002,
8.76215332727092));
#76732=CARTESIAN_POINT('Ctrl Pts',(-0.728604197596508,-1.81307802458823,
8.75824056145417));
#76733=CARTESIAN_POINT('Ctrl Pts',(-0.792010130299254,-1.78759769329899,
8.75433377457848));
#76734=CARTESIAN_POINT('Ctrl Pts',(-0.854179130749525,-1.75874654156522,
8.75042698770277));
#76735=CARTESIAN_POINT('Ctrl Pts',(-0.914729957549516,-1.72666878837879,
8.74652020082707));
#76736=CARTESIAN_POINT('Ctrl Pts',(-0.975208078883357,-1.69462955205696,
8.74261810496512));
#76737=CARTESIAN_POINT('Ctrl Pts',(-1.03407145124588,-1.65937163798819,
8.73871600910317));
#76738=CARTESIAN_POINT('Ctrl Pts',(-1.09095975959981,-1.62108692022789,
8.73481391324122));
#76739=CARTESIAN_POINT('Ctrl Pts',(-1.1478115877103,-1.5828267529572,8.73091431964047));
#76740=CARTESIAN_POINT('Ctrl Pts',(-1.20269045553328,-1.54154390667796,
8.72701472603972));
#76741=CARTESIAN_POINT('Ctrl Pts',(-1.25526294505716,-1.49747485413493,
8.72311513243897));
#76742=CARTESIAN_POINT('Ctrl Pts',(-1.3078198900863,-1.45341883181288,8.71921669185975));
#76743=CARTESIAN_POINT('Ctrl Pts',(-1.35807143246626,-1.40657855526525,
8.71531825128053));
#76744=CARTESIAN_POINT('Ctrl Pts',(-1.4057167804035,-1.35723112743998,8.71141981070131));
#76745=CARTESIAN_POINT('Ctrl Pts',(-1.45336450573064,-1.30788123729508,
8.70752117559915));
#76746=CARTESIAN_POINT('Ctrl Pts',(-1.4984054375671,-1.25602430428417,8.70362254049699));
#76747=CARTESIAN_POINT('Ctrl Pts',(-1.54057654137808,-1.2019733441951,8.69972390539483));
#76748=CARTESIAN_POINT('Ctrl Pts',(-1.58279244506785,-1.14786496382907,
8.69582112863252));
#76749=CARTESIAN_POINT('Ctrl Pts',(-1.6221321322931,-1.09155829461757,8.69191835187021));
#76750=CARTESIAN_POINT('Ctrl Pts',(-1.65837433329962,-1.03339758595278,
8.68801557510791));
#76751=CARTESIAN_POINT('Ctrl Pts',(-1.69463809005318,-0.975202285086398,
8.68411047709396));
#76752=CARTESIAN_POINT('Ctrl Pts',(-1.72780045588466,-0.915151182354898,
8.68020537908001));
#76753=CARTESIAN_POINT('Ctrl Pts',(-1.75768620406954,-0.853613031779404,
8.67630028106606));
#76754=CARTESIAN_POINT('Ctrl Pts',(-1.78762387246431,-0.791967971593504,
8.67238839876458));
#76755=CARTESIAN_POINT('Ctrl Pts',(-1.81427337050557,-0.728831161908087,
8.6684765164631));
#76756=CARTESIAN_POINT('Ctrl Pts',(-1.83750799297592,-0.664590381926799,
8.66456463416163));
#76757=CARTESIAN_POINT('Ctrl Pts',(-1.84878817131893,-0.633402121561991,
8.66266545417393));
#76758=CARTESIAN_POINT('Ctrl Pts',(-1.85926421818813,-0.601953867042989,
8.66076627418622));
#76759=CARTESIAN_POINT('Ctrl Pts',(-1.86892596382376,-0.570290927286619,
8.65886709419852));
#76760=CARTESIAN_POINT('Ctrl Pts',(-1.89335341938596,-0.490238617586443,
8.65406546346802));
#76761=CARTESIAN_POINT('Ctrl Pts',(-1.91265188010979,-0.408555106159593,
8.64926383273753));
#76762=CARTESIAN_POINT('Ctrl Pts',(-1.92664168382038,-0.325834040833328,
8.64446220200703));
#76763=CARTESIAN_POINT('Ctrl Pts',(-1.9404305170572,-0.244301304666876,
8.63972954908514));
#76764=CARTESIAN_POINT('Ctrl Pts',(-1.94906207863698,-0.161760582156713,
8.63499689616325));
#76765=CARTESIAN_POINT('Ctrl Pts',(-1.95241040069747,-0.0788011881149867,
8.63026424324136));
#76766=CARTESIAN_POINT('Ctrl Pts',(-1.95344676878525,-0.0531237093620654,
8.62879939894916));
#76767=CARTESIAN_POINT('Ctrl Pts',(-1.95397733306977,-0.0274062753568689,
8.62733455465696));
#76768=CARTESIAN_POINT('Ctrl Pts',(-1.95399928911013,-0.00166678046474256,
8.62586971036475));
#76769=CARTESIAN_POINT('',(-1.95391956053326,0.000983111039680522,7.92586964542572));
#76770=CARTESIAN_POINT('Ctrl Pts',(-1.95285709583883,-0.00166548583676096,
8.62586969212423));
#76771=CARTESIAN_POINT('Ctrl Pts',(-1.94908690947408,0.455599167126523,
8.59983157124703));
#76772=CARTESIAN_POINT('Ctrl Pts',(-1.56067665341042,1.56900554080129,8.53675619546789));
#76773=CARTESIAN_POINT('Ctrl Pts',(0.29402470952025,2.29055514341796,8.43664356478675));
#76774=CARTESIAN_POINT('Ctrl Pts',(2.08370935603324,0.995664930130409,8.32553180008087));
#76775=CARTESIAN_POINT('Ctrl Pts',(1.96685667089089,-1.21015215007575,8.21442003537499));
#76776=CARTESIAN_POINT('Ctrl Pts',(0.0505534074973701,-2.30879278288068,
8.10330827066911));
#76777=CARTESIAN_POINT('Ctrl Pts',(-1.64835232859496,-1.43126968529713,
8.00712482291886));
#76778=CARTESIAN_POINT('Ctrl Pts',(-1.94951883786448,-0.388037689702213,
7.94797863007056));
#76779=CARTESIAN_POINT('Ctrl Pts',(-1.95128693461656,0.000980964721550987,
7.92586969212423));
#76780=CARTESIAN_POINT('',(-1.95399967141271,0.00113318975355872,7.22586969217444));
#76781=CARTESIAN_POINT('Ctrl Pts',(-1.95399975265201,0.000983176418433057,
7.92586964400324));
#76782=CARTESIAN_POINT('Ctrl Pts',(-1.9539615535039,0.0769015208354533,
7.9215609870014));
#76783=CARTESIAN_POINT('Ctrl Pts',(-1.94949473679507,0.152668348582896,
7.91725232999955));
#76784=CARTESIAN_POINT('Ctrl Pts',(-1.94067686563194,0.227792236919909,
7.91294367299771));
#76785=CARTESIAN_POINT('Ctrl Pts',(-1.93182745458122,0.303184829454352,
7.90861960472992));
#76786=CARTESIAN_POINT('Ctrl Pts',(-1.91859594501537,0.377929584192814,
7.90429553646214));
#76787=CARTESIAN_POINT('Ctrl Pts',(-1.901110686543,0.45154640681996,7.89997146819435));
#76788=CARTESIAN_POINT('Ctrl Pts',(-1.88354178211006,0.525515397523577,
7.89562671445346));
#76789=CARTESIAN_POINT('Ctrl Pts',(-1.86167847786223,0.598345356879428,
7.89128196071257));
#76790=CARTESIAN_POINT('Ctrl Pts',(-1.8356992018065,0.66957034020854,7.88693720697168));
#76791=CARTESIAN_POINT('Ctrl Pts',(-1.82403434257111,0.701550808132062,
7.8849863850669));
#76792=CARTESIAN_POINT('Ctrl Pts',(-1.81154030758791,0.733208009754202,
7.88303556316212));
#76793=CARTESIAN_POINT('Ctrl Pts',(-1.79823626484276,0.764501364161226,
7.88108474125734));
#76794=CARTESIAN_POINT('Ctrl Pts',(-1.77151579091149,0.827352429560838,
7.87716661750731));
#76795=CARTESIAN_POINT('Ctrl Pts',(-1.74144327543005,0.888925511096836,
7.87324849375727));
#76796=CARTESIAN_POINT('Ctrl Pts',(-1.70816278471269,0.948839238713599,
7.86933037000724));
#76797=CARTESIAN_POINT('Ctrl Pts',(-1.67493240665714,1.0086627502216,7.86541814603831));
#76798=CARTESIAN_POINT('Ctrl Pts',(-1.63850387705473,1.06683144011301,7.86150592206939));
#76799=CARTESIAN_POINT('Ctrl Pts',(-1.59906902607522,1.12298452787509,7.85759369810046));
#76800=CARTESIAN_POINT('Ctrl Pts',(-1.55968054453133,1.17907158807721,7.85368607431673));
#76801=CARTESIAN_POINT('Ctrl Pts',(-1.51729304348515,1.23314735246802,7.84977845053299));
#76802=CARTESIAN_POINT('Ctrl Pts',(-1.47214297123592,1.28487784331457,7.84587082674926));
#76803=CARTESIAN_POINT('Ctrl Pts',(-1.42702119475532,1.3365759144123,7.84196565189225));
#76804=CARTESIAN_POINT('Ctrl Pts',(-1.37914060416938,1.3859312578222,7.83806047703524));
#76805=CARTESIAN_POINT('Ctrl Pts',(-1.32877848390436,1.43264222355508,7.83415530217822));
#76806=CARTESIAN_POINT('Ctrl Pts',(-1.27843065262459,1.47933993622599,7.83025123531638));
#76807=CARTESIAN_POINT('Ctrl Pts',(-1.22560304983721,1.52339442631165,7.82634716845454));
#76808=CARTESIAN_POINT('Ctrl Pts',(-1.17060914865412,1.56454153702843,7.8224431015927));
#76809=CARTESIAN_POINT('Ctrl Pts',(-1.11561198939385,1.60569108547847,7.81853880343701));
#76810=CARTESIAN_POINT('Ctrl Pts',(-1.0584486723113,1.64393261997036,7.81463450528131));
#76811=CARTESIAN_POINT('Ctrl Pts',(-0.999463548610668,1.67904395862603,
7.81073020712562));
#76812=CARTESIAN_POINT('Ctrl Pts',(-0.940415592690584,1.71419269863304,
7.80682175002775));
#76813=CARTESIAN_POINT('Ctrl Pts',(-0.879542380735666,1.74620433639348,
7.80291329292989));
#76814=CARTESIAN_POINT('Ctrl Pts',(-0.817214011371724,1.77490204225972,
7.79900483583202));
#76815=CARTESIAN_POINT('Ctrl Pts',(-0.754848332138476,1.80361692662215,
7.795094039125));
#76816=CARTESIAN_POINT('Ctrl Pts',(-0.691026219011583,1.82901374922341,
7.79118324241799));
#76817=CARTESIAN_POINT('Ctrl Pts',(-0.626136327081129,1.85096442426897,
7.78727244571097));
#76818=CARTESIAN_POINT('Ctrl Pts',(-0.561134388038692,1.87295300213224,
7.78335489612667));
#76819=CARTESIAN_POINT('Ctrl Pts',(-0.495061463692303,1.89148342333278,
7.77943734654238));
#76820=CARTESIAN_POINT('Ctrl Pts',(-0.4283190278697,1.90647811693834,7.77551979695809));
#76821=CARTESIAN_POINT('Ctrl Pts',(-0.396819038991215,1.91355506395098,
7.77367085682255));
#76822=CARTESIAN_POINT('Ctrl Pts',(-0.365170027134055,1.91984517650397,
7.771821916687));
#76823=CARTESIAN_POINT('Ctrl Pts',(-0.333414556241065,1.92534431561905,
7.76997297655146));
#76824=CARTESIAN_POINT('Ctrl Pts',(-0.266121357066562,1.93699757262809,
7.76605487698298));
#76825=CARTESIAN_POINT('Ctrl Pts',(-0.198083069845987,1.94514171224713,
7.7621367774145));
#76826=CARTESIAN_POINT('Ctrl Pts',(-0.129698212493694,1.94969084053753,
7.75821867784602));
#76827=CARTESIAN_POINT('Ctrl Pts',(-0.0614163370318766,1.95423311822022,
7.75430647860864));
#76828=CARTESIAN_POINT('Ctrl Pts',(0.00721058591247044,1.95519109663471,
7.75039427937127));
#76829=CARTESIAN_POINT('Ctrl Pts',(0.0757754195150875,1.95253017538713,
7.74648208013389));
#76830=CARTESIAN_POINT('Ctrl Pts',(0.144259618546025,1.94987238347327,7.74257448177561));
#76831=CARTESIAN_POINT('Ctrl Pts',(0.212681384064886,1.94360416326027,7.73866688341733));
#76832=CARTESIAN_POINT('Ctrl Pts',(0.28063188646454,1.93374293645752,7.73475928505905));
#76833=CARTESIAN_POINT('Ctrl Pts',(0.348539796439634,1.92388789082406,7.73085413604378));
#76834=CARTESIAN_POINT('Ctrl Pts',(0.415976543572401,1.91044437663898,7.72694898702851));
#76835=CARTESIAN_POINT('Ctrl Pts',(0.482538298520567,1.89348165833759,7.72304383801324));
#76836=CARTESIAN_POINT('Ctrl Pts',(0.549081161686835,1.87652375445215,7.71913979737055));
#76837=CARTESIAN_POINT('Ctrl Pts',(0.61474904924555,1.85604875071694,7.71523575672785));
#76838=CARTESIAN_POINT('Ctrl Pts',(0.679149992795631,1.83217665286012,7.71133171608516));
#76839=CARTESIAN_POINT('Ctrl Pts',(0.743554746171386,1.8083031427797,7.70742744448755));
#76840=CARTESIAN_POINT('Ctrl Pts',(0.806691946412121,1.78103231296019,7.70352317288994));
#76841=CARTESIAN_POINT('Ctrl Pts',(0.868188132147625,1.75053288092455,7.69961890129233));
#76842=CARTESIAN_POINT('Ctrl Pts',(0.929749820141615,1.72000096261912,7.69571047108546));
#76843=CARTESIAN_POINT('Ctrl Pts',(0.989666563819558,1.68623379803899,7.6918020408786));
#76844=CARTESIAN_POINT('Ctrl Pts',(1.04758902961708,1.64944633893496,7.68789361067173));
#76845=CARTESIAN_POINT('Ctrl Pts',(1.10554616473901,1.61263686080367,7.68398284108527));
#76846=CARTESIAN_POINT('Ctrl Pts',(1.16150624557331,1.57280377560179,7.6800720714988));
#76847=CARTESIAN_POINT('Ctrl Pts',(1.21515081690597,1.53020406880022,7.67616130191233));
#76848=CARTESIAN_POINT('Ctrl Pts',(1.26888801742229,1.48753080420954,7.67224377951966));
#76849=CARTESIAN_POINT('Ctrl Pts',(1.32030136025814,1.44208170913874,7.66832625712699));
#76850=CARTESIAN_POINT('Ctrl Pts',(1.36910786927658,1.39415194375826,7.66440873473432));
#76851=CARTESIAN_POINT('Ctrl Pts',(1.39214583381642,1.37152782542968,7.66255956043807));
#76852=CARTESIAN_POINT('Ctrl Pts',(1.41460354007924,1.34835148953263,7.66071038614182));
#76853=CARTESIAN_POINT('Ctrl Pts',(1.43645440818334,1.32465645856224,7.65886121184558));
#76854=CARTESIAN_POINT('Ctrl Pts',(1.48275310772801,1.27445025556959,7.65494308993208));
#76855=CARTESIAN_POINT('Ctrl Pts',(1.52650824377156,1.22171429595432,7.65102496801858));
#76856=CARTESIAN_POINT('Ctrl Pts',(1.56743145063378,1.16673675161285,7.64710684610508));
#76857=CARTESIAN_POINT('Ctrl Pts',(1.60829303453319,1.11184199352957,7.64319462417595));
#76858=CARTESIAN_POINT('Ctrl Pts',(1.64633086118598,1.05471274113225,7.63928240224682));
#76859=CARTESIAN_POINT('Ctrl Pts',(1.6812949773209,0.995672234842132,7.6353701803177));
#76860=CARTESIAN_POINT('Ctrl Pts',(1.71621797829565,0.936701155728806,7.63146255886611));
#76861=CARTESIAN_POINT('Ctrl Pts',(1.74807419765634,0.875823707500208,7.62755493741453));
#76862=CARTESIAN_POINT('Ctrl Pts',(1.7766564641253,0.813392776266045,7.62364731596295));
#76863=CARTESIAN_POINT('Ctrl Pts',(1.80522081661906,0.751000973704732,7.61974214361854));
#76864=CARTESIAN_POINT('Ctrl Pts',(1.8305150823525,0.687058065777789,7.61583697127413));
#76865=CARTESIAN_POINT('Ctrl Pts',(1.85237835253044,0.62194086461384,7.61193179892972));
#76866=CARTESIAN_POINT('Ctrl Pts',(1.87423541855999,0.556842141782514,7.60802773475753));
#76867=CARTESIAN_POINT('Ctrl Pts',(1.89266326534007,0.490570253310812,7.60412367058535));
#76868=CARTESIAN_POINT('Ctrl Pts',(1.90755004342891,0.423519576660118,7.60021960641316));
#76869=CARTESIAN_POINT('Ctrl Pts',(1.92243770281272,0.356464930619655,7.59631531112097));
#76870=CARTESIAN_POINT('Ctrl Pts',(1.93378377320702,0.288631885607086,7.59241101582878));
#76871=CARTESIAN_POINT('Ctrl Pts',(1.94152736539113,0.220425700491966,7.5885067205366));
#76872=CARTESIAN_POINT('Ctrl Pts',(1.94927920573602,0.152146864910871,7.58459826654719));
#76873=CARTESIAN_POINT('Ctrl Pts',(1.95342085438517,0.0834945857094849,
7.58068981255779));
#76874=CARTESIAN_POINT('Ctrl Pts',(1.95394335056589,0.0148789374400819,
7.57678135856838));
#76875=CARTESIAN_POINT('Ctrl Pts',(1.95446615949465,-0.053777781770528,
7.57287056511432));
#76876=CARTESIAN_POINT('Ctrl Pts',(1.95136552682704,-0.122397334968288,
7.56895977166026));
#76877=CARTESIAN_POINT('Ctrl Pts',(1.94468455410621,-0.190572781426713,
7.5650489782062));
#76878=CARTESIAN_POINT('Ctrl Pts',(1.93799204548633,-0.2588659450353,7.561131432065));
#76879=CARTESIAN_POINT('Ctrl Pts',(1.92770693201672,-0.326712985370813,
7.5572138859238));
#76880=CARTESIAN_POINT('Ctrl Pts',(1.91392363193798,-0.393716053913668,
7.5532963397826));
#76881=CARTESIAN_POINT('Ctrl Pts',(1.90741832793335,-0.425339491524659,
7.5514473755683));
#76882=CARTESIAN_POINT('Ctrl Pts',(1.90013450933198,-0.456775136292088,
7.54959841135399));
#76883=CARTESIAN_POINT('Ctrl Pts',(1.89208591038853,-0.487982487092733,
7.54774944713969));
#76884=CARTESIAN_POINT('Ctrl Pts',(1.87503022978535,-0.5541135754308,7.54383133129028));
#76885=CARTESIAN_POINT('Ctrl Pts',(1.85446950223503,-0.619480500000784,
7.53991321544087));
#76886=CARTESIAN_POINT('Ctrl Pts',(1.83048934905426,-0.683684680974283,
7.53599509959146));
#76887=CARTESIAN_POINT('Ctrl Pts',(1.80654530599257,-0.747792181138338,
7.53208288377233));
#76888=CARTESIAN_POINT('Ctrl Pts',(1.77919222713191,-0.810739955536902,
7.5281706679532));
#76889=CARTESIAN_POINT('Ctrl Pts',(1.74856603272248,-0.872142665628258,
7.52425845213407));
#76890=CARTESIAN_POINT('Ctrl Pts',(1.71797585275431,-0.933473170068925,
7.52035083682994));
#76891=CARTESIAN_POINT('Ctrl Pts',(1.68412041986387,-0.993261780504505,
7.51644322152581));
#76892=CARTESIAN_POINT('Ctrl Pts',(1.64718376858347,-1.05114301239895,7.51253560622168));
#76893=CARTESIAN_POINT('Ctrl Pts',(1.61027026762216,-1.10898796680369,7.50863044004431));
#76894=CARTESIAN_POINT('Ctrl Pts',(1.57027964312152,-1.16492750037259,7.50472527386694));
#76895=CARTESIAN_POINT('Ctrl Pts',(1.52744112751909,-1.21862200946938,7.50082010768957));
#76896=CARTESIAN_POINT('Ctrl Pts',(1.48461476834817,-1.27230128149243,7.49691604969451));
#76897=CARTESIAN_POINT('Ctrl Pts',(1.43894242902308,-1.32373640943104,7.49301199169945));
#76898=CARTESIAN_POINT('Ctrl Pts',(1.39069471413912,-1.37261947096255,7.48910793370439));
#76899=CARTESIAN_POINT('Ctrl Pts',(1.34244414300075,-1.42150542636086,7.48520364458994));
#76900=CARTESIAN_POINT('Ctrl Pts',(1.29161824096721,-1.46783866712546,7.48129935547548));
#76901=CARTESIAN_POINT('Ctrl Pts',(1.2385244013895,-1.51134817535959,7.47739506636102));
#76902=CARTESIAN_POINT('Ctrl Pts',(1.18537400774783,-1.55490402869763,7.47348661850765));
#76903=CARTESIAN_POINT('Ctrl Pts',(1.12995123666793,-1.59562983457411,7.46957817065429));
#76904=CARTESIAN_POINT('Ctrl Pts',(1.07259570016622,-1.63329558377684,7.46566972280092));
#76905=CARTESIAN_POINT('Ctrl Pts',(1.01520583236305,-1.67098387856574,7.46175893546806));
#76906=CARTESIAN_POINT('Ctrl Pts',(0.955881321579679,-1.70560822336799,
7.4578481481352));
#76907=CARTESIAN_POINT('Ctrl Pts',(0.89498739328095,-1.73698404306665,7.45393736080234));
#76908=CARTESIAN_POINT('Ctrl Pts',(0.833988319154388,-1.76841403953841,
7.4500198206949));
#76909=CARTESIAN_POINT('Ctrl Pts',(0.771414867231583,-1.79658411394221,
7.44610228058745));
#76910=CARTESIAN_POINT('Ctrl Pts',(0.70765246667827,-1.82135773158492,7.44218474048));
#76911=CARTESIAN_POINT('Ctrl Pts',(0.67755758338143,-1.83305050232956,7.44033572113127));
#76912=CARTESIAN_POINT('Ctrl Pts',(0.647198058887002,-1.84398736789094,
7.43848670178255));
#76913=CARTESIAN_POINT('Ctrl Pts',(0.616615370520906,-1.85415789102152,
7.43663768243382));
#76914=CARTESIAN_POINT('Ctrl Pts',(0.551809973377996,-1.87570945583945,
7.43271956929136));
#76915=CARTESIAN_POINT('Ctrl Pts',(0.485744862813765,-1.89390209508338,
7.42880145614889));
#76916=CARTESIAN_POINT('Ctrl Pts',(0.418801309825052,-1.9085914866437,7.42488334300642));
#76917=CARTESIAN_POINT('Ctrl Pts',(0.351958563940618,-1.92325875814974,
7.42097112996371));
#76918=CARTESIAN_POINT('Ctrl Pts',(0.284240477515498,-1.93443314714333,
7.41705891692099));
#76919=CARTESIAN_POINT('Ctrl Pts',(0.216044487830142,-1.94201976799368,
7.41314670387827));
#76920=CARTESIAN_POINT('Ctrl Pts',(0.147928693872118,-1.94959746728456,
7.40923909143995));
#76921=CARTESIAN_POINT('Ctrl Pts',(0.0793365993349622,-1.95359572344296,
7.40533147900164));
#76922=CARTESIAN_POINT('Ctrl Pts',(0.0106750676280779,-1.95397083983644,
7.40142386656333));
#76923=CARTESIAN_POINT('Ctrl Pts',(-0.0579434289782319,-1.95434572111761,
7.39751870330565));
#76924=CARTESIAN_POINT('Ctrl Pts',(-0.126630785652382,-1.95110196465935,
7.39361354004798));
#76925=CARTESIAN_POINT('Ctrl Pts',(-0.194977357877224,-1.94424788283676,
7.38970837679031));
#76926=CARTESIAN_POINT('Ctrl Pts',(-0.263304534281484,-1.93739574610866,
7.38580432176445));
#76927=CARTESIAN_POINT('Ctrl Pts',(-0.331290629025947,-1.9269353670041,
7.38190026673859));
#76928=CARTESIAN_POINT('Ctrl Pts',(-0.398530164639113,-1.91292700014212,
7.37799621171274));
#76929=CARTESIAN_POINT('Ctrl Pts',(-0.465773680043226,-1.89891780414932,
7.37409192561267));
#76930=CARTESIAN_POINT('Ctrl Pts',(-0.532270067571575,-1.88136030630986,
7.37018763951259));
#76931=CARTESIAN_POINT('Ctrl Pts',(-0.597624891061796,-1.86036568705816,
7.36628335341252));
#76932=CARTESIAN_POINT('Ctrl Pts',(-0.663049327921038,-1.83934870516972,
7.36237490862156));
#76933=CARTESIAN_POINT('Ctrl Pts',(-0.727329304875256,-1.81488744620426,
7.3584664638306));
#76934=CARTESIAN_POINT('Ctrl Pts',(-0.790087354245672,-1.78714240413602,
7.35455801903964));
#76935=CARTESIAN_POINT('Ctrl Pts',(-0.852882968216514,-1.75938075493245,
7.3506472348011));
#76936=CARTESIAN_POINT('Ctrl Pts',(-0.914154402787626,-1.72833163319366,
7.34673645056256));
#76937=CARTESIAN_POINT('Ctrl Pts',(-0.973548459849918,-1.69420169883159,
7.34282566632402));
#76938=CARTESIAN_POINT('Ctrl Pts',(-1.03304507272848,-1.66001283225558,
7.33890812932788));
#76939=CARTESIAN_POINT('Ctrl Pts',(-1.09065742549882,-1.62273280298025,
7.33499059233174));
#76940=CARTESIAN_POINT('Ctrl Pts',(-1.14606171403452,-1.58261130655138,
7.33107305533561));
#76941=CARTESIAN_POINT('Ctrl Pts',(-1.17221209141589,-1.56367428379647,
7.32922400946638));
#76942=CARTESIAN_POINT('Ctrl Pts',(-1.19787105135633,-1.54410482632948,
7.32737496359715));
#76943=CARTESIAN_POINT('Ctrl Pts',(-1.22300732171854,-1.52393211496537,
7.32552591772793));
#76944=CARTESIAN_POINT('Ctrl Pts',(-1.27559540575662,-1.48172839002112,
7.32165749261314));
#76945=CARTESIAN_POINT('Ctrl Pts',(-1.3261134392786,-1.43670517168706,7.31778906749836));
#76946=CARTESIAN_POINT('Ctrl Pts',(-1.3742376675258,-1.38909568898375,7.31392064238358));
#76947=CARTESIAN_POINT('Ctrl Pts',(-1.42227925837674,-1.34156795977201,
7.31005886000553));
#76948=CARTESIAN_POINT('Ctrl Pts',(-1.46793484780101,-1.2914631345989,7.30619707762749));
#76949=CARTESIAN_POINT('Ctrl Pts',(-1.51091317412696,-1.23905503519803,
7.30233529524944));
#76950=CARTESIAN_POINT('Ctrl Pts',(-1.55385038440043,-1.18669707302562,
7.29847720732069));
#76951=CARTESIAN_POINT('Ctrl Pts',(-1.59411508796571,-1.13204059173095,
7.29461911939193));
#76952=CARTESIAN_POINT('Ctrl Pts',(-1.63145346495995,-1.07539555126017,
7.29076103146317));
#76953=CARTESIAN_POINT('Ctrl Pts',(-1.66876970881202,-1.01878408837992,
7.28690523050068));
#76954=CARTESIAN_POINT('Ctrl Pts',(-1.70316278757363,-0.960186824623716,
7.28304942953819));
#76955=CARTESIAN_POINT('Ctrl Pts',(-1.73442094909542,-0.899944426805872,
7.2791936285757));
#76956=CARTESIAN_POINT('Ctrl Pts',(-1.76567195409799,-0.839715821413957,
7.27533871039429));
#76957=CARTESIAN_POINT('Ctrl Pts',(-1.79378923447468,-0.777843278568951,
7.27148379221288));
#76958=CARTESIAN_POINT('Ctrl Pts',(-1.81860692347361,-0.714692142040087,
7.26762887403147));
#76959=CARTESIAN_POINT('Ctrl Pts',(-1.84344269671115,-0.651494988324808,
7.26377114683508));
#76960=CARTESIAN_POINT('Ctrl Pts',(-1.86497388998003,-0.587017851092827,
7.25991341963869));
#76961=CARTESIAN_POINT('Ctrl Pts',(-1.8830832601559,-0.521644932229409,
7.2560556924423));
#76962=CARTESIAN_POINT('Ctrl Pts',(-1.90119957869136,-0.456246930519752,
7.25219648507982));
#76963=CARTESIAN_POINT('Ctrl Pts',(-1.91589134940438,-0.389952956733717,
7.24833727771733));
#76964=CARTESIAN_POINT('Ctrl Pts',(-1.92709227518885,-0.323158417664546,
7.24447807035485));
#76965=CARTESIAN_POINT('Ctrl Pts',(-1.9383106063023,-0.256260085306467,
7.24061286609755));
#76966=CARTESIAN_POINT('Ctrl Pts',(-1.94602720593144,-0.188860137495797,
7.23674766184025));
#76967=CARTESIAN_POINT('Ctrl Pts',(-1.95022767276933,-0.121359072033122,
7.23288245758296));
#76968=CARTESIAN_POINT('Ctrl Pts',(-1.95276802049565,-0.0805359481304121,
7.23054486911345));
#76969=CARTESIAN_POINT('Ctrl Pts',(-1.95402333795018,-0.039675868301506,
7.22820728064394));
#76970=CARTESIAN_POINT('Ctrl Pts',(-1.95399967141271,0.00113318975355588,
7.22586969217444));
#76971=CARTESIAN_POINT('',(-1.9539992470135,-0.00171542142396889,6.52586969212423));
#76972=CARTESIAN_POINT('Ctrl Pts',(-1.9539996714122,0.00113319063008382,
7.22586969212423));
#76973=CARTESIAN_POINT('Ctrl Pts',(-1.95396101146291,0.0677958740412391,
7.22205117909017));
#76974=CARTESIAN_POINT('Ctrl Pts',(-1.95051120810791,0.134358173529546,
7.21823266605611));
#76975=CARTESIAN_POINT('Ctrl Pts',(-1.94367936074665,0.200565556882252,
7.21441415302205));
#76976=CARTESIAN_POINT('Ctrl Pts',(-1.93666931122138,0.268499896117147,
7.21049603775012));
#76977=CARTESIAN_POINT('Ctrl Pts',(-1.92607947596587,0.336200944680773,
7.20657792247819));
#76978=CARTESIAN_POINT('Ctrl Pts',(-1.91193512166022,0.40326181391515,7.20265980720626));
#76979=CARTESIAN_POINT('Ctrl Pts',(-1.89781206650137,0.470221700151785,
7.19874759199245));
#76980=CARTESIAN_POINT('Ctrl Pts',(-1.8801452158854,0.536542842854362,7.19483537677863));
#76981=CARTESIAN_POINT('Ctrl Pts',(-1.85901154704416,0.601823950966119,
7.19092316156481));
#76982=CARTESIAN_POINT('Ctrl Pts',(-1.83790273025389,0.667028292027257,
7.18701554690439));
#76983=CARTESIAN_POINT('Ctrl Pts',(-1.81333534258699,0.7311945616895,7.18310793224396));
#76984=CARTESIAN_POINT('Ctrl Pts',(-1.78543689703329,0.793933930948994,
7.17920031758354));
#76985=CARTESIAN_POINT('Ctrl Pts',(-1.75755593720705,0.856633977461658,
7.17529515207336));
#76986=CARTESIAN_POINT('Ctrl Pts',(-1.72634826040549,0.9179084491972,7.17138998656319));
#76987=CARTESIAN_POINT('Ctrl Pts',(-1.69198992972671,0.977387373411085,
7.16748482105301));
#76988=CARTESIAN_POINT('Ctrl Pts',(-1.65764134922827,1.03684941874213,7.16358076374767));
#76989=CARTESIAN_POINT('Ctrl Pts',(-1.62014413569726,1.09451650234945,7.15967670644233));
#76990=CARTESIAN_POINT('Ctrl Pts',(-1.57971998372168,1.15004381352641,7.15577264913698));
#76991=CARTESIAN_POINT('Ctrl Pts',(-1.53929343886796,1.20557441160199,7.15186836073382));
#76992=CARTESIAN_POINT('Ctrl Pts',(-1.49593990316492,1.25896458962648,7.14796407233065));
#76993=CARTESIAN_POINT('Ctrl Pts',(-1.44992294884486,1.30990054676416,7.14405978392749));
#76994=CARTESIAN_POINT('Ctrl Pts',(-1.40385697888034,1.36089075909542,7.14015133681336));
#76995=CARTESIAN_POINT('Ctrl Pts',(-1.35512225893885,1.40942116781589,7.13624288969924));
#76996=CARTESIAN_POINT('Ctrl Pts',(-1.30402033147456,1.45521372145159,7.13233444258512));
#76997=CARTESIAN_POINT('Ctrl Pts',(-1.25288781614849,1.50103368493992,7.12842365600855));
#76998=CARTESIAN_POINT('Ctrl Pts',(-1.19938565652686,1.54411222333274,7.12451286943198));
#76999=CARTESIAN_POINT('Ctrl Pts',(-1.14384749332535,1.58421239485535,7.12060208285541));
#77000=CARTESIAN_POINT('Ctrl Pts',(-1.08821343236478,1.62438180735327,7.11668454352277));
#77001=CARTESIAN_POINT('Ctrl Pts',(-1.03053676451945,1.66156232251659,7.11276700419013));
#77002=CARTESIAN_POINT('Ctrl Pts',(-0.971178267833906,1.69556149168561,
7.10884946485749));
#77003=CARTESIAN_POINT('Ctrl Pts',(-0.943161861229763,1.7116086391174,7.10700043934372));
#77004=CARTESIAN_POINT('Ctrl Pts',(-0.914771117210568,1.72694775559153,
7.10515141382994));
#77005=CARTESIAN_POINT('Ctrl Pts',(-0.886045494940342,1.74156233907831,
7.10330238831617));
#77006=CARTESIAN_POINT('Ctrl Pts',(-0.825175436213357,1.77253087813178,
7.09938427331234));
#77007=CARTESIAN_POINT('Ctrl Pts',(-0.762559166749165,1.80036572379865,
7.09546615830851));
#77008=CARTESIAN_POINT('Ctrl Pts',(-0.698552192994512,1.82486734686732,
7.09154804330468));
#77009=CARTESIAN_POINT('Ctrl Pts',(-0.634641603700151,1.84933207433575,
7.08763582836733));
#77010=CARTESIAN_POINT('Ctrl Pts',(-0.5693449220044,1.87047336632734,7.08372361342998));
#77011=CARTESIAN_POINT('Ctrl Pts',(-0.503041007328279,1.8881381689236,7.07981139849263));
#77012=CARTESIAN_POINT('Ctrl Pts',(-0.436815062660748,1.90578219861652,
7.07590378411972));
#77013=CARTESIAN_POINT('Ctrl Pts',(-0.369584710408188,1.91995773205846,
7.07199616974681));
#77014=CARTESIAN_POINT('Ctrl Pts',(-0.301745759251162,1.93056092801391,
7.0680885553739));
#77015=CARTESIAN_POINT('Ctrl Pts',(-0.233949327192227,1.94115747825446,
7.06418339015794));
#77016=CARTESIAN_POINT('Ctrl Pts',(-0.165545537791048,1.94818605671898,
7.06027822494199));
#77017=CARTESIAN_POINT('Ctrl Pts',(-0.0969407003716783,1.95159383597393,
7.05637305972603));
#77018=CARTESIAN_POINT('Ctrl Pts',(-0.0283553316912114,1.9550006481664,
7.05246900272117));
#77019=CARTESIAN_POINT('Ctrl Pts',(0.0404304807021455,1.95478867654858,
7.04856494571631));
#77020=CARTESIAN_POINT('Ctrl Pts',(0.109006807350353,1.95095707691156,7.04466088871144));
#77021=CARTESIAN_POINT('Ctrl Pts',(0.177587193221973,1.9471252504715,7.0407566006146));
#77022=CARTESIAN_POINT('Ctrl Pts',(0.245957577760492,1.93967340064045,7.03685231251774));
#77023=CARTESIAN_POINT('Ctrl Pts',(0.313711360341332,1.92865268578684,7.03294802442089));
#77024=CARTESIAN_POINT('Ctrl Pts',(0.381537311761262,1.91762023207281,7.02903957761985));
#77025=CARTESIAN_POINT('Ctrl Pts',(0.44874486405865,1.90301140599275,7.02513113081882));
#77026=CARTESIAN_POINT('Ctrl Pts',(0.514936846692412,1.88492865751425,7.02122268401778));
#77027=CARTESIAN_POINT('Ctrl Pts',(0.581168449507529,1.86683508534162,7.01731189775863));
#77028=CARTESIAN_POINT('Ctrl Pts',(0.646382805798501,1.84526360693987,7.01340111149947));
#77029=CARTESIAN_POINT('Ctrl Pts',(0.710199863729138,1.82036593946358,7.00949032524031));
#77030=CARTESIAN_POINT('Ctrl Pts',(0.774127114542087,1.79542528119719,7.00557278622846));
#77031=CARTESIAN_POINT('Ctrl Pts',(0.836651803667251,1.76714717368171,7.00165524721661));
#77032=CARTESIAN_POINT('Ctrl Pts',(0.897416531653136,1.73573026957407,6.99773770820476));
#77033=CARTESIAN_POINT('Ctrl Pts',(0.926096704373684,1.7209018935405,6.9958886800066));
#77034=CARTESIAN_POINT('Ctrl Pts',(0.954385202896228,1.70537492504266,6.99403965180844));
#77035=CARTESIAN_POINT('Ctrl Pts',(0.982246756649369,1.6891735580016,6.99219062361028));
#77036=CARTESIAN_POINT('Ctrl Pts',(1.04128576129815,1.65484264478231,6.98827250815433));
#77037=CARTESIAN_POINT('Ctrl Pts',(1.09863976305389,1.61734470487865,6.98435439269839));
#77038=CARTESIAN_POINT('Ctrl Pts',(1.15394827459615,1.57687012133421,6.98043627724244));
#77039=CARTESIAN_POINT('Ctrl Pts',(1.20917350031563,1.53645648607599,6.97652406184528));
#77040=CARTESIAN_POINT('Ctrl Pts',(1.26235895514181,1.4930753912049,6.97261184644812));
#77041=CARTESIAN_POINT('Ctrl Pts',(1.31317052241145,1.44696205170337,6.96869963105096));
#77042=CARTESIAN_POINT('Ctrl Pts',(1.36392233800537,1.4009029390139,6.96479201620911));
#77043=CARTESIAN_POINT('Ctrl Pts',(1.41230544761326,1.35211829170706,6.96088440136726));
#77044=CARTESIAN_POINT('Ctrl Pts',(1.4580178789933,1.30088426254447,6.95697678652542));
#77045=CARTESIAN_POINT('Ctrl Pts',(1.50370165947578,1.2496823450171,6.95307162083513));
#77046=CARTESIAN_POINT('Ctrl Pts',(1.54671775544886,1.19603445715405,6.94916645514484));
#77047=CARTESIAN_POINT('Ctrl Pts',(1.58680135072359,1.14025324965193,6.94526128945455));
#77048=CARTESIAN_POINT('Ctrl Pts',(1.62687357109104,1.08448787171946,6.94135723197068));
#77049=CARTESIAN_POINT('Ctrl Pts',(1.66401465588701,1.02659077521422,6.93745317448681));
#77050=CARTESIAN_POINT('Ctrl Pts',(1.69800149227727,0.966905854891855,6.93354911700294));
#77051=CARTESIAN_POINT('Ctrl Pts',(1.73199034047711,0.907217401593002,6.92964482842312));
#77052=CARTESIAN_POINT('Ctrl Pts',(1.76282432841332,0.845741343076677,6.9257405398433));
#77053=CARTESIAN_POINT('Ctrl Pts',(1.79032583296344,0.782846991323184,6.92183625126349));
#77054=CARTESIAN_POINT('Ctrl Pts',(1.81785663112085,0.719885646782544,6.91792780397678));
#77055=CARTESIAN_POINT('Ctrl Pts',(1.8420476644635,0.655503445629625,6.91401935669008));
#77056=CARTESIAN_POINT('Ctrl Pts',(1.86276951251717,0.590089606107866,6.91011090940337));
#77057=CARTESIAN_POINT('Ctrl Pts',(1.88350376394712,0.524636612140858,6.9062001226563));
#77058=CARTESIAN_POINT('Ctrl Pts',(1.90076457378381,0.458151227022748,6.90228933590922));
#77059=CARTESIAN_POINT('Ctrl Pts',(1.91447319502982,0.391035018268564,6.89837854916215));
#77060=CARTESIAN_POINT('Ctrl Pts',(1.92820548693666,0.323802920032551,6.89446100966401));
#77061=CARTESIAN_POINT('Ctrl Pts',(1.93837327580741,0.255938310399714,6.89054347016588));
#77062=CARTESIAN_POINT('Ctrl Pts',(1.94494953168796,0.187849192670067,6.88662593066775));
#77063=CARTESIAN_POINT('Ctrl Pts',(1.94805343260339,0.155712080201971,6.88477690674663));
#77064=CARTESIAN_POINT('Ctrl Pts',(1.95035799978609,0.123524970463383,6.88292788282552));
#77065=CARTESIAN_POINT('Ctrl Pts',(1.95186442108001,0.0913306176592063,
6.8810788589044));
#77066=CARTESIAN_POINT('Ctrl Pts',(1.9550565551626,0.0231101993282924,6.87716074363215));
#77067=CARTESIAN_POINT('Ctrl Pts',(1.95467411130022,-0.0454130105096706,
6.8732426283599));
#77068=CARTESIAN_POINT('Ctrl Pts',(1.95068143748882,-0.113832901379826,
6.86932451308765));
#77069=CARTESIAN_POINT('Ctrl Pts',(1.94669477601163,-0.182149762733948,
6.86541229787626));
#77070=CARTESIAN_POINT('Ctrl Pts',(1.93910870240703,-0.250363126800586,
6.86150008266486));
#77071=CARTESIAN_POINT('Ctrl Pts',(1.92793953197579,-0.318064712039808,
6.85758786745347));
#77072=CARTESIAN_POINT('Ctrl Pts',(1.91678349589624,-0.385686683807701,
6.85368025279955));
#77073=CARTESIAN_POINT('Ctrl Pts',(1.90205281081607,-0.452797588958959,
6.84977263814563));
#77074=CARTESIAN_POINT('Ctrl Pts',(1.88381562063976,-0.518993937761935,
6.8458650234917));
#77075=CARTESIAN_POINT('Ctrl Pts',(1.86558986088048,-0.585148797066506,
6.84195985799057));
#77076=CARTESIAN_POINT('Ctrl Pts',(1.84386208601922,-0.650389763943127,
6.83805469248943));
#77077=CARTESIAN_POINT('Ctrl Pts',(1.81875125798339,-0.714324759184377,
6.83414952698829));
#77078=CARTESIAN_POINT('Ctrl Pts',(1.79364755589508,-0.778241610961009,
6.83024546969451));
#77079=CARTESIAN_POINT('Ctrl Pts',(1.76516288621379,-0.840852769204412,
6.82634141240072));
#77080=CARTESIAN_POINT('Ctrl Pts',(1.7334650825806,-0.901784235542977,6.82243735510694));
#77081=CARTESIAN_POINT('Ctrl Pts',(1.70176540263952,-0.962719308635883,
6.81853306671786));
#77082=CARTESIAN_POINT('Ctrl Pts',(1.66685244041948,-1.02197405724667,6.81462877832878));
#77083=CARTESIAN_POINT('Ctrl Pts',(1.6289400608199,-1.07919890578894,6.81072448993969));
#77084=CARTESIAN_POINT('Ctrl Pts',(1.59098729832058,-1.13648470817653,6.80681604284339));
#77085=CARTESIAN_POINT('Ctrl Pts',(1.55002901465564,-1.19173588462052,6.80290759574709));
#77086=CARTESIAN_POINT('Ctrl Pts',(1.50632194849489,-1.24463255119033,6.79899914865079));
#77087=CARTESIAN_POINT('Ctrl Pts',(1.46258872080689,-1.29756087986208,6.79508836209421));
#77088=CARTESIAN_POINT('Ctrl Pts',(1.4161037690433,-1.34813153165594,6.79117757553764));
#77089=CARTESIAN_POINT('Ctrl Pts',(1.36716169807763,-1.39606048984616,6.78726678898106));
#77090=CARTESIAN_POINT('Ctrl Pts',(1.31813511886586,-1.44407220694123,6.78334924967155));
#77091=CARTESIAN_POINT('Ctrl Pts',(1.26664332158604,-1.48943280161812,6.77943171036206));
#77092=CARTESIAN_POINT('Ctrl Pts',(1.21301437599234,-1.53189820929327,6.77551417105255));
#77093=CARTESIAN_POINT('Ctrl Pts',(1.18770223833766,-1.55194130789861,6.77366514543454));
#77094=CARTESIAN_POINT('Ctrl Pts',(1.16191442903889,-1.57134006731575,6.77181611981653));
#77095=CARTESIAN_POINT('Ctrl Pts',(1.13568750743074,-1.59007228938365,6.76996709419852));
#77096=CARTESIAN_POINT('Ctrl Pts',(1.08011223547602,-1.62976617154388,6.76604897894628));
#77097=CARTESIAN_POINT('Ctrl Pts',(1.02234325355725,-1.6666215811514,6.76213086369404));
#77098=CARTESIAN_POINT('Ctrl Pts',(0.962702363599415,-1.70038823776222,
6.7582127484418));
#77099=CARTESIAN_POINT('Ctrl Pts',(0.903151283387841,-1.73410404712939,
6.75430053325135));
#77100=CARTESIAN_POINT('Ctrl Pts',(0.84173431404722,-1.76474009404042,6.75038831806091));
#77101=CARTESIAN_POINT('Ctrl Pts',(0.778803275672308,-1.79208857420667,
6.74647610287047));
#77102=CARTESIAN_POINT('Ctrl Pts',(0.715946240879911,-1.81940489400243,
6.74256848823879));
#77103=CARTESIAN_POINT('Ctrl Pts',(0.651579122071276,-1.84344112987901,
6.73866087360711));
#77104=CARTESIAN_POINT('Ctrl Pts',(0.586077833243433,-1.86403561483698,
6.73475325897542));
#77105=CARTESIAN_POINT('Ctrl Pts',(0.52061759828876,-1.88461719190583,6.73084809349731));
#77106=CARTESIAN_POINT('Ctrl Pts',(0.454025071610393,-1.90176114998742,
6.7269429280192));
#77107=CARTESIAN_POINT('Ctrl Pts',(0.386694152911894,-1.91535470138138,
6.72303776254109));
#77108=CARTESIAN_POINT('Ctrl Pts',(0.319382341385863,-1.92894439519645,
6.71913370527109));
#77109=CARTESIAN_POINT('Ctrl Pts',(0.251333035740334,-1.93898558515639,
6.71522964800109));
#77110=CARTESIAN_POINT('Ctrl Pts',(0.182951462176241,-1.94541634682337,
6.71132559073109));
#77111=CARTESIAN_POINT('Ctrl Pts',(0.114565840871633,-1.95184748914924,
6.70742130236652));
#77112=CARTESIAN_POINT('Ctrl Pts',(0.0458484025583555,-1.95466773538512,
6.70351701400194));
#77113=CARTESIAN_POINT('Ctrl Pts',(-0.0227911685518328,-1.95386707906041,
6.69961272563736));
#77114=CARTESIAN_POINT('Ctrl Pts',(-0.0915038520423259,-1.95306556990563,
6.6957042785665));
#77115=CARTESIAN_POINT('Ctrl Pts',(-0.160138010013442,-1.94863546685146,
6.69179583149564));
#77116=CARTESIAN_POINT('Ctrl Pts',(-0.22828563931517,-1.94061888759294,
6.68788738442478));
#77117=CARTESIAN_POINT('Ctrl Pts',(-0.296474059404211,-1.93259750989048,
6.68397659789421));
#77118=CARTESIAN_POINT('Ctrl Pts',(-0.364174886377365,-1.92098546674165,
6.68006581136364));
#77119=CARTESIAN_POINT('Ctrl Pts',(-0.430989702599176,-1.90587614399611,
6.67615502483307));
#77120=CARTESIAN_POINT('Ctrl Pts',(-0.497919887916471,-1.89074073199377,
6.67223748555018));
#77121=CARTESIAN_POINT('Ctrl Pts',(-0.563960535973705,-1.87209612159104,
6.6683199462673));
#77122=CARTESIAN_POINT('Ctrl Pts',(-0.628728634016056,-1.85008548580013,
6.66440240698442));
#77123=CARTESIAN_POINT('Ctrl Pts',(-0.659298304830121,-1.83969676186236,
6.66255338115382));
#77124=CARTESIAN_POINT('Ctrl Pts',(-0.689584783439458,-1.82855887907734,
6.66070435532323));
#77125=CARTESIAN_POINT('Ctrl Pts',(-0.719549587778587,-1.81669050493684,
6.65885532949263));
#77126=CARTESIAN_POINT('Ctrl Pts',(-0.783045487526726,-1.79154123027214,
6.65493721417833));
#77127=CARTESIAN_POINT('Ctrl Pts',(-0.845347165958881,-1.76300918659432,
6.65101909886402));
#77128=CARTESIAN_POINT('Ctrl Pts',(-0.906069789364223,-1.73122890941709,
6.64710098354972));
#77129=CARTESIAN_POINT('Ctrl Pts',(-0.966700974122495,-1.6994964883005,
6.64318876829611));
#77130=CARTESIAN_POINT('Ctrl Pts',(-1.02575739066157,-1.66452576748227,
6.63927655304249));
#77131=CARTESIAN_POINT('Ctrl Pts',(-1.08287360038137,-1.62649954368179,
6.63536433778888));
#77132=CARTESIAN_POINT('Ctrl Pts',(-1.13992264447097,-1.58851803670161,
6.6314567230927));
#77133=CARTESIAN_POINT('Ctrl Pts',(-1.19503560549445,-1.54748843401052,
6.62754910839652));
#77134=CARTESIAN_POINT('Ctrl Pts',(-1.24787272958104,-1.50363880329286,
6.62364149370033));
#77135=CARTESIAN_POINT('Ctrl Pts',(-1.30067673725271,-1.45981665595151,
6.61973632815694));
#77136=CARTESIAN_POINT('Ctrl Pts',(-1.35120735987634,-1.41317830014893,
6.61583116261354));
#77137=CARTESIAN_POINT('Ctrl Pts',(-1.399156145627,-1.36399343112575,6.61192599707014));
#77138=CARTESIAN_POINT('Ctrl Pts',(-1.4470913244768,-1.31482251977901,6.60802193973417));
#77139=CARTESIAN_POINT('Ctrl Pts',(-1.49244577773927,-1.26310688183872,
6.60411788239819));
#77140=CARTESIAN_POINT('Ctrl Pts',(-1.53494763511834,-1.20915332255451,
6.60021382506222));
#77141=CARTESIAN_POINT('Ctrl Pts',(-1.57745200833494,-1.15519656956542,
6.59630953663108));
#77142=CARTESIAN_POINT('Ctrl Pts',(-1.61710314806692,-1.09900202020992,
6.59240524819994));
#77143=CARTESIAN_POINT('Ctrl Pts',(-1.65367037796729,-1.04090839223897,
6.5885009597688));
#77144=CARTESIAN_POINT('Ctrl Pts',(-1.69027655795744,-0.982752885038156,
6.58459251263093));
#77145=CARTESIAN_POINT('Ctrl Pts',(-1.72379201000291,-0.922694679357089,
6.58068406549306));
#77146=CARTESIAN_POINT('Ctrl Pts',(-1.75403075561889,-0.861099360319714,
6.5767756183552));
#77147=CARTESIAN_POINT('Ctrl Pts',(-1.78428760109273,-0.799467172473922,
6.57286483175727));
#77148=CARTESIAN_POINT('Ctrl Pts',(-1.81126364354497,-0.73629649260063,
6.56895404515935));
#77149=CARTESIAN_POINT('Ctrl Pts',(-1.83482117177094,-0.671972668805138,
6.56504325856143));
#77150=CARTESIAN_POINT('Ctrl Pts',(-1.8584193767624,-0.607537777113628,
6.56112571921136));
#77151=CARTESIAN_POINT('Ctrl Pts',(-1.87858714210892,-0.541946237426363,
6.55720817986128));
#77152=CARTESIAN_POINT('Ctrl Pts',(-1.8952369370561,-0.475597468893815,
6.55329064051121));
#77153=CARTESIAN_POINT('Ctrl Pts',(-1.90309541360779,-0.44428175339099,
6.55144161526973));
#77154=CARTESIAN_POINT('Ctrl Pts',(-1.91017093194561,-0.412797478057282,
6.54959259002824));
#77155=CARTESIAN_POINT('Ctrl Pts',(-1.91645829519957,-0.381187096792052,
6.54774356478676));
#77156=CARTESIAN_POINT('Ctrl Pts',(-1.93568455106865,-0.284525069519832,
6.54208939292406));
#77157=CARTESIAN_POINT('Ctrl Pts',(-1.94760241356582,-0.186364687119417,
6.53643522106135));
#77158=CARTESIAN_POINT('Ctrl Pts',(-1.95203469361534,-0.0876159512992307,
6.53078104919865));
#77159=CARTESIAN_POINT('Ctrl Pts',(-1.95331802390111,-0.0590240658715734,
6.52914393017384));
#77160=CARTESIAN_POINT('Ctrl Pts',(-1.95397407964231,-0.0303830267533754,
6.52750681114904));
#77161=CARTESIAN_POINT('Ctrl Pts',(-1.9539992470135,-0.00171542142396889,
6.52586969212423));
#77162=CARTESIAN_POINT('',(-1.95079827866809,-3.39314739267183E-5,5.82586969212423));
#77163=CARTESIAN_POINT('Ctrl Pts',(-1.95470819824863,-0.00170936608773048,
6.52586931091837));
#77164=CARTESIAN_POINT('Ctrl Pts',(-1.94992671209745,0.519363870229142,
6.49612347397254));
#77165=CARTESIAN_POINT('Ctrl Pts',(-1.4676232491419,1.69704784902766,6.42934038212473));
#77166=CARTESIAN_POINT('Ctrl Pts',(0.520941041773296,2.24982010296219,6.325520035375));
#77167=CARTESIAN_POINT('Ctrl Pts',(2.17254641826532,0.783014766469865,6.2144082706691));
#77168=CARTESIAN_POINT('Ctrl Pts',(1.83645143012728,-1.40018434850807,6.10329650596323));
#77169=CARTESIAN_POINT('Ctrl Pts',(-0.179844794802092,-2.30233053978416,
5.99218474125735));
#77170=CARTESIAN_POINT('Ctrl Pts',(-1.72101362137731,-1.30002449932279,
5.89970913664434));
#77171=CARTESIAN_POINT('Ctrl Pts',(-1.95084848133978,-0.324013652614182,
5.84427078693331));
#77172=CARTESIAN_POINT('Ctrl Pts',(-1.95079827866809,-3.39314739267183E-5,
5.82586969212423));
#77173=CARTESIAN_POINT('',(-1.95399923079511,0.00173379702722768,5.12586969212423));
#77174=CARTESIAN_POINT('Ctrl Pts',(-1.95079827866809,-3.39314739267183E-5,
5.82586969212423));
#77175=CARTESIAN_POINT('Ctrl Pts',(-1.95074743468102,0.328084477385078,
5.80723353203135));
#77176=CARTESIAN_POINT('Ctrl Pts',(-1.71668384482246,1.30836916436041,5.75156011703652));
#77177=CARTESIAN_POINT('Ctrl Pts',(-0.165267944017257,2.3034227947424,5.65884944713968));
#77178=CARTESIAN_POINT('Ctrl Pts',(1.84527750005803,1.38853196305902,5.54773768243383));
#77179=CARTESIAN_POINT('Ctrl Pts',(2.16754658332468,-0.796750822900473,
5.43662591772792));
#77180=CARTESIAN_POINT('Ctrl Pts',(0.506689737022561,-2.25307247443607,
5.32551415302205));
#77181=CARTESIAN_POINT('Ctrl Pts',(-1.47384180283068,-1.68900403463015,
5.22192884966718));
#77182=CARTESIAN_POINT('Ctrl Pts',(-1.94982277544559,-0.515311787546464,
5.15538080121427));
#77183=CARTESIAN_POINT('Ctrl Pts',(-1.95458374895511,0.0017287873519051,
5.12587000766333));
#77184=CARTESIAN_POINT('',(-1.95399970439072,-0.00107482137716873,4.42586969212423));
#77185=CARTESIAN_POINT('Ctrl Pts',(-1.95399923079511,0.00173379702722768,
5.12586969212423));
#77186=CARTESIAN_POINT('Ctrl Pts',(-1.95391274807805,0.0992003170110558,
5.12030494365936));
#77187=CARTESIAN_POINT('Ctrl Pts',(-1.9465302636818,0.196354128825551,5.1147401951945));
#77188=CARTESIAN_POINT('Ctrl Pts',(-1.93201158427293,0.292313595707092,
5.10917544672964));
#77189=CARTESIAN_POINT('Ctrl Pts',(-1.92689366140619,0.326139891887515,
5.10721383902319));
#77190=CARTESIAN_POINT('Ctrl Pts',(-1.92088939232674,0.359818056639332,
5.10525223131674));
#77191=CARTESIAN_POINT('Ctrl Pts',(-1.914007071507,0.393310221353584,5.10329062361029));
#77192=CARTESIAN_POINT('Ctrl Pts',(-1.90026032370521,0.460207472109741,
5.09937250832143));
#77193=CARTESIAN_POINT('Ctrl Pts',(-1.88297487280552,0.526515765509737,
5.09545439303258));
#77194=CARTESIAN_POINT('Ctrl Pts',(-1.86221641779253,0.591832757883458,
5.09153627774372));
#77195=CARTESIAN_POINT('Ctrl Pts',(-1.84148922172499,0.657051393211835,
5.08762406251592));
#77196=CARTESIAN_POINT('Ctrl Pts',(-1.81729954861703,0.721281225074169,
5.08371184728813));
#77197=CARTESIAN_POINT('Ctrl Pts',(-1.78976399250792,0.784130633964848,
5.07979963206033));
#77198=CARTESIAN_POINT('Ctrl Pts',(-1.76226081675402,0.846906135280302,
5.07589201739038));
#77199=CARTESIAN_POINT('Ctrl Pts',(-1.73141976859218,0.908303989127187,
5.07198440272043));
#77200=CARTESIAN_POINT('Ctrl Pts',(-1.69740648393353,0.96795001332734,5.06807678805048));
#77201=CARTESIAN_POINT('Ctrl Pts',(-1.66341451758442,1.02755865353419,5.06417162253355));
#77202=CARTESIAN_POINT('Ctrl Pts',(-1.6262545018986,1.08541721581697,5.06026645701662));
#77203=CARTESIAN_POINT('Ctrl Pts',(-1.58613850153253,1.14117511975863,5.0563612914997));
#77204=CARTESIAN_POINT('Ctrl Pts',(-1.54603388528254,1.19691720072579,5.0524572341904));
#77205=CARTESIAN_POINT('Ctrl Pts',(-1.50297523674509,1.25055940767055,5.0485531768811));
#77206=CARTESIAN_POINT('Ctrl Pts',(-1.45721751668746,1.30178074538658,5.0446491195718));
#77207=CARTESIAN_POINT('Ctrl Pts',(-1.41145708806801,1.35300511507533,5.0407448311675));
#77208=CARTESIAN_POINT('Ctrl Pts',(-1.36299760034251,1.4018079659198,5.03684054276319));
#77209=CARTESIAN_POINT('Ctrl Pts',(-1.31213259233443,1.44790333245481,5.03293625435889));
#77210=CARTESIAN_POINT('Ctrl Pts',(-1.26121340476127,1.49404779810546,5.02902780724792));
#77211=CARTESIAN_POINT('Ctrl Pts',(-1.20788394858165,1.53747869310908,5.02511936013696));
#77212=CARTESIAN_POINT('Ctrl Pts',(-1.15247198028643,1.57794940814168,5.02121091302599));
#77213=CARTESIAN_POINT('Ctrl Pts',(-1.09702684432159,1.61844434753134,5.01730012645504));
#77214=CARTESIAN_POINT('Ctrl Pts',(-1.03949712746111,1.65597531182826,5.01338933988409));
#77215=CARTESIAN_POINT('Ctrl Pts',(-0.980238426836116,1.69033979618119,
5.00947855331314));
#77216=CARTESIAN_POINT('Ctrl Pts',(-0.920877404256082,1.72476361766412,
5.00556101398987));
#77217=CARTESIAN_POINT('Ctrl Pts',(-0.859781877160007,1.75600982298062,
5.00164347466661));
#77218=CARTESIAN_POINT('Ctrl Pts',(-0.79733000983898,1.78392288381818,4.99772593534334));
#77219=CARTESIAN_POINT('Ctrl Pts',(-0.767853574658789,1.79709747032381,
4.9958769098637));
#77220=CARTESIAN_POINT('Ctrl Pts',(-0.738075242029198,1.80953023862869,
4.99402788438405));
#77221=CARTESIAN_POINT('Ctrl Pts',(-0.708035919494371,1.82120870212773,
4.99217885890441));
#77222=CARTESIAN_POINT('Ctrl Pts',(-0.644382102829161,1.84595555764144,
4.98826074361555));
#77223=CARTESIAN_POINT('Ctrl Pts',(-0.579303134779922,1.8674102658445,4.98434262832669));
#77224=CARTESIAN_POINT('Ctrl Pts',(-0.513172640155052,1.885409727724,4.98042451303783));
#77225=CARTESIAN_POINT('Ctrl Pts',(-0.447141727581096,1.90338208526473,
4.97651229781003));
#77226=CARTESIAN_POINT('Ctrl Pts',(-0.380062901780406,1.91790939455919,
4.97260008258223));
#77227=CARTESIAN_POINT('Ctrl Pts',(-0.312328391621999,1.9288771282243,4.96868786735443));
#77228=CARTESIAN_POINT('Ctrl Pts',(-0.244673533659072,1.93983196441567,
4.96478025268447));
#77229=CARTESIAN_POINT('Ctrl Pts',(-0.176365005912992,1.94723545993428,
4.96087263801452));
#77230=CARTESIAN_POINT('Ctrl Pts',(-0.107806996632855,1.95102374446776,
4.95696502334456));
#77231=CARTESIAN_POINT('Ctrl Pts',(-0.039291957059335,1.95480965464007,
4.95305985782764));
#77232=CARTESIAN_POINT('Ctrl Pts',(0.0294717638388294,1.95498482154557,
4.94915469231071));
#77233=CARTESIAN_POINT('Ctrl Pts',(0.0980746144653294,1.95153718130029,
4.94524952679378));
#77234=CARTESIAN_POINT('Ctrl Pts',(0.166657996979155,1.94809051942614,4.94134546948448));
#77235=CARTESIAN_POINT('Ctrl Pts',(0.235080108818078,1.94102311599331,4.93744141217518));
#77236=CARTESIAN_POINT('Ctrl Pts',(0.302932977910631,1.93037499229922,4.93353735486588));
#77237=CARTESIAN_POINT('Ctrl Pts',(0.370789863455265,1.9197262383049,4.92963306646157));
#77238=CARTESIAN_POINT('Ctrl Pts',(0.438076953822389,1.90549642203426,4.92572877805727));
#77239=CARTESIAN_POINT('Ctrl Pts',(0.504394772752544,1.88777697655732,4.92182448965297));
#77240=CARTESIAN_POINT('Ctrl Pts',(0.570783231022542,1.87003865696856,4.917916042542));
#77241=CARTESIAN_POINT('Ctrl Pts',(0.636199881316839,1.84880341735352,4.91400759543103));
#77242=CARTESIAN_POINT('Ctrl Pts',(0.700259743181115,1.8242127869522,4.91009914832006));
#77243=CARTESIAN_POINT('Ctrl Pts',(0.764357949042219,1.79960743745805,4.90618836174911));
#77244=CARTESIAN_POINT('Ctrl Pts',(0.827097300859291,1.77164290033175,4.90227757517815));
#77245=CARTESIAN_POINT('Ctrl Pts',(0.888114762520646,1.74050802026101,4.8983667886072));
#77246=CARTESIAN_POINT('Ctrl Pts',(0.949237582988419,1.70931937961563,4.89444924928393));
#77247=CARTESIAN_POINT('Ctrl Pts',(1.00863215378542,1.67494971657283,4.89053170996066));
#77248=CARTESIAN_POINT('Ctrl Pts',(1.0659626568427,1.63763231960561,4.8866141706374));
#77249=CARTESIAN_POINT('Ctrl Pts',(1.09302187748232,1.6200190138716,4.88476514515777));
#77250=CARTESIAN_POINT('Ctrl Pts',(1.11962174108735,1.60174963845557,4.88291611967814));
#77251=CARTESIAN_POINT('Ctrl Pts',(1.14572956451243,1.58285178238588,4.88106709419852));
#77252=CARTESIAN_POINT('Ctrl Pts',(1.20105247014453,1.54280691572004,4.87714897890966));
#77253=CARTESIAN_POINT('Ctrl Pts',(1.25438307974971,1.49977875441177,4.8732308636208));
#77254=CARTESIAN_POINT('Ctrl Pts',(1.30538167850735,1.45399266621855,4.86931274833194));
#77255=CARTESIAN_POINT('Ctrl Pts',(1.3563034814526,1.4082755246224,4.86540053310415));
#77256=CARTESIAN_POINT('Ctrl Pts',(1.40489987984092,1.35980902433802,4.86148831787635));
#77257=CARTESIAN_POINT('Ctrl Pts',(1.45086186696259,1.30886051319223,4.85757610264855));
#77258=CARTESIAN_POINT('Ctrl Pts',(1.4967698052224,1.25797191479637,4.8536684879786));
#77259=CARTESIAN_POINT('Ctrl Pts',(1.54004915682881,1.20460746564474,4.84976087330864));
#77260=CARTESIAN_POINT('Ctrl Pts',(1.58042698002786,1.14907204334629,4.84585325863869));
#77261=CARTESIAN_POINT('Ctrl Pts',(1.62077949585239,1.09357142866302,4.84194809312176));
#77262=CARTESIAN_POINT('Ctrl Pts',(1.6582338021363,1.03590293695401,4.83804292760484));
#77263=CARTESIAN_POINT('Ctrl Pts',(1.69255756619582,0.976404058324866,4.83413776208791));
#77264=CARTESIAN_POINT('Ctrl Pts',(1.72687158985972,0.916922064283803,4.83023370477862));
#77265=CARTESIAN_POINT('Ctrl Pts',(1.75805658922141,0.855611140342085,4.82632964746932));
#77266=CARTESIAN_POINT('Ctrl Pts',(1.78592484162299,0.792835708122365,4.82242559016002));
#77267=CARTESIAN_POINT('Ctrl Pts',(1.81379474364533,0.730056560002035,4.81852130175571));
#77268=CARTESIAN_POINT('Ctrl Pts',(1.83834731168824,0.665813182104631,4.81461701335141));
#77269=CARTESIAN_POINT('Ctrl Pts',(1.85944261980839,0.600490752335224,4.8107127249471));
#77270=CARTESIAN_POINT('Ctrl Pts',(1.88056039788703,0.535098743478489,4.80680427783614));
#77271=CARTESIAN_POINT('Ctrl Pts',(1.89821341536483,0.468625857944904,4.80289583072517));
#77272=CARTESIAN_POINT('Ctrl Pts',(1.91231169311282,0.401472275984276,4.7989873836142));
#77273=CARTESIAN_POINT('Ctrl Pts',(1.92641840959765,0.334278498234007,4.79507659704325));
#77274=CARTESIAN_POINT('Ctrl Pts',(1.93696607621066,0.26640369928676,4.7911658104723));
#77275=CARTESIAN_POINT('Ctrl Pts',(1.9439163658891,0.198255296092009,4.78725502390134));
#77276=CARTESIAN_POINT('Ctrl Pts',(1.95087865662763,0.129989221099292,4.78333748457808));
#77277=CARTESIAN_POINT('Ctrl Pts',(1.95423114908046,0.0614490899921429,
4.77941994525481));
#77278=CARTESIAN_POINT('Ctrl Pts',(1.95398761717133,-0.00695643163745314,
4.77550240593155));
#77279=CARTESIAN_POINT('Ctrl Pts',(1.95387267340996,-0.0392429109817258,
4.77365338045191));
#77280=CARTESIAN_POINT('Ctrl Pts',(1.95295739184096,-0.0714994619684756,
4.77180435497227));
#77281=CARTESIAN_POINT('Ctrl Pts',(1.95124721609382,-0.103683661616032,
4.76995532949264));
#77282=CARTESIAN_POINT('Ctrl Pts',(1.94762332566327,-0.171882508028614,
4.76603721420378));
#77283=CARTESIAN_POINT('Ctrl Pts',(1.94041247795351,-0.24002632845082,4.76211909891493));
#77284=CARTESIAN_POINT('Ctrl Pts',(1.92961967910788,-0.307707481221396,
4.75820098362607));
#77285=CARTESIAN_POINT('Ctrl Pts',(1.9188431325079,-0.375286716895494,4.75428876839827));
#77286=CARTESIAN_POINT('Ctrl Pts',(1.9044954164924,-0.442404185793469,4.75037655317047));
#77287=CARTESIAN_POINT('Ctrl Pts',(1.88663346210431,-0.508655266038109,
4.74646433794268));
#77288=CARTESIAN_POINT('Ctrl Pts',(1.86879251242828,-0.574828438522259,
4.74255672327272));
#77289=CARTESIAN_POINT('Ctrl Pts',(1.84744565914114,-0.640136773085806,
4.73864910860277));
#77290=CARTESIAN_POINT('Ctrl Pts',(1.82270092612445,-0.704185582005962,
4.73474149393282));
#77291=CARTESIAN_POINT('Ctrl Pts',(1.79797170222084,-0.768194247424886,
4.73083632841589));
#77292=CARTESIAN_POINT('Ctrl Pts',(1.76984900004189,-0.830944495371427,
4.72693116289897));
#77293=CARTESIAN_POINT('Ctrl Pts',(1.73849027101473,-0.892058057296234,
4.72302599738204));
#77294=CARTESIAN_POINT('Ctrl Pts',(1.70714044096574,-0.95315427641826,4.71912194007274));
#77295=CARTESIAN_POINT('Ctrl Pts',(1.67255663154283,-1.01261429412407,4.71521788276345));
#77296=CARTESIAN_POINT('Ctrl Pts',(1.63494312021436,-1.07008270412325,4.71131382545415));
#77297=CARTESIAN_POINT('Ctrl Pts',(1.59732738240869,-1.12755451588154,4.70740953704984));
#77298=CARTESIAN_POINT('Ctrl Pts',(1.55668185816409,-1.1830340757216,4.70350524864554));
#77299=CARTESIAN_POINT('Ctrl Pts',(1.51325419252364,-1.23619486684326,4.69960096024124));
#77300=CARTESIAN_POINT('Ctrl Pts',(1.46978026930596,-1.28941228291505,4.69569251313027));
#77301=CARTESIAN_POINT('Ctrl Pts',(1.42351860237532,-1.34030561951258,4.69178406601931));
#77302=CARTESIAN_POINT('Ctrl Pts',(1.37475653739245,-1.38858217722133,4.68787561890834));
#77303=CARTESIAN_POINT('Ctrl Pts',(1.32596528513989,-1.43688763159206,4.68396483233739));
#77304=CARTESIAN_POINT('Ctrl Pts',(1.27467102358867,-1.48257286263037,4.68005404576643));
#77305=CARTESIAN_POINT('Ctrl Pts',(1.22119520081885,-1.52538463395204,4.67614325919548));
#77306=CARTESIAN_POINT('Ctrl Pts',(1.16762704138498,-1.56827032832793,4.67222571987222));
#77307=CARTESIAN_POINT('Ctrl Pts',(1.11187020205469,-1.60827237384719,4.66830818054895));
#77308=CARTESIAN_POINT('Ctrl Pts',(1.0542754467429,-1.64518062303051,4.66439064122569));
#77309=CARTESIAN_POINT('Ctrl Pts',(1.02709150261937,-1.66260081655447,4.66254161574605));
#77310=CARTESIAN_POINT('Ctrl Pts',(0.999498482844079,-1.67933246565426,
4.6606925902664));
#77311=CARTESIAN_POINT('Ctrl Pts',(0.971534977350408,-1.69535712691596,
4.65884356478676));
#77312=CARTESIAN_POINT('Ctrl Pts',(0.912279851008944,-1.72931364670408,
4.6549254494979));
#77313=CARTESIAN_POINT('Ctrl Pts',(0.851124875507569,-1.76022716410113,
4.65100733420904));
#77314=CARTESIAN_POINT('Ctrl Pts',(0.788415197746269,-1.78788072196182,
4.64708921892018));
#77315=CARTESIAN_POINT('Ctrl Pts',(0.725799950827496,-1.81549263794424,
4.64317700369238));
#77316=CARTESIAN_POINT('Ctrl Pts',(0.661635094416118,-1.83985414011142,
4.63926478846459));
#77317=CARTESIAN_POINT('Ctrl Pts',(0.596291410110017,-1.86079352810273,
4.63535257323679));
#77318=CARTESIAN_POINT('Ctrl Pts',(0.53102456651486,-1.8817082924831,4.63144495856683));
#77319=CARTESIAN_POINT('Ctrl Pts',(0.464582114316974,-1.89920878546645,
4.62753734389688));
#77320=CARTESIAN_POINT('Ctrl Pts',(0.397354210112301,-1.91317161585312,
4.62362972922693));
#77321=CARTESIAN_POINT('Ctrl Pts',(0.330168441952001,-1.92712569483741,
4.61972456371));
#77322=CARTESIAN_POINT('Ctrl Pts',(0.26219867885986,-1.93754640980326,4.61581939819307));
#77323=CARTESIAN_POINT('Ctrl Pts',(0.193848101334831,-1.94436079820821,
4.61191423267615));
#77324=CARTESIAN_POINT('Ctrl Pts',(0.125516920332409,-1.95117325282646,
4.60801017536685));
#77325=CARTESIAN_POINT('Ctrl Pts',(0.0568056286537933,-1.95438136374034,
4.60410611805755));
#77326=CARTESIAN_POINT('Ctrl Pts',(-0.0118763931020487,-1.95396390736546,
4.60020206074825));
#77327=CARTESIAN_POINT('Ctrl Pts',(-0.0805624803904741,-1.95354642627985,
4.59629777234394));
#77328=CARTESIAN_POINT('Ctrl Pts',(-0.149218802462485,-1.94950295738358,
4.59239348393964));
#77329=CARTESIAN_POINT('Ctrl Pts',(-0.217436718029847,-1.9418643808599,
4.58848919553533));
#77330=CARTESIAN_POINT('Ctrl Pts',(-0.285727296851189,-1.93421766800105,
4.58458074842436));
#77331=CARTESIAN_POINT('Ctrl Pts',(-0.353578047466985,-1.92296826010078,
4.58067230131339));
#77332=CARTESIAN_POINT('Ctrl Pts',(-0.420587196951145,-1.90819873434629,
4.57676385420243));
#77333=CARTESIAN_POINT('Ctrl Pts',(-0.487636455772705,-1.89342036806932,
4.57285306763147));
#77334=CARTESIAN_POINT('Ctrl Pts',(-0.553842636738836,-1.87511782166209,
4.56894228106052));
#77335=CARTESIAN_POINT('Ctrl Pts',(-0.618818615045365,-1.85342372966177,
4.56503149448957));
#77336=CARTESIAN_POINT('Ctrl Pts',(-0.683906787326116,-1.83169217848865,
4.5611139551663));
#77337=CARTESIAN_POINT('Ctrl Pts',(-0.747760059950065,-1.80655757379627,
4.55719641584304));
#77338=CARTESIAN_POINT('Ctrl Pts',(-0.810011598995132,-1.77820055378839,
4.55327887651977));
#77339=CARTESIAN_POINT('Ctrl Pts',(-0.839393481943236,-1.76481642456991,
4.55142985104014));
#77340=CARTESIAN_POINT('Ctrl Pts',(-0.868418907984736,-1.75071509608578,
4.54958082556051));
#77341=CARTESIAN_POINT('Ctrl Pts',(-0.897051447481119,-1.73591897868882,
4.54773180008087));
#77342=CARTESIAN_POINT('Ctrl Pts',(-0.957724267837203,-1.70456576348041,
4.54381368479201));
#77343=CARTESIAN_POINT('Ctrl Pts',(-1.01687162431583,-1.66996566509871,
4.53989556950315));
#77344=CARTESIAN_POINT('Ctrl Pts',(-1.07412401014006,-1.63229090876616,
4.53597745421429));
#77345=CARTESIAN_POINT('Ctrl Pts',(-1.13129018293907,-1.59467288464958,
4.53206523898649));
#77346=CARTESIAN_POINT('Ctrl Pts',(-1.18656664073048,-1.55398965960322,
4.52815302375869));
#77347=CARTESIAN_POINT('Ctrl Pts',(-1.23960798587046,-1.5104595464183,4.52424080853089));
#77348=CARTESIAN_POINT('Ctrl Pts',(-1.29258695719858,-1.46698062234035,
4.52033319386094));
#77349=CARTESIAN_POINT('Ctrl Pts',(-1.3433356574388,-1.42066176945451,4.51642557919098));
#77350=CARTESIAN_POINT('Ctrl Pts',(-1.39153875831127,-1.37176378583105,
4.51251796452103));
#77351=CARTESIAN_POINT('Ctrl Pts',(-1.43971164720521,-1.32289644971376,
4.5086127990041));
#77352=CARTESIAN_POINT('Ctrl Pts',(-1.48534175713883,-1.27145353900056,
4.50470763348718));
#77353=CARTESIAN_POINT('Ctrl Pts',(-1.52814905536641,-1.21773415185037,
4.50080246797025));
#77354=CARTESIAN_POINT('Ctrl Pts',(-1.57094420574158,-1.1640300091845,4.49689841066095));
#77355=CARTESIAN_POINT('Ctrl Pts',(-1.61091782825079,-1.10805105703936,
4.49299435335165));
#77356=CARTESIAN_POINT('Ctrl Pts',(-1.64782998856845,-1.05012967236171,
4.48909029604235));
#77357=CARTESIAN_POINT('Ctrl Pts',(-1.68474433384784,-0.992204859111793,
4.48518600763805));
#77358=CARTESIAN_POINT('Ctrl Pts',(-1.71859659496775,-0.932337801239931,
4.48128171923375));
#77359=CARTESIAN_POINT('Ctrl Pts',(-1.74919100739059,-0.870888523098049,
4.47737743082945));
#77360=CARTESIAN_POINT('Ctrl Pts',(-1.77981800787394,-0.809373791409713,
4.47346898371848));
#77361=CARTESIAN_POINT('Ctrl Pts',(-1.80718001468011,-0.74627391723576,
4.46956053660752));
#77362=CARTESIAN_POINT('Ctrl Pts',(-1.83112841662984,-0.68197120306557,
4.46565208949655));
#77363=CARTESIAN_POINT('Ctrl Pts',(-1.85509115325689,-0.617629999535627,
4.4617413029256));
#77364=CARTESIAN_POINT('Ctrl Pts',(-1.87563607141369,-0.552084992547746,
4.45783051635464));
#77365=CARTESIAN_POINT('Ctrl Pts',(-1.8926645567636,-0.485733337924075,
4.45391972978369));
#77366=CARTESIAN_POINT('Ctrl Pts',(-1.9097224451867,-0.419267113946904,
4.45000219046042));
#77367=CARTESIAN_POINT('Ctrl Pts',(-1.92325168549484,-0.351991944422665,
4.44608465113716));
#77368=CARTESIAN_POINT('Ctrl Pts',(-1.93320499647078,-0.284313984215347,
4.44216711181389));
#77369=CARTESIAN_POINT('Ctrl Pts',(-1.93790282438841,-0.252370904004291,
4.44031808633426));
#77370=CARTESIAN_POINT('Ctrl Pts',(-1.94180479144181,-0.22033814772228,
4.43846906085462));
#77371=CARTESIAN_POINT('Ctrl Pts',(-1.94490995839488,-0.188258475868743,
4.43662003537499));
#77372=CARTESIAN_POINT('Ctrl Pts',(-1.95092783302923,-0.126087440802656,
4.43303658762473));
#77373=CARTESIAN_POINT('Ctrl Pts',(-1.95396529883072,-0.0636233112941925,
4.42945313987448));
#77374=CARTESIAN_POINT('Ctrl Pts',(-1.95399970439072,-0.00107482137716873,
4.42586969212423));
#77375=CARTESIAN_POINT('',(-1.95135083467133,-0.00103713828173369,3.72586969212423));
#77376=CARTESIAN_POINT('Ctrl Pts',(-1.95645520290123,-0.00105911241531774,
4.42586871599238));
#77377=CARTESIAN_POINT('Ctrl Pts',(-1.9525751484303,0.583602094023599,4.39241523421795));
#77378=CARTESIAN_POINT('Ctrl Pts',(-1.36378427143187,1.82232327203781,4.32192449754158));
#77379=CARTESIAN_POINT('Ctrl Pts',(0.742605858221022,2.18668850182256,4.21439650596322));
#77380=CARTESIAN_POINT('Ctrl Pts',(2.23977636166244,0.562558365331892,4.10328474125734));
#77381=CARTESIAN_POINT('Ctrl Pts',(1.68773665970148,-1.57626616793194,3.99217297655146));
#77382=CARTESIAN_POINT('Ctrl Pts',(-0.408442558280547,-2.27293746971917,
3.88106121184558));
#77383=CARTESIAN_POINT('Ctrl Pts',(-1.78454713380843,-1.16814864820909,
3.79229345036984));
#77384=CARTESIAN_POINT('Ctrl Pts',(-1.95259626934014,-0.259551514418081,
3.74056294379605));
#77385=CARTESIAN_POINT('Ctrl Pts',(-1.95135083467133,-0.00103713828173369,
3.72586969212423));
#77386=CARTESIAN_POINT('',(-1.95399929780826,0.00165655208450348,3.02586967148122));
#77387=CARTESIAN_POINT('Ctrl Pts',(-1.95135083467133,-0.00103713828173369,
3.72586969212423));
#77388=CARTESIAN_POINT('Ctrl Pts',(-1.94945690425454,0.392085240919391,
3.70352568889409));
#77389=CARTESIAN_POINT('Ctrl Pts',(-1.64342223932233,1.43955704004953,3.64414443076199));
#77390=CARTESIAN_POINT('Ctrl Pts',(0.0651574691963108,2.30842469421968,
3.54772591772793));
#77391=CARTESIAN_POINT('Ctrl Pts',(1.97449455267556,1.19768164639485,3.43661415302205));
#77392=CARTESIAN_POINT('Ctrl Pts',(2.07733235475046,-1.00884109381311,3.32550238831617));
#77393=CARTESIAN_POINT('Ctrl Pts',(0.279582788264533,-2.29235763554204,
3.21439062361028));
#77394=CARTESIAN_POINT('Ctrl Pts',(-1.56633376284093,-1.56083761130856,
3.11451305821298));
#77395=CARTESIAN_POINT('Ctrl Pts',(-1.94902862841993,-0.451550454744232,
3.05167274771762));
#77396=CARTESIAN_POINT('Ctrl Pts',(-1.95267758926504,0.00165506900100115,
3.02586969212423));
#77397=CARTESIAN_POINT('',(-1.95399999958081,4.04748477694372E-5,2.3258696921786));
#77398=CARTESIAN_POINT('Ctrl Pts',(-1.95399929780826,0.00165655208450348,
3.02586967148122));
#77399=CARTESIAN_POINT('Ctrl Pts',(-1.95392950841898,0.0839771859707575,
3.02118591758554));
#77400=CARTESIAN_POINT('Ctrl Pts',(-1.94865370480582,0.166072172431067,
3.01650216368985));
#77401=CARTESIAN_POINT('Ctrl Pts',(-1.93827999163124,0.247359402574485,
3.01181840979416));
#77402=CARTESIAN_POINT('Ctrl Pts',(-1.92776404327564,0.329761171330941,
3.00707043640715));
#77403=CARTESIAN_POINT('Ctrl Pts',(-1.91200951167843,0.411332865074898,
3.00232246302014));
#77404=CARTESIAN_POINT('Ctrl Pts',(-1.89117786921064,0.491489844257136,
2.99757448963314));
#77405=CARTESIAN_POINT('Ctrl Pts',(-1.88326958784551,0.521919703339655,
2.99577202448826));
#77406=CARTESIAN_POINT('Ctrl Pts',(-1.87463009643616,0.552145899352889,
2.99396955934339));
#77407=CARTESIAN_POINT('Ctrl Pts',(-1.86527001147586,0.582137255541047,
2.99216709419852));
#77408=CARTESIAN_POINT('Ctrl Pts',(-1.84492349210666,0.647331077197404,
2.98824897891026));
#77409=CARTESIAN_POINT('Ctrl Pts',(-1.82111460008519,0.711586141168167,
2.98433086362199));
#77410=CARTESIAN_POINT('Ctrl Pts',(-1.7939488123109,0.774508656380481,2.98041274833373));
#77411=CARTESIAN_POINT('Ctrl Pts',(-1.76682393191034,0.837336420250893,
2.97650053310652));
#77412=CARTESIAN_POINT('Ctrl Pts',(-1.73635238144785,0.898835169809968,
2.97258831787931));
#77413=CARTESIAN_POINT('Ctrl Pts',(-1.70268921043205,0.958626857895342,
2.96867610265209));
#77414=CARTESIAN_POINT('Ctrl Pts',(-1.66906562552191,1.01834823412324,2.96476848798272));
#77415=CARTESIAN_POINT('Ctrl Pts',(-1.63225811409756,1.07636610904359,2.96086087331335));
#77416=CARTESIAN_POINT('Ctrl Pts',(-1.59246878516366,1.13232467441073,2.95695325864398));
#77417=CARTESIAN_POINT('Ctrl Pts',(-1.55270439475709,1.18824816695184,2.95304809312763));
#77418=CARTESIAN_POINT('Ctrl Pts',(-1.5099621785381,1.24211451030917,2.94914292761129));
#77419=CARTESIAN_POINT('Ctrl Pts',(-1.46448809043197,1.29359600841334,2.94523776209494));
#77420=CARTESIAN_POINT('Ctrl Pts',(-1.41902690695965,1.34506289710126,2.94133370478621));
#77421=CARTESIAN_POINT('Ctrl Pts',(-1.37083571608951,1.39414591556065,2.93742964747748));
#77422=CARTESIAN_POINT('Ctrl Pts',(-1.32020020520382,1.44055108141982,2.93352559016876));
#77423=CARTESIAN_POINT('Ctrl Pts',(-1.26956169702248,1.48695899416548,2.92962130176502));
#77424=CARTESIAN_POINT('Ctrl Pts',(-1.21647894593077,1.5306884091681,2.92571701336128));
#77425=CARTESIAN_POINT('Ctrl Pts',(-1.16127253351463,1.57148404475022,2.92181272495754));
#77426=CARTESIAN_POINT('Ctrl Pts',(-1.10600731722641,1.6123231343666,2.91790427784713));
#77427=CARTESIAN_POINT('Ctrl Pts',(-1.04861432161665,1.65022191522982,2.91399583073671));
#77428=CARTESIAN_POINT('Ctrl Pts',(-0.98944425255216,1.68496767657172,2.9100873836263));
#77429=CARTESIAN_POINT('Ctrl Pts',(-0.930238766349994,1.71973423551336,
2.90617659705589));
#77430=CARTESIAN_POINT('Ctrl Pts',(-0.869254526509263,1.75134379249947,
2.90226581048548));
#77431=CARTESIAN_POINT('Ctrl Pts',(-0.806865544602388,1.77963029670027,
2.89835502391507));
#77432=CARTESIAN_POINT('Ctrl Pts',(-0.744368835685812,1.80796564318731,
2.89443748459233));
#77433=CARTESIAN_POINT('Ctrl Pts',(-0.680463001491532,1.83296630582697,
2.8905199452696));
#77434=CARTESIAN_POINT('Ctrl Pts',(-0.615539825796965,1.85451522583608,
2.88660240594686));
#77435=CARTESIAN_POINT('Ctrl Pts',(-0.584896966461044,1.86468602413139,
2.88475338046212));
#77436=CARTESIAN_POINT('Ctrl Pts',(-0.55402765674044,1.87408860595769,2.88290435497738));
#77437=CARTESIAN_POINT('Ctrl Pts',(-0.522973845095926,1.88271462451047,
2.88105532949264));
#77438=CARTESIAN_POINT('Ctrl Pts',(-0.457170309580566,1.90099329911221,
2.87713721420467));
#77439=CARTESIAN_POINT('Ctrl Pts',(-0.390276877561027,1.91585416506222,
2.87321909891671));
#77440=CARTESIAN_POINT('Ctrl Pts',(-0.322681570578035,1.92717217809133,
2.86930098362874));
#77441=CARTESIAN_POINT('Ctrl Pts',(-0.25518805142159,1.93847314798537,2.86538876840185));
#77442=CARTESIAN_POINT('Ctrl Pts',(-0.186995236123241,1.94624177242017,
2.86147655317495));
#77443=CARTESIAN_POINT('Ctrl Pts',(-0.118504816070256,1.95040319128332,
2.85756433794806));
#77444=CARTESIAN_POINT('Ctrl Pts',(-0.0500949371229088,1.95455971653834,
2.85365672327902));
#77445=CARTESIAN_POINT('Ctrl Pts',(0.018611362888003,1.95511743097582,2.84974910860998));
#77446=CARTESIAN_POINT('Ctrl Pts',(0.0872055421906917,1.95205307136134,
2.84584149394094));
#77447=CARTESIAN_POINT('Ctrl Pts',(0.155756729116554,1.94899063237779,2.84193632842493));
#77448=CARTESIAN_POINT('Ctrl Pts',(0.2241954444467,1.94231064457378,2.83803116290892));
#77449=CARTESIAN_POINT('Ctrl Pts',(0.292112973773808,1.932041927742,2.83412599739292));
#77450=CARTESIAN_POINT('Ctrl Pts',(0.360011229468601,1.92177612496605,2.83022194008454));
#77451=CARTESIAN_POINT('Ctrl Pts',(0.427388106646916,1.90792368837881,2.82631788277616));
#77452=CARTESIAN_POINT('Ctrl Pts',(0.493841654345922,1.89056510610793,2.82241382546779));
#77453=CARTESIAN_POINT('Ctrl Pts',(0.560299135666208,1.87320549632097,2.81850953706441));
#77454=CARTESIAN_POINT('Ctrl Pts',(0.625832703735697,1.85233945560431,2.81460524866103));
#77455=CARTESIAN_POINT('Ctrl Pts',(0.690053985753285,1.82809778095867,2.81070096025765));
#77456=CARTESIAN_POINT('Ctrl Pts',(0.754343673955492,1.80383028495881,2.80679251314761));
#77457=CARTESIAN_POINT('Ctrl Pts',(0.817317825459981,1.7761801533597,2.80288406603757));
#77458=CARTESIAN_POINT('Ctrl Pts',(0.878607484600926,1.74532658491276,2.79897561892752));
#77459=CARTESIAN_POINT('Ctrl Pts',(0.939933829592058,1.71445454859692,2.7950648323575));
#77460=CARTESIAN_POINT('Ctrl Pts',(0.99957324842819,1.68037550339476,2.79115404578747));
#77461=CARTESIAN_POINT('Ctrl Pts',(1.05718333684116,1.64331354047406,2.78724325921744));
#77462=CARTESIAN_POINT('Ctrl Pts',(1.11489290055181,1.60618758268899,2.78332571989509));
#77463=CARTESIAN_POINT('Ctrl Pts',(1.1705657414821,1.56606871482815,2.77940818057274));
#77464=CARTESIAN_POINT('Ctrl Pts',(1.22389096795314,1.5232225374392,2.7754906412504));
#77465=CARTESIAN_POINT('Ctrl Pts',(1.24905975243211,1.50299972216366,2.77364161576251));
#77466=CARTESIAN_POINT('Ctrl Pts',(1.2737060714098,1.48216989278257,2.77179259027463));
#77467=CARTESIAN_POINT('Ctrl Pts',(1.29780015455336,1.46076375873762,2.76994356478675));
#77468=CARTESIAN_POINT('Ctrl Pts',(1.34885591135648,1.41540381009871,2.7660254494939));
#77469=CARTESIAN_POINT('Ctrl Pts',(1.39763192331083,1.36727401419716,2.76210733420104));
#77470=CARTESIAN_POINT('Ctrl Pts',(1.4438126318655,1.31663247873718,2.75818921890819));
#77471=CARTESIAN_POINT('Ctrl Pts',(1.48992379958754,1.26606720140861,2.75427700367639));
#77472=CARTESIAN_POINT('Ctrl Pts',(1.53344709136623,1.21299805153902,2.75036478844458));
#77473=CARTESIAN_POINT('Ctrl Pts',(1.57410168834624,1.15772184688099,2.74645257321278));
#77474=CARTESIAN_POINT('Ctrl Pts',(1.614708477674,1.10251064411121,2.74254495853883));
#77475=CARTESIAN_POINT('Ctrl Pts',(1.65245298183955,1.04509793538905,2.73863734386487));
#77476=CARTESIAN_POINT('Ctrl Pts',(1.68709400825014,0.985814286428475,2.73472972919092));
#77477=CARTESIAN_POINT('Ctrl Pts',(1.72171332290509,0.926567794337453,2.73082456367));
#77478=CARTESIAN_POINT('Ctrl Pts',(1.7532327707603,0.865453111888877,2.72691939814908));
#77479=CARTESIAN_POINT('Ctrl Pts',(1.78145481681984,0.802829207010667,2.72301423262816));
#77480=CARTESIAN_POINT('Ctrl Pts',(1.80966885402884,0.740223073540446,2.71911017531488));
#77481=CARTESIAN_POINT('Ctrl Pts',(1.83458714503851,0.676109016099035,2.7152061180016));
#77482=CARTESIAN_POINT('Ctrl Pts',(1.85605922720639,0.610868353331555,2.71130206068832));
#77483=CARTESIAN_POINT('Ctrl Pts',(1.87753258038291,0.545623828738059,2.70739777228006));
#77484=CARTESIAN_POINT('Ctrl Pts',(1.8955591683825,0.479253034445765,2.70349348387179));
#77485=CARTESIAN_POINT('Ctrl Pts',(1.91003815619439,0.412153177691916,2.69958919546352));
#77486=CARTESIAN_POINT('Ctrl Pts',(1.9245325664997,0.344981848600845,2.69568074834865));
#77487=CARTESIAN_POINT('Ctrl Pts',(1.93547173140084,0.277080388989802,2.69177230123377));
#77488=CARTESIAN_POINT('Ctrl Pts',(1.94280600936491,0.208855955087703,2.68786385411889));
#77489=CARTESIAN_POINT('Ctrl Pts',(1.95014467737165,0.140590684421846,2.68395306754406));
#77490=CARTESIAN_POINT('Ctrl Pts',(1.9538741373926,0.0720025459420695,2.68004228096922));
#77491=CARTESIAN_POINT('Ctrl Pts',(1.95399686406196,0.00350074792200107,
2.67613149439438));
#77492=CARTESIAN_POINT('Ctrl Pts',(1.95411980264337,-0.0651193321011138,
2.67221395506731));
#77493=CARTESIAN_POINT('Ctrl Pts',(1.95062360334309,-0.133652283136143,
2.66829641574024));
#77494=CARTESIAN_POINT('Ctrl Pts',(1.94356270676489,-0.20169284784722,2.66437887641317));
#77495=CARTESIAN_POINT('Ctrl Pts',(1.94023005931933,-0.233807071822553,
2.66252985096907));
#77496=CARTESIAN_POINT('Ctrl Pts',(1.93610404326396,-0.265811739818377,
2.66068082552497));
#77497=CARTESIAN_POINT('Ctrl Pts',(1.93119430378674,-0.297665182750104,
2.65883180008087));
#77498=CARTESIAN_POINT('Ctrl Pts',(1.92079048519854,-0.365163151472968,
2.65491368479703));
#77499=CARTESIAN_POINT('Ctrl Pts',(1.90682305849002,-0.432248824807374,
2.6509955695132));
#77500=CARTESIAN_POINT('Ctrl Pts',(1.88933763808645,-0.498517090288694,
2.64707745422936));
#77501=CARTESIAN_POINT('Ctrl Pts',(1.87187854795656,-0.564685566258203,
2.64316523900656));
#77502=CARTESIAN_POINT('Ctrl Pts',(1.85091210235727,-0.63003860547196,2.63925302378377));
#77503=CARTESIAN_POINT('Ctrl Pts',(1.82653528100206,-0.694179276019334,
2.63534080856097));
#77504=CARTESIAN_POINT('Ctrl Pts',(1.80218712549705,-0.758244520536934,
2.63143319389597));
#77505=CARTESIAN_POINT('Ctrl Pts',(1.77443673291253,-0.821099770196362,
2.62752557923097));
#77506=CARTESIAN_POINT('Ctrl Pts',(1.7434309311173,-0.88236307063673,2.62361796456596));
#77507=CARTESIAN_POINT('Ctrl Pts',(1.71244456264873,-0.943587973433383,
2.61971279905396));
#77508=CARTESIAN_POINT('Ctrl Pts',(1.6782070540418,-1.00322246839439,2.61580763354195));
#77509=CARTESIAN_POINT('Ctrl Pts',(1.64091277790259,-1.06090586543576,2.61190246802994));
#77510=CARTESIAN_POINT('Ctrl Pts',(1.60362908513036,-1.11857289308691,2.60799841072552));
#77511=CARTESIAN_POINT('Ctrl Pts',(1.5632906137981,-1.17428950910011,2.6040943534211));
#77512=CARTESIAN_POINT('Ctrl Pts',(1.52013605046243,-1.22772243935039,2.60019029611667));
#77513=CARTESIAN_POINT('Ctrl Pts',(1.47697893265452,-1.28115853248605,2.5962860077172));
#77514=CARTESIAN_POINT('Ctrl Pts',(1.43100570294498,-1.33231029042934,2.59238171931772));
#77515=CARTESIAN_POINT('Ctrl Pts',(1.38249531981184,-1.38087750749238,2.58847743091825));
#77516=CARTESIAN_POINT('Ctrl Pts',(1.3339332651734,-1.42949645659816,2.58456898381201));
#77517=CARTESIAN_POINT('Ctrl Pts',(1.28282901206506,-1.47552502208498,2.58066053670577));
#77518=CARTESIAN_POINT('Ctrl Pts',(1.22949765098527,-1.51870060453721,2.57675208959952));
#77519=CARTESIAN_POINT('Ctrl Pts',(1.1761343676139,-1.56190203038636,2.57284130303324));
#77520=CARTESIAN_POINT('Ctrl Pts',(1.12054172136735,-1.60224678562586,2.56893051646696));
#77521=CARTESIAN_POINT('Ctrl Pts',(1.06306480169621,-1.63951493661833,2.56501972990067));
#77522=CARTESIAN_POINT('Ctrl Pts',(1.0054886366679,-1.67684743850117,2.56110219058195));
#77523=CARTESIAN_POINT('Ctrl Pts',(0.94602213063127,-1.7110924881611,2.55718465126322));
#77524=CARTESIAN_POINT('Ctrl Pts',(0.88503524782068,-1.74207594843479,2.5532671119445));
#77525=CARTESIAN_POINT('Ctrl Pts',(0.856250264768582,-1.7566997222329,2.55141808642133));
#77526=CARTESIAN_POINT('Ctrl Pts',(0.827126876633474,-1.7705976045977,2.54956906089816));
#77527=CARTESIAN_POINT('Ctrl Pts',(0.797705319577693,-1.78375509056525,
2.54772003537499));
#77528=CARTESIAN_POINT('Ctrl Pts',(0.735360559618111,-1.8116360182389,2.54380192009024));
#77529=CARTESIAN_POINT('Ctrl Pts',(0.671428735074593,-1.83629972407899,
2.5398838048055));
#77530=CARTESIAN_POINT('Ctrl Pts',(0.606274899919665,-1.85756473527234,
2.53596568952076));
#77531=CARTESIAN_POINT('Ctrl Pts',(0.541219176122421,-1.87879772472646,
2.53205347429714));
#77532=CARTESIAN_POINT('Ctrl Pts',(0.474945557611846,-1.89664202535494,
2.52814125907352));
#77533=CARTESIAN_POINT('Ctrl Pts',(0.407840094249134,-1.9109637509704,2.52422904384991));
#77534=CARTESIAN_POINT('Ctrl Pts',(0.340813543357728,-1.92526863499495,
2.52032142918422));
#77535=CARTESIAN_POINT('Ctrl Pts',(0.272957569114629,-1.93605906862085,
2.51641381451854));
#77536=CARTESIAN_POINT('Ctrl Pts',(0.204672684488128,-1.94325116550188,
2.51250619985285));
#77537=CARTESIAN_POINT('Ctrl Pts',(0.136430598384416,-1.95043875463389,
2.50860103434024));
#77538=CARTESIAN_POINT('Ctrl Pts',(0.0677606232386084,-1.95403242943041,
2.50469586882763));
#77539=CARTESIAN_POINT('Ctrl Pts',(-0.000928795607166038,-1.95399977925759,
2.50079070331502));
#77540=CARTESIAN_POINT('Ctrl Pts',(-0.0695987217732036,-1.95396713835024,
2.49688664601008));
#77541=CARTESIAN_POINT('Ctrl Pts',(-0.138287589036128,-1.95031021560445,
2.49298258870514));
#77542=CARTESIAN_POINT('Ctrl Pts',(-0.206585940107364,-1.94304869968561,
2.4890785314002));
#77543=CARTESIAN_POINT('Ctrl Pts',(-0.274888333999684,-1.93578675393196,
2.48517424300029));
#77544=CARTESIAN_POINT('Ctrl Pts',(-0.342799676956306,-1.92491984594802,
2.48126995460038));
#77545=CARTESIAN_POINT('Ctrl Pts',(-0.409916440956191,-1.91051943497935,
2.47736566620048));
#77546=CARTESIAN_POINT('Ctrl Pts',(-0.477104695303022,-1.89610368521431,
2.47345721909392));
#77547=CARTESIAN_POINT('Ctrl Pts',(-0.543496199768764,-1.87814702455178,
2.46954877198737));
#77548=CARTESIAN_POINT('Ctrl Pts',(-0.608699413580939,-1.85677166714333,
2.46564032488082));
#77549=CARTESIAN_POINT('Ctrl Pts',(-0.673941655760215,-1.8353835151923,
2.4617295383143));
#77550=CARTESIAN_POINT('Ctrl Pts',(-0.737993732994083,-1.81057277164882,
2.45781875174779));
#77551=CARTESIAN_POINT('Ctrl Pts',(-0.800483669333991,-1.78250999860578,
2.45390796518127));
#77552=CARTESIAN_POINT('Ctrl Pts',(-0.863081507001688,-1.75439876959287,
2.44999042586242));
#77553=CARTESIAN_POINT('Ctrl Pts',(-0.92411138307502,-1.72302452865832,
2.44607288654357));
#77554=CARTESIAN_POINT('Ctrl Pts',(-0.983226296378127,-1.68860357991761,
2.44215534722472));
#77555=CARTESIAN_POINT('Ctrl Pts',(-1.01112773509442,-1.67235735814069,
2.44030632170618));
#77556=CARTESIAN_POINT('Ctrl Pts',(-1.03860300262693,-1.65543304013966,
2.43845729618765));
#77557=CARTESIAN_POINT('Ctrl Pts',(-1.0656180846027,-1.63785655591925,2.43660827066911));
#77558=CARTESIAN_POINT('Ctrl Pts',(-1.12282902060775,-1.60063412162017,
2.43269251425173));
#77559=CARTESIAN_POINT('Ctrl Pts',(-1.17820141177215,-1.56033624286675,
2.42877675783435));
#77560=CARTESIAN_POINT('Ctrl Pts',(-1.23138500423445,-1.51717071265778,
2.42486100141697));
#77561=CARTESIAN_POINT('Ctrl Pts',(-1.28448848720085,-1.47407020191638,
2.42095114323357));
#77562=CARTESIAN_POINT('Ctrl Pts',(-1.33540933515797,-1.42811091996629,
2.41704128505018));
#77563=CARTESIAN_POINT('Ctrl Pts',(-1.383825852666,-1.37954413104229,2.41313142686679));
#77564=CARTESIAN_POINT('Ctrl Pts',(-1.43218550557035,-1.3310343832139,2.40922616076369));
#77565=CARTESIAN_POINT('Ctrl Pts',(-1.47804632320186,-1.27992355751628,
2.40532089466059));
#77566=CARTESIAN_POINT('Ctrl Pts',(-1.5211207485684,-1.22650220883402,2.4014156285575));
#77567=CARTESIAN_POINT('Ctrl Pts',(-1.56416826194705,-1.17311423667798,
2.39751280238188));
#77568=CARTESIAN_POINT('Ctrl Pts',(-1.60443252781338,-1.11741898759487,
2.39360997620626));
#77569=CARTESIAN_POINT('Ctrl Pts',(-1.64166491920676,-1.05974161617153,
2.38970715003064));
#77570=CARTESIAN_POINT('Ctrl Pts',(-1.67888686115016,-1.00208043218031,
2.38580541920198));
#77571=CARTESIAN_POINT('Ctrl Pts',(-1.71307835079115,-0.9424386438043,2.38190368837333));
#77572=CARTESIAN_POINT('Ctrl Pts',(-1.74403397574648,-0.881170523475403,
2.37800195754467));
#77573=CARTESIAN_POINT('Ctrl Pts',(-1.77499156512658,-0.819898515109583,
2.3740999791146));
#77574=CARTESIAN_POINT('Ctrl Pts',(-1.80271266238679,-0.757000410711466,
2.37019800068453));
#77575=CARTESIAN_POINT('Ctrl Pts',(-1.82703856344133,-0.692853583160422,
2.36629602225445));
#77576=CARTESIAN_POINT('Ctrl Pts',(-1.85139041431136,-0.62863832655777,
2.36238988136314));
#77577=CARTESIAN_POINT('Ctrl Pts',(-1.87233966637274,-0.56317214996081,
2.35848374047183));
#77578=CARTESIAN_POINT('Ctrl Pts',(-1.88977676046506,-0.496849872301682,
2.35457759958051));
#77579=CARTESIAN_POINT('Ctrl Pts',(-1.90722439512171,-0.430487503430625,
2.35066909746266));
#77580=CARTESIAN_POINT('Ctrl Pts',(-1.921155546953,-0.363268485977131,2.3467605953448));
#77581=CARTESIAN_POINT('Ctrl Pts',(-1.93151188760856,-0.295597408694372,
2.34285209322695));
#77582=CARTESIAN_POINT('Ctrl Pts',(-1.94188602271753,-0.227810057732313,
2.33893687544947));
#77583=CARTESIAN_POINT('Ctrl Pts',(-1.94867304006574,-0.159569586596278,
2.33502165767198));
#77584=CARTESIAN_POINT('Ctrl Pts',(-1.95186658470269,-0.09128436624665,
2.3311064398945));
#77585=CARTESIAN_POINT('Ctrl Pts',(-1.95329041248901,-0.0608397020313837,
2.32936085732253));
#77586=CARTESIAN_POINT('Ctrl Pts',(-1.95400062983249,-0.0303861200153032,
2.32761527475057));
#77587=CARTESIAN_POINT('Ctrl Pts',(-1.95399999958081,4.04748477704995E-5,
2.3258696921786));
#77588=CARTESIAN_POINT('',(-1.95399927560819,-0.00168253459542325,1.62586971130486));
#77589=CARTESIAN_POINT('Ctrl Pts',(-1.95399999958079,4.04757954714693E-5,
2.32586969212423));
#77590=CARTESIAN_POINT('Ctrl Pts',(-1.95399995466613,0.00220876511265513,
2.32574529673723));
#77591=CARTESIAN_POINT('Ctrl Pts',(-1.95399630063441,0.0043770500002713,
2.32562090135023));
#77592=CARTESIAN_POINT('Ctrl Pts',(-1.95398903752031,0.00654532279172306,
2.32549650596323));
#77593=CARTESIAN_POINT('Ctrl Pts',(-1.95376026924542,0.0748399990821359,
2.32157839071464));
#77594=CARTESIAN_POINT('Ctrl Pts',(-1.94994624385776,0.143258050123744,
2.31766027546604));
#77595=CARTESIAN_POINT('Ctrl Pts',(-1.94253169459442,0.211392089483348,
2.31374216021745));
#77596=CARTESIAN_POINT('Ctrl Pts',(-1.93512831046787,0.279423529771489,
2.30982994502983));
#77597=CARTESIAN_POINT('Ctrl Pts',(-1.92413521564132,0.34717132210442,2.30591772984221));
#77598=CARTESIAN_POINT('Ctrl Pts',(-1.90958915417286,0.414228514548907,
2.30200551465458));
#77599=CARTESIAN_POINT('Ctrl Pts',(-1.89506019810102,0.481206851292453,
2.29809790002448));
#77600=CARTESIAN_POINT('Ctrl Pts',(-1.87698667693864,0.547495722583235,
2.29419028539438));
#77601=CARTESIAN_POINT('Ctrl Pts',(-1.85545685829453,0.612695558175348,
2.29028267076427));
#77602=CARTESIAN_POINT('Ctrl Pts',(-1.83394053376913,0.677854528847234,
2.28637750528697));
#77603=CARTESIAN_POINT('Ctrl Pts',(-1.80897236286763,0.741925351793865,
2.28247233980967));
#77604=CARTESIAN_POINT('Ctrl Pts',(-1.78069079593143,0.804522398249488,
2.27856717433237));
#77605=CARTESIAN_POINT('Ctrl Pts',(-1.75241725473457,0.867101680923494,
2.27466311706242));
#77606=CARTESIAN_POINT('Ctrl Pts',(-1.72083238653793,0.928207569318252,
2.27075905979247));
#77607=CARTESIAN_POINT('Ctrl Pts',(-1.686122546459,0.98747494060488,2.26685500252251));
#77608=CARTESIAN_POINT('Ctrl Pts',(-1.65141065177845,1.04674582014268,2.26295071415722));
#77609=CARTESIAN_POINT('Ctrl Pts',(-1.613573668758,1.10417754335984,2.25904642579192));
#77610=CARTESIAN_POINT('Ctrl Pts',(-1.57284270275735,1.15943168508668,2.25514213742662));
#77611=CARTESIAN_POINT('Ctrl Pts',(-1.5320683515978,1.21474468153647,2.25123369035389));
#77612=CARTESIAN_POINT('Ctrl Pts',(-1.48839415803323,1.26787507083712,2.24732524328116));
#77613=CARTESIAN_POINT('Ctrl Pts',(-1.44209256024326,1.31851622958955,2.24341679620843));
#77614=CARTESIAN_POINT('Ctrl Pts',(-1.39576324792855,1.36918770037685,2.23950600967533));
#77615=CARTESIAN_POINT('Ctrl Pts',(-1.34680375212342,1.4173666302547,2.23559522314223));
#77616=CARTESIAN_POINT('Ctrl Pts',(-1.29552253323629,1.46278411458322,2.23168443660913));
#77617=CARTESIAN_POINT('Ctrl Pts',(-1.24415276709222,1.50828002126094,2.22776689732273));
#77618=CARTESIAN_POINT('Ctrl Pts',(-1.19045366141732,1.55100465976764,2.22384935803633));
#77619=CARTESIAN_POINT('Ctrl Pts',(-1.13476509845124,1.59073070358781,2.21993181874993));
#77620=CARTESIAN_POINT('Ctrl Pts',(-1.10848084604684,1.60948086173847,2.21808279291906));
#77621=CARTESIAN_POINT('Ctrl Pts',(-1.08175379135749,1.62756366470977,2.2162337670882));
#77622=CARTESIAN_POINT('Ctrl Pts',(-1.05462155966551,1.64495877330974,2.21438474125734));
#77623=CARTESIAN_POINT('Ctrl Pts',(-0.997127927251723,1.68181928633346,
2.21046662598212));
#77624=CARTESIAN_POINT('Ctrl Pts',(-0.937585506254232,1.71573501490396,
2.2065485107069));
#77625=CARTESIAN_POINT('Ctrl Pts',(-0.876328230286788,1.74647211051377,
2.20263039543167));
#77626=CARTESIAN_POINT('Ctrl Pts',(-0.815163198082612,1.77716292092193,
2.19871818021799));
#77627=CARTESIAN_POINT('Ctrl Pts',(-0.752288871962661,1.80468437908947,
2.19480596500431));
#77628=CARTESIAN_POINT('Ctrl Pts',(-0.688067038568517,1.82884656284653,
2.19089374979063));
#77629=CARTESIAN_POINT('Ctrl Pts',(-0.623920726658672,1.85298033315157,
2.18698613513542));
#77630=CARTESIAN_POINT('Ctrl Pts',(-0.5584305127052,1.8737625020737,2.18307852048021));
#77631=CARTESIAN_POINT('Ctrl Pts',(-0.491979936173606,1.89105043359573,
2.179170905825));
#77632=CARTESIAN_POINT('Ctrl Pts',(-0.425571008491863,1.90832752965927,
2.1752657403232));
#77633=CARTESIAN_POINT('Ctrl Pts',(-0.358203387217572,1.92211460914435,
2.1713605748214));
#77634=CARTESIAN_POINT('Ctrl Pts',(-0.290276126774211,1.93231875481893,
2.1674554093196));
#77635=CARTESIAN_POINT('Ctrl Pts',(-0.22236814273083,1.94252000476074,2.16355135202579));
#77636=CARTESIAN_POINT('Ctrl Pts',(-0.153901320986516,1.94914026630843,
2.15964729473197));
#77637=CARTESIAN_POINT('Ctrl Pts',(-0.0852834807025519,1.95213798895448,
2.15574323743815));
#77638=CARTESIAN_POINT('Ctrl Pts',(-0.0166615786908634,1.95513588904613,
2.15183894904965));
#77639=CARTESIAN_POINT('Ctrl Pts',(0.0521108680863909,1.95451080561036,
2.14793466066116));
#77640=CARTESIAN_POINT('Ctrl Pts',(0.120624188422045,1.95027326422928,2.14403037227266));
#77641=CARTESIAN_POINT('Ctrl Pts',(0.189210486659719,1.94603120917293,2.14012192517789));
#77642=CARTESIAN_POINT('Ctrl Pts',(0.257536615736428,1.93816904745832,2.13621347808311));
#77643=CARTESIAN_POINT('Ctrl Pts',(0.325197194094168,1.92674927921442,2.13230503098834));
#77644=CARTESIAN_POINT('Ctrl Pts',(0.392898271707902,1.91532267549662,2.12839424443382));
#77645=CARTESIAN_POINT('Ctrl Pts',(0.459932525669257,1.90033433457933,2.1244834578793));
#77646=CARTESIAN_POINT('Ctrl Pts',(0.525906715726977,1.88189748029835,2.12057267132478));
#77647=CARTESIAN_POINT('Ctrl Pts',(0.591994823367634,1.86342879111534,2.11665513201814));
#77648=CARTESIAN_POINT('Ctrl Pts',(0.657018748055493,1.84149986135365,2.1127375927115));
#77649=CARTESIAN_POINT('Ctrl Pts',(0.720603128731074,1.81627286795321,2.10882005340486));
#77650=CARTESIAN_POINT('Ctrl Pts',(0.750614097239236,1.8043660679427,2.10697102778706));
#77651=CARTESIAN_POINT('Ctrl Pts',(0.780304706589721,1.79172523352155,2.10512200216926));
#77652=CARTESIAN_POINT('Ctrl Pts',(0.809637458011172,1.77837093616186,2.10327297655146));
#77653=CARTESIAN_POINT('Ctrl Pts',(0.871794037028583,1.75007296209412,2.09935486108842));
#77654=CARTESIAN_POINT('Ctrl Pts',(0.932588463664215,1.71845627840504,2.09543674562538));
#77655=CARTESIAN_POINT('Ctrl Pts',(0.991643125554879,1.68367452660535,2.09151863016234));
#77656=CARTESIAN_POINT('Ctrl Pts',(1.05060886049195,1.64894515060681,2.0876064147597));
#77657=CARTESIAN_POINT('Ctrl Pts',(1.1078396096568,1.61106041311778,2.08369419935705));
#77658=CARTESIAN_POINT('Ctrl Pts',(1.16297954867285,1.5702211848554,2.07978198395441));
#77659=CARTESIAN_POINT('Ctrl Pts',(1.21805464604646,1.52942998135844,2.07587436910949));
#77660=CARTESIAN_POINT('Ctrl Pts',(1.2710434228508,1.48569147852043,2.07196675426457));
#77661=CARTESIAN_POINT('Ctrl Pts',(1.32161797465028,1.43925047475458,2.06805913941965));
#77662=CARTESIAN_POINT('Ctrl Pts',(1.37216082813179,1.39283857854682,2.06415397372778));
#77663=CARTESIAN_POINT('Ctrl Pts',(1.42029209672764,1.34372787337746,2.06024880803592));
#77664=CARTESIAN_POINT('Ctrl Pts',(1.46571722372466,1.29220316517058,2.05634364234405));
#77665=CARTESIAN_POINT('Ctrl Pts',(1.51112945997923,1.24069307864531,2.05243958486009));
#77666=CARTESIAN_POINT('Ctrl Pts',(1.55383675401182,1.1867707178078,2.04853552737614));
#77667=CARTESIAN_POINT('Ctrl Pts',(1.59358294342151,1.13075611978713,2.04463146989218));
#77668=CARTESIAN_POINT('Ctrl Pts',(1.6333314855435,1.07473820607166,2.04072718131377));
#77669=CARTESIAN_POINT('Ctrl Pts',(1.67011829250234,1.01662821192939,2.03682289273536));
#77670=CARTESIAN_POINT('Ctrl Pts',(1.70372994251718,0.956775983692321,2.03291860415695));
#77671=CARTESIAN_POINT('Ctrl Pts',(1.73737739442587,0.896860003062237,2.02901015687389));
#77672=CARTESIAN_POINT('Ctrl Pts',(1.76784269853303,0.835198514510433,2.02510170959083));
#77673=CARTESIAN_POINT('Ctrl Pts',(1.79495842050219,0.772165959278372,2.02119326230777));
#77674=CARTESIAN_POINT('Ctrl Pts',(1.8220903729889,0.709095674975499,2.01728247556561));
#77675=CARTESIAN_POINT('Ctrl Pts',(1.84586858283634,0.644653152234568,2.01337168882346));
#77676=CARTESIAN_POINT('Ctrl Pts',(1.86617481225867,0.579230152954181,2.00946090208131));
#77677=CARTESIAN_POINT('Ctrl Pts',(1.88651610441448,0.513694187886812,2.00554336259002));
#77678=CARTESIAN_POINT('Ctrl Pts',(1.90337333019351,0.447174843903795,2.00162582309873));
#77679=CARTESIAN_POINT('Ctrl Pts',(1.91667907404262,0.380075422945414,1.99770828360744));
#77680=CARTESIAN_POINT('Ctrl Pts',(1.9229591992879,0.34840543348198,1.99585925968682));
#77681=CARTESIAN_POINT('Ctrl Pts',(1.92844890762637,0.316606311276526,1.9940102357662));
#77682=CARTESIAN_POINT('Ctrl Pts',(1.93314513506615,0.284720717142359,1.99216121184558));
#77683=CARTESIAN_POINT('Ctrl Pts',(1.94309652556393,0.217154569090327,1.98824309686718));
#77684=CARTESIAN_POINT('Ctrl Pts',(1.94952108028574,0.148932131488614,1.98432498188878));
#77685=CARTESIAN_POINT('Ctrl Pts',(1.95234299222131,0.0804539664923356,
1.98040686691037));
#77686=CARTESIAN_POINT('Ctrl Pts',(1.95516065480438,0.012078918768361,1.97649465199266));
#77687=CARTESIAN_POINT('Ctrl Pts',(1.95438642123413,-0.0565506045830932,
1.97258243707494));
#77688=CARTESIAN_POINT('Ctrl Pts',(1.9499959792906,-0.12502672014604,1.96867022215723));
#77689=CARTESIAN_POINT('Ctrl Pts',(1.94561070027235,-0.193422311453924,
1.96476260779533));
#77690=CARTESIAN_POINT('Ctrl Pts',(1.93761768967133,-0.261664364700758,
1.96085499343343));
#77691=CARTESIAN_POINT('Ctrl Pts',(1.92604468353289,-0.329344617436922,
1.95694737907154));
#77692=CARTESIAN_POINT('Ctrl Pts',(1.91447893093686,-0.396982450634276,
1.95304221386124));
#77693=CARTESIAN_POINT('Ctrl Pts',(1.89933771653323,-0.464058698052798,
1.94913704865094));
#77694=CARTESIAN_POINT('Ctrl Pts',(1.88070047635929,-0.530171404568323,
1.94523188344064));
#77695=CARTESIAN_POINT('Ctrl Pts',(1.86206852505165,-0.596265349654448,
1.94132782643608));
#77696=CARTESIAN_POINT('Ctrl Pts',(1.83994265086077,-0.66139582344277,1.93742376943153));
#77697=CARTESIAN_POINT('Ctrl Pts',(1.81445271556354,-0.725174008762105,
1.93351971242698));
#77698=CARTESIAN_POINT('Ctrl Pts',(1.78896127141129,-0.788955969376814,
1.9296154243251));
#77699=CARTESIAN_POINT('Ctrl Pts',(1.7601055557336,-0.851385026801486,1.92571113622322));
#77700=CARTESIAN_POINT('Ctrl Pts',(1.72806365945861,-0.912092094504996,
1.92180684812134));
#77701=CARTESIAN_POINT('Ctrl Pts',(1.69598763326759,-0.97286382527044,1.91789840130725));
#77702=CARTESIAN_POINT('Ctrl Pts',(1.66071888352847,-1.03190946997123,1.91398995449316));
#77703=CARTESIAN_POINT('Ctrl Pts',(1.62248111169852,-1.08888522911349,1.91008150767908));
#77704=CARTESIAN_POINT('Ctrl Pts',(1.58422045204491,-1.14589509199835,1.90617072140228));
#77705=CARTESIAN_POINT('Ctrl Pts',(1.5429875287408,-1.20083221010605,1.90225993512548));
#77706=CARTESIAN_POINT('Ctrl Pts',(1.49904728425969,-1.25338471330779,1.89834914884868));
#77707=CARTESIAN_POINT('Ctrl Pts',(1.45503116810331,-1.30602795898273,1.89443160981231));
#77708=CARTESIAN_POINT('Ctrl Pts',(1.40829873554755,-1.35627801184808,1.89051407077594));
#77709=CARTESIAN_POINT('Ctrl Pts',(1.35915219619628,-1.40385943298281,1.88659653173957));
#77710=CARTESIAN_POINT('Ctrl Pts',(1.33595565971069,-1.42631725373596,1.88474750353961));
#77711=CARTESIAN_POINT('Ctrl Pts',(1.3122218116172,-1.44818115840508,1.88289847533965));
#77712=CARTESIAN_POINT('Ctrl Pts',(1.28798482614457,-1.46942542771702,1.8810494471397));
#77713=CARTESIAN_POINT('Ctrl Pts',(1.23662633221909,-1.51444231637426,1.87713133184096));
#77714=CARTESIAN_POINT('Ctrl Pts',(1.18280308149621,-1.55685262414134,1.87321321654222));
#77715=CARTESIAN_POINT('Ctrl Pts',(1.12681042945077,-1.5963753493715,1.86929510124348));
#77716=CARTESIAN_POINT('Ctrl Pts',(1.07090209351593,-1.63583855960549,1.86538288600896));
#77717=CARTESIAN_POINT('Ctrl Pts',(1.01283123827593,-1.67242253565744,1.86147067077444));
#77718=CARTESIAN_POINT('Ctrl Pts',(0.952927307329273,-1.70588556091731,
1.85755845553992));
#77719=CARTESIAN_POINT('Ctrl Pts',(0.893093820302652,-1.73930923539272,
1.85365084086788));
#77720=CARTESIAN_POINT('Ctrl Pts',(0.831431966017609,-1.76961900915968,
1.84974322619584));
#77721=CARTESIAN_POINT('Ctrl Pts',(0.76829974480643,-1.79661668202496,1.84583561152381));
#77722=CARTESIAN_POINT('Ctrl Pts',(0.705207092658434,-1.82359743369528,
1.84193044600766));
#77723=CARTESIAN_POINT('Ctrl Pts',(0.640646352942322,-1.84727000943735,
1.83802528049152));
#77724=CARTESIAN_POINT('Ctrl Pts',(0.574998277036943,-1.86748306054019,
1.83412011497538));
#77725=CARTESIAN_POINT('Ctrl Pts',(0.509368830786191,-1.88769037556995,
1.8302160576697));
#77726=CARTESIAN_POINT('Ctrl Pts',(0.442653130781479,-1.90443997021895,
1.82631200036403));
#77727=CARTESIAN_POINT('Ctrl Pts',(0.375248250188822,-1.91762998274699,
1.82240794305835));
#77728=CARTESIAN_POINT('Ctrl Pts',(0.307839379710729,-1.93082077602916,
1.81850365466049));
#77729=CARTESIAN_POINT('Ctrl Pts',(0.239741730868927,-1.94045147692993,
1.81459936626262));
#77730=CARTESIAN_POINT('Ctrl Pts',(0.17136196882874,-1.94647144228708,1.81069507786476));
#77731=CARTESIAN_POINT('Ctrl Pts',(0.102909371214237,-1.95249781988699,
1.80678663076439));
#77732=CARTESIAN_POINT('Ctrl Pts',(0.0341745516291942,-1.95490574325592,
1.80287818366402));
#77733=CARTESIAN_POINT('Ctrl Pts',(-0.0344323210079937,-1.95369660266634,
1.79896973656365));
#77734=CARTESIAN_POINT('Ctrl Pts',(-0.103080259282135,-1.95248673832816,
1.79505895000568));
#77735=CARTESIAN_POINT('Ctrl Pts',(-0.171599607462033,-1.9476555357918,
1.79114816344771));
#77736=CARTESIAN_POINT('Ctrl Pts',(-0.239584643263601,-1.93925635198451,
1.78723737688973));
#77737=CARTESIAN_POINT('Ctrl Pts',(-0.307687068716483,-1.93084266532012,
1.78331983758294));
#77738=CARTESIAN_POINT('Ctrl Pts',(-0.375252856385077,-1.91884878728751,
1.77940229827615));
#77739=CARTESIAN_POINT('Ctrl Pts',(-0.441886668296444,-1.90337914572527,
1.77548475896936));
#77740=CARTESIAN_POINT('Ctrl Pts',(-0.473336925339729,-1.89607768435688,
1.77363573345751));
#77741=CARTESIAN_POINT('Ctrl Pts',(-0.504579789940459,-1.88800264381133,
1.77178670794566));
#77742=CARTESIAN_POINT('Ctrl Pts',(-0.535575116404463,-1.87916877759512,
1.76993768243381));
#77743=CARTESIAN_POINT('Ctrl Pts',(-0.601254738444671,-1.86044966537967,
1.76601956603965));
#77744=CARTESIAN_POINT('Ctrl Pts',(-0.66608198802966,-1.83824590595076,
1.7621014496455));
#77745=CARTESIAN_POINT('Ctrl Pts',(-0.729660572885464,-1.81265315170235,
1.75818333325134));
#77746=CARTESIAN_POINT('Ctrl Pts',(-0.793143418573306,-1.78709893604367,
1.75427111691306));
#77747=CARTESIAN_POINT('Ctrl Pts',(-0.855380878611871,-1.75816603597598,
1.75035890057479));
#77748=CARTESIAN_POINT('Ctrl Pts',(-0.915991167107972,-1.72600005265938,
1.74644668423651));
#77749=CARTESIAN_POINT('Ctrl Pts',(-0.976530181170627,-1.69387189480598,
1.74253906845385));
#77750=CARTESIAN_POINT('Ctrl Pts',(-1.03544539143528,-1.65851843388911,
1.73863145267119));
#77751=CARTESIAN_POINT('Ctrl Pts',(-1.09237607387451,-1.62013286900381,
1.73472383688853));
#77752=CARTESIAN_POINT('Ctrl Pts',(-1.1492710742204,-1.58177136280268,1.73081867025815));
#77753=CARTESIAN_POINT('Ctrl Pts',(-1.20418360718472,-1.54038179681547,
1.72691350362778));
#77754=CARTESIAN_POINT('Ctrl Pts',(-1.25677996197875,-1.49620190053638,
1.72300833699741));
#77755=CARTESIAN_POINT('Ctrl Pts',(-1.30936139097415,-1.45203454163252,
1.7191042785756));
#77756=CARTESIAN_POINT('Ctrl Pts',(-1.35962757016161,-1.40507874059613,
1.71520022015379));
#77757=CARTESIAN_POINT('Ctrl Pts',(-1.40727750401264,-1.35561278641799,
1.71129616173197));
#77758=CARTESIAN_POINT('Ctrl Pts',(-1.45493025839965,-1.30614390420844,
1.70739187221777));
#77759=CARTESIAN_POINT('Ctrl Pts',(-1.49996612059321,-1.25416492989935,
1.70348758270357));
#77760=CARTESIAN_POINT('Ctrl Pts',(-1.54212191610968,-1.1999899982309,1.69958329318937));
#77761=CARTESIAN_POINT('Ctrl Pts',(-1.58432261431633,-1.14575736156264,
1.69567484498001));
#77762=CARTESIAN_POINT('Ctrl Pts',(-1.62363682094623,-1.089324488464,1.69176639677066));
#77763=CARTESIAN_POINT('Ctrl Pts',(-1.65984317018685,-1.03103668721539,
1.6878579485613));
#77764=CARTESIAN_POINT('Ctrl Pts',(-1.69607119123201,-0.97271399700772,
1.68394716089692));
#77765=CARTESIAN_POINT('Ctrl Pts',(-1.72918741547169,-0.912534599962121,
1.68003637323254));
#77766=CARTESIAN_POINT('Ctrl Pts',(-1.75901654307767,-0.850868263116606,
1.67612558556816));
#77767=CARTESIAN_POINT('Ctrl Pts',(-1.78889717645636,-0.789095447383394,
1.67220804517057));
#77768=CARTESIAN_POINT('Ctrl Pts',(-1.81547919475816,-0.72583102078802,
1.66829050477299));
#77769=CARTESIAN_POINT('Ctrl Pts',(-1.8386358331236,-0.661463735327861,
1.6643729643754));
#77770=CARTESIAN_POINT('Ctrl Pts',(-1.84956539097328,-0.631083420233703,
1.66252394882624));
#77771=CARTESIAN_POINT('Ctrl Pts',(-1.85973260901456,-0.600457624876922,
1.66067493327709));
#77772=CARTESIAN_POINT('Ctrl Pts',(-1.86912810006625,-0.569628076504945,
1.65882591772793));
#77773=CARTESIAN_POINT('Ctrl Pts',(-1.89347575123831,-0.489735808456053,
1.65403434426414));
#77774=CARTESIAN_POINT('Ctrl Pts',(-1.91271599857493,-0.408219073121368,
1.64924277080036));
#77775=CARTESIAN_POINT('Ctrl Pts',(-1.92666967351934,-0.325668495775797,
1.64445119733657));
#77776=CARTESIAN_POINT('Ctrl Pts',(-1.94042573682919,-0.24428699787267,
1.63972748202973));
#77777=CARTESIAN_POINT('Ctrl Pts',(-1.94904385906538,-0.161900712891478,
1.63500376672289));
#77778=CARTESIAN_POINT('Ctrl Pts',(-1.95239846276358,-0.0790964133094032,
1.63028005141604));
#77779=CARTESIAN_POINT('Ctrl Pts',(-1.95344248159806,-0.0533260821115529,
1.62880993804565));
#77780=CARTESIAN_POINT('Ctrl Pts',(-1.9539770316284,-0.0275154182212127,
1.62733982467525));
#77781=CARTESIAN_POINT('Ctrl Pts',(-1.95399927560819,-0.00168253459542325,
1.62586971130486));
#77782=CARTESIAN_POINT('',(-1.95128228942929,0.000979822369055472,0.92586969212423));
#77783=CARTESIAN_POINT('Ctrl Pts',(-1.95279539392324,-0.00168116113097749,
1.62586969212423));
#77784=CARTESIAN_POINT('Ctrl Pts',(-1.94903666796486,0.455824327828861,
1.59981784575684));
#77785=CARTESIAN_POINT('Ctrl Pts',(-1.56045216071061,1.56950483372459,1.53672874448747));
#77786=CARTESIAN_POINT('Ctrl Pts',(0.294933807152575,2.29043279904662,1.43660238831617));
#77787=CARTESIAN_POINT('Ctrl Pts',(2.08404446099042,0.994902325724279,1.32549062361027));
#77788=CARTESIAN_POINT('Ctrl Pts',(1.96642629593332,-1.21088396446362,1.21437885890441));
#77789=CARTESIAN_POINT('Ctrl Pts',(0.0496914524290246,-2.3088068886435,
1.10326709419851));
#77790=CARTESIAN_POINT('Ctrl Pts',(-1.64863658953277,-1.43079008949268,
1.00709737193847));
#77791=CARTESIAN_POINT('Ctrl Pts',(-1.94952095194778,-0.387800287767629,
0.947964904580365));
#77792=CARTESIAN_POINT('Ctrl Pts',(-1.95128228942929,0.000979822369055472,
0.92586969212423));
#77793=CARTESIAN_POINT('Ctrl Pts',(-1.95128228942929,0.000979822369055472,
0.92586969212423));
#77794=CARTESIAN_POINT('Ctrl Pts',(-1.9524734062589,0.263895099571634,0.910927649678405));
#77795=CARTESIAN_POINT('Ctrl Pts',(-1.78055803458398,1.17701113300587,0.858948352330618));
#77796=CARTESIAN_POINT('Ctrl Pts',(-0.393209187557522,2.27560539746712,
0.769931800080873));
#77797=CARTESIAN_POINT('Ctrl Pts',(1.69826458517494,1.56495710236821,0.65882003537499));
#77798=CARTESIAN_POINT('Ctrl Pts',(2.23594625441704,-0.577613834845561,
0.547708270669108));
#77799=CARTESIAN_POINT('Ctrl Pts',(0.727960807006617,-2.19149445634993,
0.436596505963225));
#77800=CARTESIAN_POINT('Ctrl Pts',(-1.37113217187641,-1.81423802364418,
0.329317307026286));
#77801=CARTESIAN_POINT('Ctrl Pts',(-1.95230380632447,-0.579097070743308,
0.259075362991307));
#77802=CARTESIAN_POINT('Ctrl Pts',(-1.95633563170751,0.00125569164583384,
0.22587067385829));
#77803=CARTESIAN_POINT('Origin',(0.,0.,-1.2940562256037));
#77804=CARTESIAN_POINT('',(-0.840025297123077,1.30917445368953,9.44449999999999));
#77805=CARTESIAN_POINT('Ctrl Pts',(-1.55549943430639,-0.00132660186739831,
8.85594377445462));
#77806=CARTESIAN_POINT('Ctrl Pts',(-1.55543973182031,-0.0713304105477647,
8.86094835465193));
#77807=CARTESIAN_POINT('Ctrl Pts',(-1.55065051292772,-0.141127590573169,
8.86595293484923));
#77808=CARTESIAN_POINT('Ctrl Pts',(-1.54123780639817,-0.210157736305244,
8.87095751504654));
#77809=CARTESIAN_POINT('Ctrl Pts',(-1.53168240264542,-0.280234383389748,
8.87603796499451));
#77810=CARTESIAN_POINT('Ctrl Pts',(-1.51736233716873,-0.349520592233542,
8.88111841494248));
#77811=CARTESIAN_POINT('Ctrl Pts',(-1.49843717350737,-0.417452137437612,
8.88619886489045));
#77812=CARTESIAN_POINT('Ctrl Pts',(-1.49503204889598,-0.429674772898193,
8.8871129687505));
#77813=CARTESIAN_POINT('Ctrl Pts',(-1.49147796610598,-0.441853609476848,
8.88802707261054));
#77814=CARTESIAN_POINT('Ctrl Pts',(-1.48777601674914,-0.453985433671693,
8.88894117647058));
#77815=CARTESIAN_POINT('Ctrl Pts',(-1.47100147783177,-0.508958027156549,
8.8930832295612));
#77816=CARTESIAN_POINT('Ctrl Pts',(-1.45114017341744,-0.563117052848065,
8.89722528265182));
#77817=CARTESIAN_POINT('Ctrl Pts',(-1.42828994739172,-0.616090964208816,
8.90136733574244));
#77818=CARTESIAN_POINT('Ctrl Pts',(-1.40548044525633,-0.668970464960515,
8.90550200682662));
#77819=CARTESIAN_POINT('Ctrl Pts',(-1.37969279869364,-0.720668567521905,
8.9096366779108));
#77820=CARTESIAN_POINT('Ctrl Pts',(-1.35107433676145,-0.770829674146372,
8.91377134899497));
#77821=CARTESIAN_POINT('Ctrl Pts',(-1.32248438637216,-0.820940807066931,
8.91790190085526));
#77822=CARTESIAN_POINT('Ctrl Pts',(-1.29106946520881,-0.869517526065842,
8.92203245271556));
#77823=CARTESIAN_POINT('Ctrl Pts',(-1.25702387485257,-0.916226624831783,
8.92616300457585));
#77824=CARTESIAN_POINT('Ctrl Pts',(-1.22299901527941,-0.962907281846979,
8.93029104129178));
#77825=CARTESIAN_POINT('Ctrl Pts',(-1.1863469685452,-1.00772215129541,8.93441907800771));
#77826=CARTESIAN_POINT('Ctrl Pts',(-1.14730541416721,-1.05036685811321,
8.93854711472363));
#77827=CARTESIAN_POINT('Ctrl Pts',(-1.10827251054623,-1.09300211579399,
8.94267423675665));
#77828=CARTESIAN_POINT('Ctrl Pts',(-1.0668515029429,-1.13346778021883,8.94680135878967));
#77829=CARTESIAN_POINT('Ctrl Pts',(-1.02331895594617,-1.17149415892749,
8.95092848082269));
#77830=CARTESIAN_POINT('Ctrl Pts',(-0.979746190478903,-1.20955566911588,
8.95505941578528));
#77831=CARTESIAN_POINT('Ctrl Pts',(-0.934058380981908,-1.24517304472543,
8.95919035074787));
#77832=CARTESIAN_POINT('Ctrl Pts',(-0.886566399666688,-1.27811590592639,
8.96332128571047));
#77833=CARTESIAN_POINT('Ctrl Pts',(-0.839054400608773,-1.31107265245496,
8.96745396185106));
#77834=CARTESIAN_POINT('Ctrl Pts',(-0.789737159647339,-1.3413523627722,
8.97158663799166));
#77835=CARTESIAN_POINT('Ctrl Pts',(-0.738953100619293,-1.36876899624631,
8.97571931413225));
#77836=CARTESIAN_POINT('Ctrl Pts',(-0.688068277551448,-1.39624002889212,
8.97986019019131));
#77837=CARTESIAN_POINT('Ctrl Pts',(-0.635711294687051,-1.420836408742,8.98400106625037));
#77838=CARTESIAN_POINT('Ctrl Pts',(-0.582242820401354,-1.44241933850426,
8.98814194230942));
#77839=CARTESIAN_POINT('Ctrl Pts',(-0.53097645972821,-1.4631133694516,8.9921122752651));
#77840=CARTESIAN_POINT('Ctrl Pts',(-0.478688799021197,-1.48103727978222,
8.99608260822078));
#77841=CARTESIAN_POINT('Ctrl Pts',(-0.425708788396775,-1.49611238798486,
9.00005294117646));
#77842=CARTESIAN_POINT('Ctrl Pts',(-0.370250558459497,-1.51189265694248,
9.00420899240009));
#77843=CARTESIAN_POINT('Ctrl Pts',(-0.313799216031233,-1.52461775351157,
9.00836504362372));
#77844=CARTESIAN_POINT('Ctrl Pts',(-0.256722338787837,-1.53416879474434,
9.01252109484735));
#77845=CARTESIAN_POINT('Ctrl Pts',(-0.199747628091171,-1.54370273979127,
9.01666970681673));
#77846=CARTESIAN_POINT('Ctrl Pts',(-0.142150112715516,-1.55007382314112,
9.02081831878611));
#77847=CARTESIAN_POINT('Ctrl Pts',(-0.0843106401441304,-1.55321343219742,
9.02496693075549));
#77848=CARTESIAN_POINT('Ctrl Pts',(-0.0265292103499676,-1.556349890609,
9.02911137953062));
#77849=CARTESIAN_POINT('Ctrl Pts',(0.0314931802133244,-1.5562612727405,
9.03325582830573));
#77850=CARTESIAN_POINT('Ctrl Pts',(0.0893691334599006,-1.55293058698212,
9.03740027708085));
#77851=CARTESIAN_POINT('Ctrl Pts',(0.147209030981919,-1.54960197618375,
9.04154214393559));
#77852=CARTESIAN_POINT('Ctrl Pts',(0.204902155333508,-1.54303533153495,
9.04568401079032));
#77853=CARTESIAN_POINT('Ctrl Pts',(0.262061867499625,-1.53326573939504,
9.04982587764506));
#77854=CARTESIAN_POINT('Ctrl Pts',(0.319207719778275,-1.52349851615172,
9.05396674019437));
#77855=CARTESIAN_POINT('Ctrl Pts',(0.375819905685316,-1.51052997465528,
9.0581076027437));
#77856=CARTESIAN_POINT('Ctrl Pts',(0.4315198464109,-1.4944466775879,9.06224846529302));
#77857=CARTESIAN_POINT('Ctrl Pts',(0.487267719514499,-1.47834954009871,
9.06639289124629));
#77858=CARTESIAN_POINT('Ctrl Pts',(0.542101278672587,-1.45913243303908,
9.07053731719956));
#77859=CARTESIAN_POINT('Ctrl Pts',(0.595656362187317,-1.4369320610891,9.07468174315283));
#77860=CARTESIAN_POINT('Ctrl Pts',(0.649232471956938,-1.41472297305377,
9.07882779624868));
#77861=CARTESIAN_POINT('Ctrl Pts',(0.701528636045423,-1.38952850838614,
9.08297384934453));
#77862=CARTESIAN_POINT('Ctrl Pts',(0.752202910871132,-1.36153260367756,
9.08711990244037));
#77863=CARTESIAN_POINT('Ctrl Pts',(0.802972913637875,-1.33348381236479,
9.09127378777709));
#77864=CARTESIAN_POINT('Ctrl Pts',(0.852114462357514,-1.30262328027436,
9.09542767311381));
#77865=CARTESIAN_POINT('Ctrl Pts',(0.899313161807077,-1.2691792966325,9.09958155845052));
#77866=CARTESIAN_POINT('Ctrl Pts',(0.943184497516362,-1.23809301139754,
9.10344260759446));
#77867=CARTESIAN_POINT('Ctrl Pts',(0.985377319286091,-1.20477534810784,
9.10730365673841));
#77868=CARTESIAN_POINT('Ctrl Pts',(1.02566651802248,-1.16943937158266,9.11116470588235));
#77869=CARTESIAN_POINT('Ctrl Pts',(1.06901228936252,-1.13142260265758,9.11531867663816));
#77870=CARTESIAN_POINT('Ctrl Pts',(1.11032977131098,-1.09091527354039,9.11947264739397));
#77871=CARTESIAN_POINT('Ctrl Pts',(1.14932007750667,-1.04816201488132,9.12362661814979));
#77872=CARTESIAN_POINT('Ctrl Pts',(1.18824256998146,-1.00548311464189,9.12777336412998));
#77873=CARTESIAN_POINT('Ctrl Pts',(1.22484557426173,-0.96056641928244,9.13192011011017));
#77874=CARTESIAN_POINT('Ctrl Pts',(1.25886528700759,-0.913694937693807,
9.13606685609037));
#77875=CARTESIAN_POINT('Ctrl Pts',(1.2928519207076,-0.866869031560226,9.14020956998477));
#77876=CARTESIAN_POINT('Ctrl Pts',(1.32425993691622,-0.818092523598639,
9.14435228387917));
#77877=CARTESIAN_POINT('Ctrl Pts',(1.35286540666698,-0.767681862130256,
9.14849499777358));
#77878=CARTESIAN_POINT('Ctrl Pts',(1.38145396231313,-0.717301007940313,
9.1526352621261));
#77879=CARTESIAN_POINT('Ctrl Pts',(1.40724300119445,-0.665288366385306,
9.15677552647862));
#77880=CARTESIAN_POINT('Ctrl Pts',(1.43005280857806,-0.61198792036934,9.16091579083114));
#77881=CARTESIAN_POINT('Ctrl Pts',(1.45285782014583,-0.558698680897996,
9.1650551846833));
#77882=CARTESIAN_POINT('Ctrl Pts',(1.47268463995099,-0.504122651506405,
9.16919457853547));
#77883=CARTESIAN_POINT('Ctrl Pts',(1.48940121121041,-0.44862487898575,9.17333397238763));
#77884=CARTESIAN_POINT('Ctrl Pts',(1.50613305510685,-0.393076402446755,
9.17747714808351));
#77885=CARTESIAN_POINT('Ctrl Pts',(1.51974882106387,-0.336604997763444,
9.18162032377938));
#77886=CARTESIAN_POINT('Ctrl Pts',(1.53016642110373,-0.279590725394439,
9.18576349947525));
#77887=CARTESIAN_POINT('Ctrl Pts',(1.54058840773718,-0.222552445726188,
9.18990841975988));
#77888=CARTESIAN_POINT('Ctrl Pts',(1.54780947771502,-0.164971358526727,
9.19405334004451));
#77889=CARTESIAN_POINT('Ctrl Pts',(1.55179929110059,-0.107234370141864,
9.19819826032914));
#77890=CARTESIAN_POINT('Ctrl Pts',(1.5557968462222,-0.0493853503206549,
9.20235122331545));
#77891=CARTESIAN_POINT('Ctrl Pts',(1.55655060718025,0.00861965443070754,
9.20650418630176));
#77892=CARTESIAN_POINT('Ctrl Pts',(1.55408244028937,0.0663929121535176,
9.21065714928806));
#77893=CARTESIAN_POINT('Ctrl Pts',(1.5517805958615,0.120273001000367,9.21453025638812));
#77894=CARTESIAN_POINT('Ctrl Pts',(1.54667699860277,0.173951210085379,9.21840336348818));
#77895=CARTESIAN_POINT('Ctrl Pts',(1.53882965619224,0.2271200986775,9.22227647058824));
#77896=CARTESIAN_POINT('Ctrl Pts',(1.53051710541967,0.283440960291726,9.2263791843138));
#77897=CARTESIAN_POINT('Ctrl Pts',(1.51908864750968,0.339437969704746,9.23048189803935));
#77898=CARTESIAN_POINT('Ctrl Pts',(1.50458123384946,0.394734797994868,9.23458461176491));
#77899=CARTESIAN_POINT('Ctrl Pts',(1.49002394797367,0.450221720495112,9.23870142941196));
#77900=CARTESIAN_POINT('Ctrl Pts',(1.47236650807424,0.505003095242158,9.24281824705901));
#77901=CARTESIAN_POINT('Ctrl Pts',(1.45169879005861,0.558704638375561,9.24693506470606));
#77902=CARTESIAN_POINT('Ctrl Pts',(1.43115897989575,0.612073834751231,9.25102640429573));
#77903=CARTESIAN_POINT('Ctrl Pts',(1.40764621358612,0.664376016200432,9.25511774388541));
#77904=CARTESIAN_POINT('Ctrl Pts',(1.38129899902813,0.715257523752038,9.25920908347508));
#77905=CARTESIAN_POINT('Ctrl Pts',(1.35496716769441,0.766109323357077,9.26329803427354));
#77906=CARTESIAN_POINT('Ctrl Pts',(1.32580441021765,0.815541619358912,9.26738698507201));
#77907=CARTESIAN_POINT('Ctrl Pts',(1.29399652331559,0.863222594495276,9.27147593587048));
#77908=CARTESIAN_POINT('Ctrl Pts',(1.26219434468097,0.910895012767786,9.27556415286274));
#77909=CARTESIAN_POINT('Ctrl Pts',(1.22774827427068,0.956816290476871,9.279652369855));
#77910=CARTESIAN_POINT('Ctrl Pts',(1.19088777442527,1.00068304608624,9.28374058684726));
#77911=CARTESIAN_POINT('Ctrl Pts',(1.15358469214915,1.04507650793688,9.2878778908845));
#77912=CARTESIAN_POINT('Ctrl Pts',(1.11380914503604,1.08736533131285,9.29201519492173));
#77913=CARTESIAN_POINT('Ctrl Pts',(1.07183952108797,1.12727117014226,9.29615249895897));
#77914=CARTESIAN_POINT('Ctrl Pts',(1.03030294825522,1.16676525241093,9.30024711345174));
#77915=CARTESIAN_POINT('Ctrl Pts',(0.986617827983286,1.20392500632945,9.30434172794452));
#77916=CARTESIAN_POINT('Ctrl Pts',(0.941087448215,1.23852116042165,9.30843634243729));
#77917=CARTESIAN_POINT('Ctrl Pts',(0.894845033952962,1.27365835228226,9.31259499124676));
#77918=CARTESIAN_POINT('Ctrl Pts',(0.846699616070225,1.30615074376982,9.31675364005623));
#77919=CARTESIAN_POINT('Ctrl Pts',(0.796996945149251,1.33580541974599,9.3209122888657));
#77920=CARTESIAN_POINT('Ctrl Pts',(0.747294274228271,1.36546009572216,9.32507093767517));
#77921=CARTESIAN_POINT('Ctrl Pts',(0.696034890907428,1.39227686998508,9.32922958648464));
#77922=CARTESIAN_POINT('Ctrl Pts',(0.643584947354596,1.41611393098811,9.33338823529411));
#77923=CARTESIAN_POINT('Ctrl Pts',(0.589802482825656,1.44055658623288,9.33765253696792));
#77924=CARTESIAN_POINT('Ctrl Pts',(0.534533878903967,1.46197317255622,9.34191683864173));
#77925=CARTESIAN_POINT('Ctrl Pts',(0.478142784720276,1.48018908502257,9.34618114031555));
#77926=CARTESIAN_POINT('Ctrl Pts',(0.42187304527927,1.49836579648737,9.35043626512837));
#77927=CARTESIAN_POINT('Ctrl Pts',(0.364486077933698,1.5133553832069,9.35469138994119));
#77928=CARTESIAN_POINT('Ctrl Pts',(0.306365181237462,1.52503135237455,9.35894651475401));
#77929=CARTESIAN_POINT('Ctrl Pts',(0.248318301789434,1.53669245213795,9.36319622064443));
#77930=CARTESIAN_POINT('Ctrl Pts',(0.189539821845199,1.5450482175854,9.36744592653485));
#77931=CARTESIAN_POINT('Ctrl Pts',(0.130426816967745,1.55002228868351,9.37169563242526));
#77932=CARTESIAN_POINT('Ctrl Pts',(0.0713711454148003,1.55499153546194,
9.37594121655317));
#77933=CARTESIAN_POINT('Ctrl Pts',(0.0119820753840637,1.55658556146196,
9.38018680068109));
#77934=CARTESIAN_POINT('Ctrl Pts',(-0.0473362918699389,1.55477957456097,
9.384432384809));
#77935=CARTESIAN_POINT('Ctrl Pts',(-0.106615111848175,1.55297479170294,
9.38867513842599));
#77936=CARTESIAN_POINT('Ctrl Pts',(-0.165822838377672,1.54777451490192,
9.39291789204299));
#77937=CARTESIAN_POINT('Ctrl Pts',(-0.224555229378385,1.539206028756,9.39716064565998));
#77938=CARTESIAN_POINT('Ctrl Pts',(-0.283283918780829,1.53063808263737,
9.4014031318782));
#77939=CARTESIAN_POINT('Ctrl Pts',(-0.341536850008862,1.51870240632424,
9.40564561809641));
#77940=CARTESIAN_POINT('Ctrl Pts',(-0.398916173355118,1.50347801335294,
9.40988810431463));
#77941=CARTESIAN_POINT('Ctrl Pts',(-0.45628943741574,1.48825522808526,9.41413014252415));
#77942=CARTESIAN_POINT('Ctrl Pts',(-0.512788809163372,1.46974454738153,
9.41837218073367));
#77943=CARTESIAN_POINT('Ctrl Pts',(-0.568030026120002,1.4480753224284,9.42261421894319));
#77944=CARTESIAN_POINT('Ctrl Pts',(-0.62331200894357,1.42639010643109,9.42685938761172));
#77945=CARTESIAN_POINT('Ctrl Pts',(-0.677333531145685,1.40154187177771,
9.43110455628025));
#77946=CARTESIAN_POINT('Ctrl Pts',(-0.729729856627479,1.37370833379813,
9.43534972494878));
#77947=CARTESIAN_POINT('Ctrl Pts',(-0.767375851189521,1.35371034329428,
9.43839981663252));
#77948=CARTESIAN_POINT('Ctrl Pts',(-0.804183296364171,1.33217229576637,
9.44144990831626));
#77949=CARTESIAN_POINT('Ctrl Pts',(-0.840025297123083,1.30917445368953,
9.44449999999999));
#77950=CARTESIAN_POINT('',(0.964986447796937,1.21999237930745,9.44449999999999));
#77951=CARTESIAN_POINT('Origin',(0.,0.,9.4445));
#77952=CARTESIAN_POINT('Ctrl Pts',(-1.55549989237731,-0.000578631300119371,
8.99405622560371));
#77953=CARTESIAN_POINT('Ctrl Pts',(-1.5554901928385,-0.0266533209394235,
8.99593481580826));
#77954=CARTESIAN_POINT('Ctrl Pts',(-1.55482490216014,-0.0527164090981486,
8.99781340601282));
#77955=CARTESIAN_POINT('Ctrl Pts',(-1.55350552651592,-0.0787453432559613,
8.99969199621737));
#77956=CARTESIAN_POINT('Ctrl Pts',(-1.55058691562536,-0.136324343623012,
9.00384765412568));
#77957=CARTESIAN_POINT('Ctrl Pts',(-1.5444568005893,-0.193860047852549,
9.00800331203398));
#77958=CARTESIAN_POINT('Ctrl Pts',(-1.53512090481116,-0.250966247953344,
9.01215896994229));
#77959=CARTESIAN_POINT('Ctrl Pts',(-1.52580175101302,-0.307970040006427,
9.01630717554572));
#77960=CARTESIAN_POINT('Ctrl Pts',(-1.51328831174432,-0.364545349116219,
9.02045538114915));
#77961=CARTESIAN_POINT('Ctrl Pts',(-1.49763817662938,-0.420309578646767,
9.02460358675258));
#77962=CARTESIAN_POINT('Ctrl Pts',(-1.48200377836541,-0.476017734963701,
9.02874762116561));
#77963=CARTESIAN_POINT('Ctrl Pts',(-1.46323907375425,-0.530915930872425,
9.03289165557864));
#77964=CARTESIAN_POINT('Ctrl Pts',(-1.44145263545854,-0.584631978025173,
9.03703568999167));
#77965=CARTESIAN_POINT('Ctrl Pts',(-1.41967980895633,-0.638314464311682,
9.04117713528298));
#77966=CARTESIAN_POINT('Ctrl Pts',(-1.39488918624381,-0.690815786388868,
9.04531858057428));
#77967=CARTESIAN_POINT('Ctrl Pts',(-1.36723840323526,-0.741781233733169,
9.04946002586559));
#77968=CARTESIAN_POINT('Ctrl Pts',(-1.33959436840948,-0.792734242943131,
9.05360046043579));
#77969=CARTESIAN_POINT('Ctrl Pts',(-1.30909180633639,-0.842151665824471,
9.057740895006));
#77970=CARTESIAN_POINT('Ctrl Pts',(-1.27593449635465,-0.889702990335659,
9.06188132957621));
#77971=CARTESIAN_POINT('Ctrl Pts',(-1.24274862502127,-0.937295275048407,
9.0660253306724));
#77972=CARTESIAN_POINT('Ctrl Pts',(-1.20690373175877,-0.983017821460801,
9.0701693317686));
#77973=CARTESIAN_POINT('Ctrl Pts',(-1.16864643086464,-1.02656990489072,
9.07431333286479));
#77974=CARTESIAN_POINT('Ctrl Pts',(-1.13037415153796,-1.07013903975733,
9.07845895641316));
#77975=CARTESIAN_POINT('Ctrl Pts',(-1.0896879441992,-1.11153564492548,9.08260457996152));
#77976=CARTESIAN_POINT('Ctrl Pts',(-1.04687198965965,-1.15049523565552,
9.08675020350989));
#77977=CARTESIAN_POINT('Ctrl Pts',(-1.00397488784166,-1.18952866485981,
9.09090368408426));
#77978=CARTESIAN_POINT('Ctrl Pts',(-0.958940375162835,-1.22611551941561,
9.09505716465863));
#77979=CARTESIAN_POINT('Ctrl Pts',(-0.912085762463041,-1.2600316709957,
9.099210645233));
#77980=CARTESIAN_POINT('Ctrl Pts',(-0.868153216420064,-1.29183265717479,
9.10310509587635));
#77981=CARTESIAN_POINT('Ctrl Pts',(-0.822621105439473,-1.32128589012233,
9.10699954651969));
#77982=CARTESIAN_POINT('Ctrl Pts',(-0.775770919578585,-1.34824320147969,
9.11089399716303));
#77983=CARTESIAN_POINT('Ctrl Pts',(-0.725804427847385,-1.3769936162386,
9.11504749265707));
#77984=CARTESIAN_POINT('Ctrl Pts',(-0.674135562699792,-1.40302129179383,
9.11920098815111));
#77985=CARTESIAN_POINT('Ctrl Pts',(-0.621092211084585,-1.42612226521083,
9.12335448364515));
#77986=CARTESIAN_POINT('Ctrl Pts',(-0.568141288735605,-1.44918298464769,
9.12750074157729));
#77987=CARTESIAN_POINT('Ctrl Pts',(-0.513821106347082,-1.46932691961064,
9.13164699950943));
#77988=CARTESIAN_POINT('Ctrl Pts',(-0.458484563219447,-1.48639569270416,
9.13579325744156));
#77989=CARTESIAN_POINT('Ctrl Pts',(-0.403201937413972,-1.50344783478884,
9.13993547545519));
#77990=CARTESIAN_POINT('Ctrl Pts',(-0.346905406819296,-1.51743060000223,
9.14407769346883));
#77991=CARTESIAN_POINT('Ctrl Pts',(-0.289966662188531,-1.52823413939725,
9.14821991148246));
#77992=CARTESIAN_POINT('Ctrl Pts',(-0.233061683793884,-1.5390312719973,
9.15235967304728));
#77993=CARTESIAN_POINT('Ctrl Pts',(-0.175515755424508,-1.54665281998605,
9.1564994346121));
#77994=CARTESIAN_POINT('Ctrl Pts',(-0.117712368437924,-1.55103966690628,
9.16063919617692));
#77995=CARTESIAN_POINT('Ctrl Pts',(-0.0599212198648014,-1.555425585022,
9.16477808125134));
#77996=CARTESIAN_POINT('Ctrl Pts',(-0.00187323828847601,-1.55657812269653,
9.16891696632577));
#77997=CARTESIAN_POINT('Ctrl Pts',(0.0560435218902042,-1.55449006868945,
9.17305585140019));
#77998=CARTESIAN_POINT('Ctrl Pts',(0.114013266983416,-1.55240010443459,
9.17719852291694));
#77999=CARTESIAN_POINT('Ctrl Pts',(0.171851030721492,-1.54706364185241,
9.18134119443368));
#78000=CARTESIAN_POINT('Ctrl Pts',(0.229170667221835,-1.53852561086421,
9.18548386595042));
#78001=CARTESIAN_POINT('Ctrl Pts',(0.286514385640701,-1.52998399276034,
9.18962827794363));
#78002=CARTESIAN_POINT('Ctrl Pts',(0.343339033121586,-1.51823822868701,
9.19377268993684));
#78003=CARTESIAN_POINT('Ctrl Pts',(0.399268682012365,-1.50338443838032,
9.19791710193004));
#78004=CARTESIAN_POINT('Ctrl Pts',(0.455307235367057,-1.48850172523749,
9.20206958379272));
#78005=CARTESIAN_POINT('Ctrl Pts',(0.510446811804607,-1.47049905229525,
9.20622206565539));
#78006=CARTESIAN_POINT('Ctrl Pts',(0.564327542277097,-1.44952222301953,
9.21037454751807));
#78007=CARTESIAN_POINT('Ctrl Pts',(0.615024959781817,-1.42978472016108,
9.21428169771494));
#78008=CARTESIAN_POINT('Ctrl Pts',(0.664607737056635,-1.40741471629783,
9.21818884791181));
#78009=CARTESIAN_POINT('Ctrl Pts',(0.712796415253884,-1.38257062040288,
9.22209599810868));
#78010=CARTESIAN_POINT('Ctrl Pts',(0.763391522821897,-1.35648586872969,
9.2261982622066));
#78011=CARTESIAN_POINT('Ctrl Pts',(0.812672697808314,-1.32755818907571,
9.23030052630453));
#78012=CARTESIAN_POINT('Ctrl Pts',(0.860295839293345,-1.29594418047019,
9.23440279040245));
#78013=CARTESIAN_POINT('Ctrl Pts',(0.908132233227251,-1.26418860697535,
9.23852342409628));
#78014=CARTESIAN_POINT('Ctrl Pts',(0.954295192671738,-1.22972276755281,
9.24264405779011));
#78015=CARTESIAN_POINT('Ctrl Pts',(0.998458660824575,-1.19275334945009,
9.24676469148394));
#78016=CARTESIAN_POINT('Ctrl Pts',(1.04230309037482,-1.15605099985406,9.25085555756054));
#78017=CARTESIAN_POINT('Ctrl Pts',(1.08417639440084,-1.11688145289402,9.25494642363714));
#78018=CARTESIAN_POINT('Ctrl Pts',(1.12378878969793,-1.07549012368745,9.25903728971374));
#78019=CARTESIAN_POINT('Ctrl Pts',(1.16337799901314,-1.03412302171083,9.26312576131896));
#78020=CARTESIAN_POINT('Ctrl Pts',(1.20070855244863,-0.990537097348186,
9.26721423292418));
#78021=CARTESIAN_POINT('Ctrl Pts',(1.23552663022966,-0.945015447489269,
9.2713027045294));
#78022=CARTESIAN_POINT('Ctrl Pts',(1.27033841526179,-0.89950202485972,9.27539043721603));
#78023=CARTESIAN_POINT('Ctrl Pts',(1.30263830177598,-0.852053994283024,
9.27947816990265));
#78024=CARTESIAN_POINT('Ctrl Pts',(1.33221350220979,-0.80298657182417,9.28356590258928));
#78025=CARTESIAN_POINT('Ctrl Pts',(1.3621982727763,-0.753239642534148,9.28771024396137));
#78026=CARTESIAN_POINT('Ctrl Pts',(1.38938199043749,-0.701828586715616,
9.29185458533345));
#78027=CARTESIAN_POINT('Ctrl Pts',(1.41359048438248,-0.649108767821922,
9.29599892670554));
#78028=CARTESIAN_POINT('Ctrl Pts',(1.43750571082689,-0.597027609455958,
9.30009306253248));
#78029=CARTESIAN_POINT('Ctrl Pts',(1.45851728171959,-0.543669757738866,
9.30418719835942));
#78030=CARTESIAN_POINT('Ctrl Pts',(1.47650651044374,-0.489396336947121,
9.30828133418636));
#78031=CARTESIAN_POINT('Ctrl Pts',(1.49482663648289,-0.434124600469282,
9.31245077833102));
#78032=CARTESIAN_POINT('Ctrl Pts',(1.51001195109945,-0.37790382886161,9.31662022247569));
#78033=CARTESIAN_POINT('Ctrl Pts',(1.52199141655154,-0.321126731904137,
9.32078966662035));
#78034=CARTESIAN_POINT('Ctrl Pts',(1.53397088200363,-0.264349634946657,
9.32495911076502));
#78035=CARTESIAN_POINT('Ctrl Pts',(1.54274449746717,-0.207016792366188,
9.32912855490969));
#78036=CARTESIAN_POINT('Ctrl Pts',(1.54829678086355,-0.149523671596055,
9.33329799905435));
#78037=CARTESIAN_POINT('Ctrl Pts',(1.5539750612308,-0.0907258697522934,
9.33756205964687));
#78038=CARTESIAN_POINT('Ctrl Pts',(1.55630942801978,-0.0315034819748185,
9.34182612023938));
#78039=CARTESIAN_POINT('Ctrl Pts',(1.55525257737604,0.0277429372124185,
9.3460901808319));
#78040=CARTESIAN_POINT('Ctrl Pts',(1.55419800600909,0.0868615814976223,
9.35034504525809));
#78041=CARTESIAN_POINT('Ctrl Pts',(1.54976676979609,0.146003672121871,9.35459990968429));
#78042=CARTESIAN_POINT('Ctrl Pts',(1.54196344786062,0.204765659869519,9.35885477411049));
#78043=CARTESIAN_POINT('Ctrl Pts',(1.5341700838921,0.263452660331324,9.36310420882358));
#78044=CARTESIAN_POINT('Ctrl Pts',(1.52301324130298,0.321760042456003,9.36735364353668));
#78045=CARTESIAN_POINT('Ctrl Pts',(1.50854939055218,0.379287471800296,9.37160307824977));
#78046=CARTESIAN_POINT('Ctrl Pts',(1.49409960192587,0.436758971510931,9.37584838155408));
#78047=CARTESIAN_POINT('Ctrl Pts',(1.47634930865275,0.493451555208341,9.3800936848584));
#78048=CARTESIAN_POINT('Ctrl Pts',(1.45540604204976,0.548974956409712,9.38433898816271));
#78049=CARTESIAN_POINT('Ctrl Pts',(1.43447678114563,0.604461226629996,9.38858145244288));
#78050=CARTESIAN_POINT('Ctrl Pts',(1.41035896085714,0.658779414523991,9.39282391672304));
#78051=CARTESIAN_POINT('Ctrl Pts',(1.38320942293468,0.711556000821227,9.39706638100321));
#78052=CARTESIAN_POINT('Ctrl Pts',(1.35606162195232,0.764329210642272,9.40130857386416));
#78053=CARTESIAN_POINT('Ctrl Pts',(1.32588269933253,0.815560577204835,9.40555076672511));
#78054=CARTESIAN_POINT('Ctrl Pts',(1.29287636066414,0.864899396482526,9.40979295958606));
#78055=CARTESIAN_POINT('Ctrl Pts',(1.2598735525539,0.914232938180896,9.41403469867633));
#78056=CARTESIAN_POINT('Ctrl Pts',(1.22404420512749,0.961673934813684,9.41827643776661));
#78057=CARTESIAN_POINT('Ctrl Pts',(1.18563523847262,1.00690085474787,9.42251817685689));
#78058=CARTESIAN_POINT('Ctrl Pts',(1.14719782176396,1.05216127488829,9.42676305786208));
#78059=CARTESIAN_POINT('Ctrl Pts',(1.10617728710028,1.09520397430549,9.43100793886727));
#78060=CARTESIAN_POINT('Ctrl Pts',(1.06285997935682,1.13574157020056,9.43525281987246));
#78061=CARTESIAN_POINT('Ctrl Pts',(1.03140539151689,1.16517768794019,9.4383352132483));
#78062=CARTESIAN_POINT('Ctrl Pts',(0.99874058480781,1.19329361845858,9.44141760662415));
#78063=CARTESIAN_POINT('Ctrl Pts',(0.964986447796939,1.21999237930745,9.44449999999999));
#78064=CARTESIAN_POINT('Origin',(0.,0.,9.5));
#78065=CARTESIAN_POINT('',(-1.84236513795726,-0.000200609048493022,9.15763482856377));
#78066=CARTESIAN_POINT('Ctrl Pts',(0.964986447796979,1.21999237930743,9.44449999999999));
#78067=CARTESIAN_POINT('Ctrl Pts',(1.08560030229,1.13318400160663,9.43775928913704));
#78068=CARTESIAN_POINT('Ctrl Pts',(1.19286327134867,1.02899315757803,9.43165929429191));
#78069=CARTESIAN_POINT('Ctrl Pts',(1.38336247774274,0.78338519890483,9.41850392344787));
#78070=CARTESIAN_POINT('Ctrl Pts',(1.46275942778644,0.640439473146718,9.41142100787987));
#78071=CARTESIAN_POINT('Ctrl Pts',(1.59405703872584,0.289070474707947,9.39396691671519));
#78072=CARTESIAN_POINT('Ctrl Pts',(1.62885716287837,0.0760950411825039,
9.38329941785984));
#78073=CARTESIAN_POINT('Ctrl Pts',(1.61182773281384,-0.347980912653401,
9.3646306987772));
#78074=CARTESIAN_POINT('Ctrl Pts',(1.56058342560136,-0.555567132615176,
9.35695125924503));
#78075=CARTESIAN_POINT('Ctrl Pts',(1.39250704246998,-0.922566442698323,
9.34073391190102));
#78076=CARTESIAN_POINT('Ctrl Pts',(1.28243138363951,-1.08322129741915,9.33237183821666));
#78077=CARTESIAN_POINT('Ctrl Pts',(1.03840088300862,-1.33466736093396,9.3163239698559));
#78078=CARTESIAN_POINT('Ctrl Pts',(0.866309261774041,-1.48184220392284,
9.3056566762329));
#78079=CARTESIAN_POINT('Ctrl Pts',(0.412140887062194,-1.67767483685419,
9.28642581763546));
#78080=CARTESIAN_POINT('Ctrl Pts',(0.194750287412152,-1.72435577821932,
9.27861688942565));
#78081=CARTESIAN_POINT('Ctrl Pts',(-0.257099384488897,-1.736029196837,9.26045970387453));
#78082=CARTESIAN_POINT('Ctrl Pts',(-0.489372106073173,-1.69608434724234,
9.25004792636098));
#78083=CARTESIAN_POINT('Ctrl Pts',(-0.884973762473043,-1.5427681115351,
9.23180320826604));
#78084=CARTESIAN_POINT('Ctrl Pts',(-1.04951278218718,-1.44452702535207,
9.22468464517327));
#78085=CARTESIAN_POINT('Ctrl Pts',(-1.37115962638764,-1.17394870584797,
9.20956351272862));
#78086=CARTESIAN_POINT('Ctrl Pts',(-1.51720372489576,-0.99309098074786,
9.20123624930322));
#78087=CARTESIAN_POINT('Ctrl Pts',(-1.69399973984075,-0.664427569501659,
9.18603024705193));
#78088=CARTESIAN_POINT('Ctrl Pts',(-1.74712287279637,-0.530140739618914,
9.17986752410044));
#78089=CARTESIAN_POINT('Ctrl Pts',(-1.81744855644709,-0.263866966136998,
9.16821855214639));
#78090=CARTESIAN_POINT('Ctrl Pts',(-1.83715573107123,-0.133049066016314,
9.16279996303978));
#78091=CARTESIAN_POINT('Ctrl Pts',(-1.84209656264027,-0.000614842640808093,
9.15790333475071));
#78092=CARTESIAN_POINT('Ctrl Pts',(1.57783641624473,1.14957158812871,9.04780057559153));
#78093=CARTESIAN_POINT('Ctrl Pts',(1.52810092067142,1.20153114569838,9.0574016669285));
#78094=CARTESIAN_POINT('Ctrl Pts',(1.4757016834809,1.25063809809762,9.06692903469903));
#78095=CARTESIAN_POINT('Ctrl Pts',(1.42089948536213,1.29662118218321,9.07641432798314));
#78096=CARTESIAN_POINT('Ctrl Pts',(1.36749733311227,1.34142952457733,9.08565729803691));
#78097=CARTESIAN_POINT('Ctrl Pts',(1.31181359643843,1.38327130064711,9.09486045306681));
#78098=CARTESIAN_POINT('Ctrl Pts',(1.25409138389606,1.42188378312268,9.10408368015105));
#78099=CARTESIAN_POINT('Ctrl Pts',(1.21543754680529,1.44774073734434,9.11026003932826));
#78100=CARTESIAN_POINT('Ctrl Pts',(1.17586965463972,1.47214936941216,9.11644603315947));
#78101=CARTESIAN_POINT('Ctrl Pts',(1.13546015350029,1.49502814066238,9.12266707759137));
#78102=CARTESIAN_POINT('Ctrl Pts',(1.10079817205115,1.51465282105421,9.12800329112069));
#78103=CARTESIAN_POINT('Ctrl Pts',(1.06551698574574,1.53315187233987,9.13336540041012));
#78104=CARTESIAN_POINT('Ctrl Pts',(1.02966136659078,1.55047227609227,9.13877276809619));
#78105=CARTESIAN_POINT('Ctrl Pts',(1.01944191431497,1.555408881392,9.14031395849557));
#78106=CARTESIAN_POINT('Ctrl Pts',(1.00917785748784,1.56024865575544,9.14185853052058));
#78107=CARTESIAN_POINT('Ctrl Pts',(0.998880077105522,1.5649861731208,9.14340550186703));
#78108=CARTESIAN_POINT('Ctrl Pts',(0.938429655183682,1.59279652767935,9.15248659188081));
#78109=CARTESIAN_POINT('Ctrl Pts',(0.876724909237559,1.61713151747312,9.16166360683785));
#78110=CARTESIAN_POINT('Ctrl Pts',(0.813962174626755,1.63784581666518,9.17104583411974));
#78111=CARTESIAN_POINT('Ctrl Pts',(0.793731103129688,1.64452290730766,9.17407012093769));
#78112=CARTESIAN_POINT('Ctrl Pts',(0.773389798665458,1.65082359212481,9.17711583460595));
#78113=CARTESIAN_POINT('Ctrl Pts',(0.752943954195354,1.656742326203,9.18018689597204));
#78114=CARTESIAN_POINT('Ctrl Pts',(0.685138060299321,1.67637101189959,9.19037165803664));
#78115=CARTESIAN_POINT('Ctrl Pts',(0.616177319257057,1.69180559672274,9.20083482083306));
#78116=CARTESIAN_POINT('Ctrl Pts',(0.546368309836355,1.70301140123728,9.21149051924861));
#78117=CARTESIAN_POINT('Ctrl Pts',(0.485285426593238,1.71281648018751,9.22081425536221));
#78118=CARTESIAN_POINT('Ctrl Pts',(0.423553097709839,1.71938155637349,9.23028512190475));
#78119=CARTESIAN_POINT('Ctrl Pts',(0.361421529909612,1.72264105607437,9.23985292365802));
#78120=CARTESIAN_POINT('Ctrl Pts',(0.34963016087468,1.72325964603118,9.24166870724952));
#78121=CARTESIAN_POINT('Ctrl Pts',(0.337823543788487,1.72375903562151,9.24348816903752));
#78122=CARTESIAN_POINT('Ctrl Pts',(0.326020291990775,1.72413841101507,9.24530843418927));
#78123=CARTESIAN_POINT('Ctrl Pts',(0.260499809734028,1.72624434412302,9.25541282343905));
#78124=CARTESIAN_POINT('Ctrl Pts',(0.19495931580534,1.72466195618245,9.26555860148615));
#78125=CARTESIAN_POINT('Ctrl Pts',(0.129717803358982,1.71940174492272,9.27571201101684));
#78126=CARTESIAN_POINT('Ctrl Pts',(0.0648998775900165,1.71417568608109,
9.28579949857782));
#78127=CARTESIAN_POINT('Ctrl Pts',(0.000376941694672228,1.7053181900444,
9.29589425669667));
#78128=CARTESIAN_POINT('Ctrl Pts',(-0.0634948351275549,1.69282106251119,
9.30598856445142));
#78129=CARTESIAN_POINT('Ctrl Pts',(-0.126013627091431,1.68058865948019,
9.31586904622187));
#78130=CARTESIAN_POINT('Ctrl Pts',(-0.187908231055998,1.66486839910538,
9.32574896303347));
#78131=CARTESIAN_POINT('Ctrl Pts',(-0.24880479275547,1.64564964474991,9.3356483009401));
#78132=CARTESIAN_POINT('Ctrl Pts',(-0.265085021026627,1.64051165831418,
9.33829481293282));
#78133=CARTESIAN_POINT('Ctrl Pts',(-0.281293709851209,1.63512364377799,
9.34094287203815));
#78134=CARTESIAN_POINT('Ctrl Pts',(-0.297423275648299,1.62948545004139,
9.34359321518114));
#78135=CARTESIAN_POINT('Ctrl Pts',(-0.30743974502818,1.625984128578,9.34523907975505));
#78136=CARTESIAN_POINT('Ctrl Pts',(-0.317424735746893,1.62238658086478,
9.34688567512058));
#78137=CARTESIAN_POINT('Ctrl Pts',(-0.327364914290974,1.61869735262368,
9.34853128806519));
#78138=CARTESIAN_POINT('Ctrl Pts',(-0.385432578540992,1.59714594226462,
9.35814448560777));
#78139=CARTESIAN_POINT('Ctrl Pts',(-0.442079483362686,1.57243010146291,
9.36773988234226));
#78140=CARTESIAN_POINT('Ctrl Pts',(-0.497012128252419,1.54462866539572,
9.37737904315513));
#78141=CARTESIAN_POINT('Ctrl Pts',(-0.551000823362909,1.51730496273262,
9.38685256687298));
#78142=CARTESIAN_POINT('Ctrl Pts',(-0.603333782033549,1.48700109740394,
9.39636859881508));
#78143=CARTESIAN_POINT('Ctrl Pts',(-0.653723422148521,1.45377417399759,
9.40600700702671));
#78144=CARTESIAN_POINT('Ctrl Pts',(-0.699035964422128,1.4238950883753,9.41467428027064));
#78145=CARTESIAN_POINT('Ctrl Pts',(-0.742776628534788,1.39165290498635,
9.42344082135282));
#78146=CARTESIAN_POINT('Ctrl Pts',(-0.784729150829576,1.3570706466195,9.43237741146729));
#78147=CARTESIAN_POINT('Ctrl Pts',(-0.788069690410533,1.35431697660029,
9.43308900236489));
#78148=CARTESIAN_POINT('Ctrl Pts',(-0.791398865710535,1.35154847642802,
9.43380167144245));
#78149=CARTESIAN_POINT('Ctrl Pts',(-0.7947165535573,1.34876516188143,9.43451545443494));
#78150=CARTESIAN_POINT('Ctrl Pts',(-0.810068690312162,1.33588576287689,
9.43781838545804));
#78151=CARTESIAN_POINT('Ctrl Pts',(-0.825175397375869,1.32268873629791,
9.44114528312219));
#78152=CARTESIAN_POINT('Ctrl Pts',(-0.840025297123097,1.30917445368955,
9.44449999999998));
#78153=CARTESIAN_POINT('Ctrl Pts',(-1.84249520620809,-1.04387282595019E-15,
9.15750479379191));
#78154=CARTESIAN_POINT('Ctrl Pts',(-1.84342557490868,0.0255843048651023,
9.15657442509132));
#78155=CARTESIAN_POINT('Ctrl Pts',(-1.84380342678949,0.0512172914604668,
9.15566374529628));
#78156=CARTESIAN_POINT('Ctrl Pts',(-1.8436302880131,0.0768851883582362,
9.15476723119598));
#78157=CARTESIAN_POINT('Ctrl Pts',(-1.84315348435067,0.147571533166139,
9.15229833765667));
#78158=CARTESIAN_POINT('Ctrl Pts',(-1.8385033733487,0.218128048887438,9.1499488369688));
#78159=CARTESIAN_POINT('Ctrl Pts',(-1.829823624367,0.288237312311215,9.14761363519918));
#78160=CARTESIAN_POINT('Ctrl Pts',(-1.82117196456348,0.358119689958019,
9.14528599054886));
#78161=CARTESIAN_POINT('Ctrl Pts',(-1.80851533144921,0.427557438695703,
9.14297219045531));
#78162=CARTESIAN_POINT('Ctrl Pts',(-1.79197172346283,0.49620682453524,9.14059582919536));
#78163=CARTESIAN_POINT('Ctrl Pts',(-1.77951701963477,0.547888886230224,
9.13880680737464));
#78164=CARTESIAN_POINT('Ctrl Pts',(-1.76485880483925,0.5991234665025,9.1369828833152));
#78165=CARTESIAN_POINT('Ctrl Pts',(-1.74804397062882,0.649754936470355,
9.1351034343108));
#78166=CARTESIAN_POINT('Ctrl Pts',(-1.73847181500994,0.678577837944145,
9.13403352317622));
#78167=CARTESIAN_POINT('Ctrl Pts',(-1.72820074137517,0.707205162873137,
9.13294581355773));
#78168=CARTESIAN_POINT('Ctrl Pts',(-1.71723927293521,0.735607328247734,
9.1318381060832));
#78169=CARTESIAN_POINT('Ctrl Pts',(-1.71240747914154,0.748126947050236,
9.13134983080056));
#78170=CARTESIAN_POINT('Ctrl Pts',(-1.70744153904584,0.760602809394986,
9.13085768542315));
#78171=CARTESIAN_POINT('Ctrl Pts',(-1.70234218031443,0.773032349297603,
9.1303615558247));
#78172=CARTESIAN_POINT('Ctrl Pts',(-1.69796348408131,0.783705295136006,
9.12993554131614));
#78173=CARTESIAN_POINT('Ctrl Pts',(-1.69348687217055,0.794342776028454,
9.12950663900286));
#78174=CARTESIAN_POINT('Ctrl Pts',(-1.6889179804492,0.804931912536332,9.12907527449553));
#78175=CARTESIAN_POINT('Ctrl Pts',(-1.66040388987596,0.871017872960098,
9.1263831628452));
#78176=CARTESIAN_POINT('Ctrl Pts',(-1.62824798634224,0.935339672795842,
9.12358735490002));
#78177=CARTESIAN_POINT('Ctrl Pts',(-1.59268341757425,0.99755604372753,9.12070265019255));
#78178=CARTESIAN_POINT('Ctrl Pts',(-1.55704284135595,1.05990538148225,9.11781178038713));
#78179=CARTESIAN_POINT('Ctrl Pts',(-1.51797988143916,1.12014042703985,9.11483190560086));
#78180=CARTESIAN_POINT('Ctrl Pts',(-1.47570599844027,1.17793996136523,9.11181284126448));
#78181=CARTESIAN_POINT('Ctrl Pts',(-1.43416890647619,1.23473210825217,9.10884639616671));
#78182=CARTESIAN_POINT('Ctrl Pts',(-1.38953274198914,1.2891736439028,9.10584254470439));
#78183=CARTESIAN_POINT('Ctrl Pts',(-1.34196257272456,1.34097455280792,9.10287683639888));
#78184=CARTESIAN_POINT('Ctrl Pts',(-1.32667583540764,1.35762084394903,9.10192380208083));
#78185=CARTESIAN_POINT('Ctrl Pts',(-1.3110857787495,1.3739945103908,9.10097490118564));
#78186=CARTESIAN_POINT('Ctrl Pts',(-1.29519684402696,1.39008601519461,9.1000331596533));
#78187=CARTESIAN_POINT('Ctrl Pts',(-1.28692690184776,1.39846139193493,9.09954299790513));
#78188=CARTESIAN_POINT('Ctrl Pts',(-1.27858264381706,1.4067535669247,9.09905517532569));
#78189=CARTESIAN_POINT('Ctrl Pts',(-1.2701663787571,1.41496029262394,9.09857020654789));
#78190=CARTESIAN_POINT('Ctrl Pts',(-1.22072939905454,1.46316644213651,9.09572150923928));
#78191=CARTESIAN_POINT('Ctrl Pts',(-1.16879887319286,1.50843891952808,9.09296975259348));
#78192=CARTESIAN_POINT('Ctrl Pts',(-1.11453995621698,1.550592707069,9.09040919115646));
#78193=CARTESIAN_POINT('Ctrl Pts',(-1.06201853480217,1.5913966331896,9.08793062479745));
#78194=CARTESIAN_POINT('Ctrl Pts',(-1.0073091984942,1.62928311296455,9.0856308892326));
#78195=CARTESIAN_POINT('Ctrl Pts',(-0.950637932866433,1.66420382554962,
9.08341792443461));
#78196=CARTESIAN_POINT('Ctrl Pts',(-0.947477902479955,1.66615102951029,
9.08329452793149));
#78197=CARTESIAN_POINT('Ctrl Pts',(-0.944311758662973,1.66808901067078,
9.08317140122102));
#78198=CARTESIAN_POINT('Ctrl Pts',(-0.941139535971432,1.67001775994204,
9.08304852834237));
#78199=CARTESIAN_POINT('Ctrl Pts',(-0.879859752551074,1.70727659991257,
9.0806749171163));
#78200=CARTESIAN_POINT('Ctrl Pts',(-0.816315831409928,1.74108997628849,
9.07839543674175));
#78201=CARTESIAN_POINT('Ctrl Pts',(-0.750802631996302,1.77133860261608,
9.07611199979561));
#78202=CARTESIAN_POINT('Ctrl Pts',(-0.735354339772224,1.77847135789392,
9.0755735556113));
#78203=CARTESIAN_POINT('Ctrl Pts',(-0.719796650695635,1.78540568824835,
9.07503498604674));
#78204=CARTESIAN_POINT('Ctrl Pts',(-0.704133638622343,1.79213966692767,
9.07449519169253));
#78205=CARTESIAN_POINT('Ctrl Pts',(-0.689232335423251,1.79854616508826,
9.07398164810976));
#78206=CARTESIAN_POINT('Ctrl Pts',(-0.674231156838674,1.80477300329879,
9.07346684130825));
#78207=CARTESIAN_POINT('Ctrl Pts',(-0.659161822527577,1.81080758331309,
9.07295085375021));
#78208=CARTESIAN_POINT('Ctrl Pts',(-0.59180873473216,1.83777941824091,9.07064462345622));
#78209=CARTESIAN_POINT('Ctrl Pts',(-0.522999968241605,1.86095469047836,
9.06830887730024));
#78210=CARTESIAN_POINT('Ctrl Pts',(-0.453122176480387,1.88028588298503,
9.06588658332271));
#78211=CARTESIAN_POINT('Ctrl Pts',(-0.382259594422812,1.89988951070062,
9.06343015186683));
#78212=CARTESIAN_POINT('Ctrl Pts',(-0.3102979315688,1.91553942838373,9.06088454492288));
#78213=CARTESIAN_POINT('Ctrl Pts',(-0.237641237294552,1.92717683998401,
9.05822660172882));
#78214=CARTESIAN_POINT('Ctrl Pts',(-0.165233254770242,1.93877441546137,
9.05557775696277));
#78215=CARTESIAN_POINT('Ctrl Pts',(-0.0921354293764491,1.94638696167918,
9.05281738641335));
#78216=CARTESIAN_POINT('Ctrl Pts',(-0.0187427861903081,1.94995074918594,
9.04995917573888));
#78217=CARTESIAN_POINT('Ctrl Pts',(0.00621919604093061,1.95116284888092,
9.0489870537254));
#78218=CARTESIAN_POINT('Ctrl Pts',(0.031215354135369,1.95190653702187,9.04800392274799));
#78219=CARTESIAN_POINT('Ctrl Pts',(0.0562304113113475,1.95217907313218,
9.0470112666143));
#78220=CARTESIAN_POINT('',(-1.,-1.22464679914735E-16,10.));
#78221=CARTESIAN_POINT('',(-1.5,1.83697019872103E-16,9.5));
#78222=CARTESIAN_POINT('Origin',(0.,0.,10.));
#78223=CARTESIAN_POINT('Ctrl Pts',(1.13606309729039,-1.59291788311565,-0.231572901724461));
#78224=CARTESIAN_POINT('Ctrl Pts',(1.66580374373072,-1.21512888180952,-0.194523781698427));
#78225=CARTESIAN_POINT('Ctrl Pts',(2.30944801597464,0.103719845647892,-0.120437406770433));
#78226=CARTESIAN_POINT('Ctrl Pts',(1.16339425275335,2.00013089295272,-0.00931377694047787));
#78227=CARTESIAN_POINT('Ctrl Pts',(-1.04791896608993,2.06049732145338,0.101797987765405));
#78228=CARTESIAN_POINT('Ctrl Pts',(-2.29996171030973,0.238632901556859,
0.212909752471286));
#78229=CARTESIAN_POINT('Ctrl Pts',(-1.44799824011824,-1.80309610357979,
0.324021517177169));
#78230=CARTESIAN_POINT('Ctrl Pts',(0.728904987242802,-2.1943368700259,0.435133281883051));
#78231=CARTESIAN_POINT('Ctrl Pts',(2.23884632299531,-0.578363011946529,
0.546245046588933));
#78232=CARTESIAN_POINT('Ctrl Pts',(1.70046726949765,1.56698688412613,0.657356811294816));
#78233=CARTESIAN_POINT('Ctrl Pts',(-0.393719188013592,2.27855690477491,
0.768468576000697));
#78234=CARTESIAN_POINT('Ctrl Pts',(-2.12767440764199,0.905496867856805,
0.879580340706581));
#78235=CARTESIAN_POINT('Ctrl Pts',(-1.91498907715104,-1.29605005156759,
0.990692105412462));
#78236=CARTESIAN_POINT('Ctrl Pts',(0.0497559032715141,-2.31180145897258,
1.10180387011835));
#78237=CARTESIAN_POINT('Ctrl Pts',(1.9689767915461,-1.21245450603212,1.21291563482423));
#78238=CARTESIAN_POINT('Ctrl Pts',(2.08674750979809,0.996192734636249,1.32402739953011));
#78239=CARTESIAN_POINT('Ctrl Pts',(0.295316342405819,2.29340353780112,1.435139164236));
#78240=CARTESIAN_POINT('Ctrl Pts',(-1.76630463899123,1.49234098525026,1.54625092894187));
#78241=CARTESIAN_POINT('Ctrl Pts',(-2.21190301684171,-0.67409086830421,
1.65736269364776));
#78242=CARTESIAN_POINT('Ctrl Pts',(-0.633792933399775,-2.22378495174526,
1.76847445835364));
#78243=CARTESIAN_POINT('Ctrl Pts',(1.52418525493671,-1.73889983355718,1.87958622305952));
#78244=CARTESIAN_POINT('Ctrl Pts',(2.28765995870177,0.336934972534499,1.9906979877654));
#78245=CARTESIAN_POINT('Ctrl Pts',(0.958114915389017,2.10450208243153,2.10180975247129));
#78246=CARTESIAN_POINT('Ctrl Pts',(-1.24802606205186,1.9466237960034,2.21292151717718));
#78247=CARTESIAN_POINT('Ctrl Pts',(-2.31232637129592,0.00774565228208377,
2.32403328188306));
#78248=CARTESIAN_POINT('Ctrl Pts',(-1.26103921283396,-1.93821911551469,
2.43514504658893));
#78249=CARTESIAN_POINT('Ctrl Pts',(0.943994572770135,-2.11087363186064,
2.54625681129481));
#78250=CARTESIAN_POINT('Ctrl Pts',(2.28535136603151,-0.352253281953543,
2.65736857600071));
#78251=CARTESIAN_POINT('Ctrl Pts',(1.53580059245491,1.72864969858349,2.76848034070657));
#78252=CARTESIAN_POINT('Ctrl Pts',(-0.618880756285069,2.22798111542639,
2.87959210541247));
#78253=CARTESIAN_POINT('Ctrl Pts',(-2.20733737683441,0.68889400174652,2.99070387011834));
#78254=CARTESIAN_POINT('Ctrl Pts',(-1.7762627812942,-1.48047417152237,3.10181563482422));
#78255=CARTESIAN_POINT('Ctrl Pts',(0.279945412928593,-2.29533087084941,
3.21292739953011));
#78256=CARTESIAN_POINT('Ctrl Pts',(2.08002669781736,-1.01014958159571,3.32403916423598));
#78257=CARTESIAN_POINT('Ctrl Pts',(1.97705551298443,1.19923506428337,3.43515092894188));
#78258=CARTESIAN_POINT('Ctrl Pts',(0.0652419797826839,2.31141876883474,
3.54626269364775));
#78259=CARTESIAN_POINT('Ctrl Pts',(-1.90626257127342,1.30884538819506,3.65737445835364));
#78260=CARTESIAN_POINT('Ctrl Pts',(-2.1336944630698,-0.891213318517691,
3.76848622305952));
#78261=CARTESIAN_POINT('Ctrl Pts',(-0.408972316733737,-2.27588551666947,
3.8795979877654));
#78262=CARTESIAN_POINT('Ctrl Pts',(1.68992568908689,-1.57831061778191,3.99070975247128));
#78263=CARTESIAN_POINT('Ctrl Pts',(2.24268139796916,0.563288015177147,4.10182151717717));
#78264=CARTESIAN_POINT('Ctrl Pts',(0.743569033391774,2.18952468207605,4.21293328188306));
#78265=CARTESIAN_POINT('Ctrl Pts',(-1.43584752482253,1.81252727601552,4.32404504658893));
#78266=CARTESIAN_POINT('Ctrl Pts',(-2.30158230139483,-0.222782743374198,
4.43515681129481));
#78267=CARTESIAN_POINT('Ctrl Pts',(-1.06155954729496,-2.05426497034491,
4.54626857600071));
#78268=CARTESIAN_POINT('Ctrl Pts',(1.14970243193213,-2.00626457847626,4.65738034070657));
#78269=CARTESIAN_POINT('Ctrl Pts',(2.30908173348749,-0.122697958066977,
4.76849210541246));
#78270=CARTESIAN_POINT('Ctrl Pts',(1.35584214399455,1.87312715035776,4.87960387011834));
#78271=CARTESIAN_POINT('Ctrl Pts',(-0.837880917841919,2.15519577030842,
4.99071563482423));
#78272=CARTESIAN_POINT('Ctrl Pts',(-2.2650122086686,0.465438433546961,5.1018273995301));
#78273=CARTESIAN_POINT('Ctrl Pts',(-1.61984458036479,-1.65015659144846,
5.21293916423598));
#78274=CARTESIAN_POINT('Ctrl Pts',(0.507346924100459,-2.25599475607619,
5.32405092894189));
#78275=CARTESIAN_POINT('Ctrl Pts',(2.17035793611363,-0.79778422521133,5.43516269364775));
#78276=CARTESIAN_POINT('Ctrl Pts',(1.8476708631746,1.39033291775907,5.54627445835364));
#78277=CARTESIAN_POINT('Ctrl Pts',(-0.165482299961806,2.30641038179036,
5.6573862230595));
#78278=CARTESIAN_POINT('Ctrl Pts',(-2.02723283931421,1.11231302073658,5.76849798776541));
#78279=CARTESIAN_POINT('Ctrl Pts',(-2.03423292489276,-1.09945879779015,
5.87960975247127));
#78280=CARTESIAN_POINT('Ctrl Pts',(-0.180078057223998,-2.30531671015481,
5.99072151717718));
#78281=CARTESIAN_POINT('Ctrl Pts',(1.83883334564853,-1.40200041659325,6.10183328188304));
#78282=CARTESIAN_POINT('Ctrl Pts',(2.17536425594361,0.784030352831153,6.21294504658893));
#78283=CARTESIAN_POINT('Ctrl Pts',(0.521616713088515,2.25273816620926,6.32405681129482));
#78284=CARTESIAN_POINT('Ctrl Pts',(-1.60936700050969,1.66037679481931,6.43516857600069));
#78285=CARTESIAN_POINT('Ctrl Pts',(-2.2679129552827,-0.451092078529837,
6.54628034070658));
#78286=CARTESIAN_POINT('Ctrl Pts',(-0.851506051454237,-2.14984899164026,
6.65739210541246));
#78287=CARTESIAN_POINT('Ctrl Pts',(1.34395850160194,-1.88167181004001,6.76850387011834));
#78288=CARTESIAN_POINT('Ctrl Pts',(2.30981211862901,0.108079520188228,6.87961563482422));
#78289=CARTESIAN_POINT('Ctrl Pts',(1.16237862931446,1.99894701892701,6.9907273995301));
#78290=CARTESIAN_POINT('Ctrl Pts',(-1.048535261215,2.06094326183436,7.10183916423599));
#78291=CARTESIAN_POINT('Ctrl Pts',(-2.30012597472422,0.237346780966457,
7.21295092894187));
#78292=CARTESIAN_POINT('Ctrl Pts',(-1.4472917606237,-1.80340234398078,7.32406269364775));
#78293=CARTESIAN_POINT('Ctrl Pts',(0.729695116197456,-2.19418748774512,
7.43517445835364));
#78294=CARTESIAN_POINT('Ctrl Pts',(2.23907061743849,-0.577472336492666,
7.54628622305951));
#78295=CARTESIAN_POINT('Ctrl Pts',(1.6998828851918,1.56758199492804,7.6573979877654));
#78296=CARTESIAN_POINT('Ctrl Pts',(-0.394559581775687,2.27842890415167,
7.76850975247128));
#78297=CARTESIAN_POINT('Ctrl Pts',(-2.12800802962129,0.904700757977686,
7.87962151717716));
#78298=CARTESIAN_POINT('Ctrl Pts',(-1.91451385442197,-1.29675194351212,
7.99073328188305));
#78299=CARTESIAN_POINT('Ctrl Pts',(0.0506189763134289,-2.31178733491431,
8.10184504658893));
#78300=CARTESIAN_POINT('Ctrl Pts',(1.96940772470891,-1.21172174246582,8.21295681129481));
#78301=CARTESIAN_POINT('Ctrl Pts',(2.08641197020285,0.996956328156063,8.3240685760007));
#78302=CARTESIAN_POINT('Ctrl Pts',(0.294406065655051,2.29352604085566,8.43518034070657));
#78303=CARTESIAN_POINT('Ctrl Pts',(-1.76673675864417,1.49166283229086,8.54629210541247));
#78304=CARTESIAN_POINT('Ctrl Pts',(-2.21188103147225,-0.674860552072349,
8.65740387011833));
#78305=CARTESIAN_POINT('Ctrl Pts',(-0.632537782229339,-2.22411004328669,
8.76851563482423));
#78306=CARTESIAN_POINT('Ctrl Pts',(1.52400006892491,-1.73816200658177,8.8796273995301));
#78307=CARTESIAN_POINT('Ctrl Pts',(2.28913633277906,0.33743832952732,8.99073916423599));
#78308=CARTESIAN_POINT('Ctrl Pts',(0.953931268377545,2.1057836989737,9.10186283730748));
#78309=CARTESIAN_POINT('Ctrl Pts',(-0.50962975476275,1.9979286932635,9.17594925547701));
#78310=CARTESIAN_POINT('Ctrl Pts',(-1.05712610504189,1.64636300407581,9.21299841874458));
#78311=CARTESIAN_POINT('Ctrl Pts',(1.05790529558725,-1.4833298150454,-0.153859353408328));
#78312=CARTESIAN_POINT('Ctrl Pts',(1.55120134269385,-1.13153158654066,-0.116810233382295));
#78313=CARTESIAN_POINT('Ctrl Pts',(2.15056478096174,0.0965842251456926,
-0.0427238584543007));
#78314=CARTESIAN_POINT('Ctrl Pts',(1.08335614789265,1.8625277667843,0.068399771375655));
#78315=CARTESIAN_POINT('Ctrl Pts',(-0.975825221518905,1.91874116244765,
0.179511536081537));
#78316=CARTESIAN_POINT('Ctrl Pts',(-2.14173110524213,0.222215659377068,
0.29062330078742));
#78317=CARTESIAN_POINT('Ctrl Pts',(-1.34838021750347,-1.6790483917481,0.401735065493302));
#78318=CARTESIAN_POINT('Ctrl Pts',(0.678758466693704,-2.04337294349185,
0.512846830199185));
#78319=CARTESIAN_POINT('Ctrl Pts',(2.08482027692988,-0.538573336788539,
0.623958594905066));
#78320=CARTESIAN_POINT('Ctrl Pts',(1.58348011977939,1.45918279256373,0.73507035961095));
#78321=CARTESIAN_POINT('Ctrl Pts',(-0.366632465192586,2.12179888740995,
0.84618212431683));
#78322=CARTESIAN_POINT('Ctrl Pts',(-1.98129666256959,0.843201345002855,
0.957293889022715));
#78323=CARTESIAN_POINT('Ctrl Pts',(-1.78324345764042,-1.20688561768239,
1.06840565372859));
#78324=CARTESIAN_POINT('Ctrl Pts',(0.0463328433809853,-2.15275631399923,
1.17951741843448));
#78325=CARTESIAN_POINT('Ctrl Pts',(1.83351697597882,-1.12904119995556,1.29062918314035));
#78326=CARTESIAN_POINT('Ctrl Pts',(1.94318541499513,0.927657602743041,1.40174094784624));
#78327=CARTESIAN_POINT('Ctrl Pts',(0.274999446113248,2.13562411572477,1.51285271255212));
#78328=CARTESIAN_POINT('Ctrl Pts',(-1.6447880717769,1.38967231211328,1.62396447725801));
#78329=CARTESIAN_POINT('Ctrl Pts',(-2.05973059104138,-0.627715398015217,
1.73507624196389));
#78330=CARTESIAN_POINT('Ctrl Pts',(-0.590189842578783,-2.07079508374983,
1.84618800666977));
#78331=CARTESIAN_POINT('Ctrl Pts',(1.41932578964969,-1.61926863640188,1.95729977137565));
#78332=CARTESIAN_POINT('Ctrl Pts',(2.13027567798452,0.313754836824603,2.06841153608153));
#78333=CARTESIAN_POINT('Ctrl Pts',(0.892199425532491,1.95971852521992,2.17952330078742));
#78334=CARTESIAN_POINT('Ctrl Pts',(-1.16216553748166,1.81270180082412,2.2906350654933));
#78335=CARTESIAN_POINT('Ctrl Pts',(-2.15324511389767,0.00721277417295179,
2.40174683019918));
#78336=CARTESIAN_POINT('Ctrl Pts',(-1.17428342174132,-1.804875337648,2.51285859490507));
#78337=CARTESIAN_POINT('Ctrl Pts',(0.879050520979899,-1.96565173077709,
2.62397035961094));
#78338=CARTESIAN_POINT('Ctrl Pts',(2.12812590970401,-0.328019291582862,
2.73508212431683));
#78339=CARTESIAN_POINT('Ctrl Pts',(1.43014202608922,1.60972368058472,2.84619388902271));
#78340=CARTESIAN_POINT('Ctrl Pts',(-0.576303579416129,2.07470256370406,
2.95730565372859));
#78341=CARTESIAN_POINT('Ctrl Pts',(-2.05547905364616,0.641500119389611,
3.06841741843448));
#78342=CARTESIAN_POINT('Ctrl Pts',(-1.65406112316078,-1.37862190028811,
3.17952918314036));
#78343=CARTESIAN_POINT('Ctrl Pts',(0.260685991402141,-2.13741885392462,
3.29064094784625));
#78344=CARTESIAN_POINT('Ctrl Pts',(1.93692697512326,-0.940654259656997,
3.40175271255211));
#78345=CARTESIAN_POINT('Ctrl Pts',(1.8410399051291,1.11673121694138,3.51286447725801));
#78346=CARTESIAN_POINT('Ctrl Pts',(0.060753523348571,2.15239995181797,3.62397624196388));
#78347=CARTESIAN_POINT('Ctrl Pts',(-1.77511730971615,1.218800672761,3.73508800666977));
#78348=CARTESIAN_POINT('Ctrl Pts',(-1.98690255587955,-0.829900461872639,
3.84619977137565));
#78349=CARTESIAN_POINT('Ctrl Pts',(-0.380836223492431,-2.11931128295378,
3.95731153608153));
#78350=CARTESIAN_POINT('Ctrl Pts',(1.57366376911455,-1.46972748662942,4.06842330078742));
#78351=CARTESIAN_POINT('Ctrl Pts',(2.0883915100185,0.524535455484849,4.1795350654933));
#78352=CARTESIAN_POINT('Ctrl Pts',(0.692413669571699,2.03889181992781,4.29064683019919));
#78353=CARTESIAN_POINT('Ctrl Pts',(-1.33706543570381,1.68783072724259,4.40175859490506));
#78354=CARTESIAN_POINT('Ctrl Pts',(-2.14324020442421,-0.207455945486791,
4.51287035961095));
#78355=CARTESIAN_POINT('Ctrl Pts',(-0.988527370832692,-1.91293757877584,
4.62398212431683));
#78356=CARTESIAN_POINT('Ctrl Pts',(1.07060628409766,-1.86823947277342,4.73509388902271));
#78357=CARTESIAN_POINT('Ctrl Pts',(2.15022369763304,-0.114256699215363,
4.84620565372859));
#78358=CARTESIAN_POINT('Ctrl Pts',(1.26256418990569,1.74426150835986,4.95731741843447));
#78359=CARTESIAN_POINT('Ctrl Pts',(-0.780237173595914,2.00692463638197,
5.06842918314036));
#78360=CARTESIAN_POINT('Ctrl Pts',(-2.10918602658192,0.433417637447724,
5.17954094784624));
#78361=CARTESIAN_POINT('Ctrl Pts',(-1.50840403467324,-1.53663066849473,
5.29065271255212));
#78362=CARTESIAN_POINT('Ctrl Pts',(0.472442947038698,-2.10078894822159,
5.40176447725801));
#78363=CARTESIAN_POINT('Ctrl Pts',(2.02104368974809,-0.74289901555643,5.51287624196389));
#78364=CARTESIAN_POINT('Ctrl Pts',(1.72055653890764,1.29468209981882,5.62398800666977));
#78365=CARTESIAN_POINT('Ctrl Pts',(-0.154097604149901,2.14773612708039,
5.73509977137565));
#78366=CARTESIAN_POINT('Ctrl Pts',(-1.88776517890069,1.03578915448837,5.84621153608153));
#78367=CARTESIAN_POINT('Ctrl Pts',(-1.89428367916776,-1.02381926429645,
5.95732330078742));
#78368=CARTESIAN_POINT('Ctrl Pts',(-0.167689216215796,-2.14671769683858,
6.06843506549329));
#78369=CARTESIAN_POINT('Ctrl Pts',(1.71232701661002,-1.30554690902911,6.17954683019919));
#78370=CARTESIAN_POINT('Ctrl Pts',(2.02570558948953,0.730091369167335,6.29065859490506));
#78371=CARTESIAN_POINT('Ctrl Pts',(0.485731016489559,2.09775640216495,6.40177035961095));
#78372=CARTESIAN_POINT('Ctrl Pts',(-1.49864728151395,1.54614775191534,6.51288212431683));
#78373=CARTESIAN_POINT('Ctrl Pts',(-2.11188721035553,-0.420058269485543,
6.62399388902271));
#78374=CARTESIAN_POINT('Ctrl Pts',(-0.792924938065964,-2.00194570036965,
6.73510565372859));
#78375=CARTESIAN_POINT('Ctrl Pts',(1.25149810717844,-1.75221832057249,6.84621741843447));
#78376=CARTESIAN_POINT('Ctrl Pts',(2.15090383442374,0.100643966892662,6.95732918314036));
#78377=CARTESIAN_POINT('Ctrl Pts',(1.08241039636101,1.86142533981164,7.06844094784623));
#78378=CARTESIAN_POINT('Ctrl Pts',(-0.976399117350945,1.91915642344125,
7.17955271255213));
#78379=CARTESIAN_POINT('Ctrl Pts',(-2.14188406874776,0.221018020102809,
7.290664477258));
#78380=CARTESIAN_POINT('Ctrl Pts',(-1.34772234172149,-1.67933356370967,
7.40177624196389));
#78381=CARTESIAN_POINT('Ctrl Pts',(0.679494237098812,-2.04323383827288,
7.51288800666976));
#78382=CARTESIAN_POINT('Ctrl Pts',(2.08502914057466,-0.537743937187812,
7.62399977137566));
#78383=CARTESIAN_POINT('Ctrl Pts',(1.58293593939601,1.45973696149177,7.73511153608152));
#78384=CARTESIAN_POINT('Ctrl Pts',(-0.367415042334137,2.12167969285334,
7.84622330078743));
#78385=CARTESIAN_POINT('Ctrl Pts',(-1.98160733233737,0.842460005143296,
7.95733506549329));
#78386=CARTESIAN_POINT('Ctrl Pts',(-1.78280092883823,-1.2075392215243,8.0684468301992));
#78387=CARTESIAN_POINT('Ctrl Pts',(0.0471365395345726,-2.15274316163464,
8.17955859490505));
#78388=CARTESIAN_POINT('Ctrl Pts',(1.83391826220672,-1.12835884836871,8.29067035961095));
#78389=CARTESIAN_POINT('Ctrl Pts',(1.94287295953775,0.928368663273228,8.40178212431683));
#78390=CARTESIAN_POINT('Ctrl Pts',(0.274151793727225,2.13573819092923,8.51289388902271));
#78391=CARTESIAN_POINT('Ctrl Pts',(-1.6451904628679,1.38904081408411,8.6240056537286));
#78392=CARTESIAN_POINT('Ctrl Pts',(-2.05971011820072,-0.628432129802549,
8.73511741843447));
#78393=CARTESIAN_POINT('Ctrl Pts',(-0.58902104211943,-2.07109780994878,
8.84622918314036));
#78394=CARTESIAN_POINT('Ctrl Pts',(1.41915334389115,-1.61858156975358,8.95734094784623));
#78395=CARTESIAN_POINT('Ctrl Pts',(2.13165048186501,0.314223564335907,9.06845271255213));
#78396=CARTESIAN_POINT('Ctrl Pts',(0.888303601137828,1.96091197031123,9.17957638562361));
#78397=CARTESIAN_POINT('Ctrl Pts',(-0.474568725661671,1.86047707196044,
9.25366280379315));
#78398=CARTESIAN_POINT('Ctrl Pts',(-0.984398936374817,1.53309806878228,
9.29071196706072));
#78399=CARTESIAN_POINT('Ctrl Pts',(0.97974749388411,-1.37374174697515,-0.0761458050921956));
#78400=CARTESIAN_POINT('Ctrl Pts',(1.43659894165698,-1.0479342912718,-0.039096685066162));
#78401=CARTESIAN_POINT('Ctrl Pts',(1.99168154594883,0.0894486046434957,
0.034989689861832));
#78402=CARTESIAN_POINT('Ctrl Pts',(1.00331804303196,1.72492464061588,0.146113319691788));
#78403=CARTESIAN_POINT('Ctrl Pts',(-0.903731476947885,1.77698500344193,
0.257225084397669));
#78404=CARTESIAN_POINT('Ctrl Pts',(-1.98350050017455,0.205798417197274,
0.368336849103552));
#78405=CARTESIAN_POINT('Ctrl Pts',(-1.2487621948887,-1.5550006799164,0.479448613809434));
#78406=CARTESIAN_POINT('Ctrl Pts',(0.628611946144605,-1.89240901695779,
0.590560378515317));
#78407=CARTESIAN_POINT('Ctrl Pts',(1.93079423086444,-0.498783661630547,
0.701672143221198));
#78408=CARTESIAN_POINT('Ctrl Pts',(1.46649297006114,1.35137870100134,0.812783907927082));
#78409=CARTESIAN_POINT('Ctrl Pts',(-0.339545742371582,1.96504087004499,
0.923895672632963));
#78410=CARTESIAN_POINT('Ctrl Pts',(-1.83491891749717,0.780905822148899,
1.03500743733885));
#78411=CARTESIAN_POINT('Ctrl Pts',(-1.6514978381298,-1.11772118379719,1.14611920204473));
#78412=CARTESIAN_POINT('Ctrl Pts',(0.0429097834904605,-1.99371116902587,
1.25723096675061));
#78413=CARTESIAN_POINT('Ctrl Pts',(1.69805716041152,-1.04562789387901,1.36834273145649));
#78414=CARTESIAN_POINT('Ctrl Pts',(1.79962332019217,0.859122470849831,1.47945449616237));
#78415=CARTESIAN_POINT('Ctrl Pts',(0.254682549820674,1.9778446936484,1.59056626086826));
#78416=CARTESIAN_POINT('Ctrl Pts',(-1.52327150456256,1.28700363897632,1.70167802557414));
#78417=CARTESIAN_POINT('Ctrl Pts',(-1.90755816524105,-0.581339927726226,
1.81278979028002));
#78418=CARTESIAN_POINT('Ctrl Pts',(-0.546586751757789,-1.91780521575438,
1.9239015549859));
#78419=CARTESIAN_POINT('Ctrl Pts',(1.31446632436265,-1.49963743924658,2.03501331969179));
#78420=CARTESIAN_POINT('Ctrl Pts',(1.97289139726728,0.29057470111471,2.14612508439767));
#78421=CARTESIAN_POINT('Ctrl Pts',(0.826283935675965,1.81493496800831,2.25723684910355));
#78422=CARTESIAN_POINT('Ctrl Pts',(-1.07630501291146,1.67877980564486,2.36834861380944));
#78423=CARTESIAN_POINT('Ctrl Pts',(-1.99416385649942,0.00667989606382068,
2.47946037851531));
#78424=CARTESIAN_POINT('Ctrl Pts',(-1.08752763064868,-1.6715315597813,2.5905721432212));
#78425=CARTESIAN_POINT('Ctrl Pts',(0.814106469189659,-1.82042982969354,
2.70168390792707));
#78426=CARTESIAN_POINT('Ctrl Pts',(1.97090045337651,-0.303785301212181,
2.81279567263297));
#78427=CARTESIAN_POINT('Ctrl Pts',(1.32448345972351,1.49079766258596,2.92390743733884));
#78428=CARTESIAN_POINT('Ctrl Pts',(-0.533726402547186,1.92142401198172,
3.03501920204473));
#78429=CARTESIAN_POINT('Ctrl Pts',(-1.9036207304579,0.594106237032703,3.14613096675061));
#78430=CARTESIAN_POINT('Ctrl Pts',(-1.53185946502735,-1.27676962905383,
3.25724273145649));
#78431=CARTESIAN_POINT('Ctrl Pts',(0.241426569875686,-1.97950683699981,
3.36835449616238));
#78432=CARTESIAN_POINT('Ctrl Pts',(1.79382725242915,-0.871158937718284,
3.47946626086825));
#78433=CARTESIAN_POINT('Ctrl Pts',(1.70502429727377,1.03422736959939,3.59057802557414));
#78434=CARTESIAN_POINT('Ctrl Pts',(0.0562650669144604,1.9933811348012,3.70168979028002));
#78435=CARTESIAN_POINT('Ctrl Pts',(-1.64397204815888,1.12875595732695,3.81280155498591));
#78436=CARTESIAN_POINT('Ctrl Pts',(-1.84011064868929,-0.768587605227587,
3.92391331969179));
#78437=CARTESIAN_POINT('Ctrl Pts',(-0.35270013025113,-1.96273704923809,
4.03502508439767));
#78438=CARTESIAN_POINT('Ctrl Pts',(1.45740184914221,-1.36114435547694,4.14613684910356));
#78439=CARTESIAN_POINT('Ctrl Pts',(1.93410162206783,0.48578289579255,4.25724861380943));
#78440=CARTESIAN_POINT('Ctrl Pts',(0.641258305751626,1.88825895777957,4.36836037851532));
#78441=CARTESIAN_POINT('Ctrl Pts',(-1.23828334658509,1.56313417846968,4.4794721432212));
#78442=CARTESIAN_POINT('Ctrl Pts',(-1.9848981074536,-0.192129147599384,
4.59058390792708));
#78443=CARTESIAN_POINT('Ctrl Pts',(-0.915495194370431,-1.77161018720676,
4.70169567263296));
#78444=CARTESIAN_POINT('Ctrl Pts',(0.991510136263189,-1.73021436707057,
4.81280743733884));
#78445=CARTESIAN_POINT('Ctrl Pts',(1.99136566177859,-0.105815440363751,
4.92391920204473));
#78446=CARTESIAN_POINT('Ctrl Pts',(1.16928623581682,1.61539586636197,5.03503096675061));
#78447=CARTESIAN_POINT('Ctrl Pts',(-0.722593429349912,1.85865350245553,
5.1461427314565));
#78448=CARTESIAN_POINT('Ctrl Pts',(-1.95335984449524,0.40139684134849,5.25725449616237));
#78449=CARTESIAN_POINT('Ctrl Pts',(-1.39696348898167,-1.42310474554101,
5.36836626086826));
#78450=CARTESIAN_POINT('Ctrl Pts',(0.437538969976939,-1.945583140367,5.47947802557413));
#78451=CARTESIAN_POINT('Ctrl Pts',(1.87172944338254,-0.688013805901528,
5.59058979028003));
#78452=CARTESIAN_POINT('Ctrl Pts',(1.59344221464069,1.19903128187857,5.7017015549859));
#78453=CARTESIAN_POINT('Ctrl Pts',(-0.142712908337992,1.98906187237041,
5.81281331969179));
#78454=CARTESIAN_POINT('Ctrl Pts',(-1.74829751848718,0.959265288240166,
5.92392508439767));
#78455=CARTESIAN_POINT('Ctrl Pts',(-1.75433443344276,-0.94817973080275,
6.03503684910355));
#78456=CARTESIAN_POINT('Ctrl Pts',(-0.155300375207596,-1.98811868352235,
6.14614861380944));
#78457=CARTESIAN_POINT('Ctrl Pts',(1.58582068757151,-1.20909340146497,6.25726037851532));
#78458=CARTESIAN_POINT('Ctrl Pts',(1.87604692303546,0.676152385503515,6.3683721432212));
#78459=CARTESIAN_POINT('Ctrl Pts',(0.449845319890602,1.94277463812065,6.47948390792708));
#78460=CARTESIAN_POINT('Ctrl Pts',(-1.38792756251823,1.43191870901136,6.59059567263297));
#78461=CARTESIAN_POINT('Ctrl Pts',(-1.95586146542837,-0.389024460441244,
6.70170743733884));
#78462=CARTESIAN_POINT('Ctrl Pts',(-0.734343824677687,-1.85404240909904,
6.81281920204473));
#78463=CARTESIAN_POINT('Ctrl Pts',(1.15903771275493,-1.62276483110497,6.9239309667506));
#78464=CARTESIAN_POINT('Ctrl Pts',(1.99199555021847,0.093208413597094,7.0350427314565));
#78465=CARTESIAN_POINT('Ctrl Pts',(1.00244216340755,1.72390366069626,7.14615449616237));
#78466=CARTESIAN_POINT('Ctrl Pts',(-0.904262973486885,1.77736958504813,
7.25726626086827));
#78467=CARTESIAN_POINT('Ctrl Pts',(-1.98364216277129,0.20468925923916,7.36837802557414));
#78468=CARTESIAN_POINT('Ctrl Pts',(-1.24815292281929,-1.55526478343856,
7.47948979028002));
#78469=CARTESIAN_POINT('Ctrl Pts',(0.629293358000169,-1.89228018880065,
7.59060155498591));
#78470=CARTESIAN_POINT('Ctrl Pts',(1.93098766371084,-0.498015537882957,
7.70171331969178));
#78471=CARTESIAN_POINT('Ctrl Pts',(1.46598899360024,1.35189192805549,7.81282508439768));
#78472=CARTESIAN_POINT('Ctrl Pts',(-0.340270502892587,1.964930481555,7.92393684910355));
#78473=CARTESIAN_POINT('Ctrl Pts',(-1.83520663505345,0.780219252308907,
8.03504861380944));
#78474=CARTESIAN_POINT('Ctrl Pts',(-1.65108800325447,-1.11832649953649,
8.14616037851531));
#78475=CARTESIAN_POINT('Ctrl Pts',(0.0436541027557139,-1.99369898835498,
8.25727214322121));
#78476=CARTESIAN_POINT('Ctrl Pts',(1.69842879970453,-1.0449959542716,8.36838390792707));
#78477=CARTESIAN_POINT('Ctrl Pts',(1.79933394887264,0.859780998390392,8.47949567263297));
#78478=CARTESIAN_POINT('Ctrl Pts',(0.253897521799402,1.97795034100281,8.59060743733884));
#78479=CARTESIAN_POINT('Ctrl Pts',(-1.52364416709162,1.28641879587735,8.70171920204473));
#78480=CARTESIAN_POINT('Ctrl Pts',(-1.90753920492918,-0.582003707532747,
8.8128309667506));
#78481=CARTESIAN_POINT('Ctrl Pts',(-0.545504302009522,-1.91808557661087,
8.9239427314565));
#78482=CARTESIAN_POINT('Ctrl Pts',(1.31430661885738,-1.49900113292539,9.03505449616237));
#78483=CARTESIAN_POINT('Ctrl Pts',(1.97416463095097,0.291008799144495,9.14616626086825));
#78484=CARTESIAN_POINT('Ctrl Pts',(0.822675933898107,1.81604024164875,9.25728993393975));
#78485=CARTESIAN_POINT('Ctrl Pts',(-0.439507696560592,1.7230254506574,9.33137635210928));
#78486=CARTESIAN_POINT('Ctrl Pts',(-0.911671767707743,1.41983313348876,
9.36842551537684));
#78487=CARTESIAN_POINT('Ctrl Pts',(0.901589692180969,-1.2641536789049,0.00156774322393706));
#78488=CARTESIAN_POINT('Ctrl Pts',(1.32199654062011,-0.964336996002927,
0.0386168632499707));
#78489=CARTESIAN_POINT('Ctrl Pts',(1.83279831093593,0.082312984141298,0.112703238177965));
#78490=CARTESIAN_POINT('Ctrl Pts',(0.923279938171269,1.58732151444747,0.223826868007921));
#78491=CARTESIAN_POINT('Ctrl Pts',(-0.831637732376869,1.63522884443621,
0.334938632713803));
#78492=CARTESIAN_POINT('Ctrl Pts',(-1.82526989510695,0.189381175017482,
0.446050397419685));
#78493=CARTESIAN_POINT('Ctrl Pts',(-1.14914417227393,-1.4309529680847,0.557162162125568));
#78494=CARTESIAN_POINT('Ctrl Pts',(0.578465425595506,-1.74144509042373,
0.668273926831449));
#78495=CARTESIAN_POINT('Ctrl Pts',(1.77676818479901,-0.458993986472553,
0.779385691537333));
#78496=CARTESIAN_POINT('Ctrl Pts',(1.34950582034287,1.24357460943893,0.890497456243214));
#78497=CARTESIAN_POINT('Ctrl Pts',(-0.312459019550576,1.80828285268003,
1.0016092209491));
#78498=CARTESIAN_POINT('Ctrl Pts',(-1.68854117242476,0.718610299294945,
1.11272098565498));
#78499=CARTESIAN_POINT('Ctrl Pts',(-1.51975221861918,-1.02855674991199,
1.22383275036086));
#78500=CARTESIAN_POINT('Ctrl Pts',(0.0394867235999322,-1.83466602405251,
1.33494451506675));
#78501=CARTESIAN_POINT('Ctrl Pts',(1.56259734484424,-0.962214587802463,
1.44605627977263));
#78502=CARTESIAN_POINT('Ctrl Pts',(1.65606122538921,0.79058733895662,1.55716804447851));
#78503=CARTESIAN_POINT('Ctrl Pts',(0.234365653528104,1.82006527157203,1.66827980918439));
#78504=CARTESIAN_POINT('Ctrl Pts',(-1.40175493734822,1.18433496583934,1.77939157389028));
#78505=CARTESIAN_POINT('Ctrl Pts',(-1.75538573944072,-0.534964457437233,
1.89050333859615));
#78506=CARTESIAN_POINT('Ctrl Pts',(-0.502983660936798,-1.76481534775894,
2.00161510330204));
#78507=CARTESIAN_POINT('Ctrl Pts',(1.20960685907562,-1.38000624209127,2.11272686800792));
#78508=CARTESIAN_POINT('Ctrl Pts',(1.81550711655005,0.267394565404816,2.2238386327138));
#78509=CARTESIAN_POINT('Ctrl Pts',(0.76036844581944,1.6701514107967,2.33495039741969));
#78510=CARTESIAN_POINT('Ctrl Pts',(-0.990444488341258,1.54485781046558,
2.44606216212557));
#78511=CARTESIAN_POINT('Ctrl Pts',(-1.83508259910117,0.00614701795468853,
2.55717392683145));
#78512=CARTESIAN_POINT('Ctrl Pts',(-1.00077183955604,-1.5381877819146,2.66828569153734));
#78513=CARTESIAN_POINT('Ctrl Pts',(0.749162417399423,-1.67520792861,2.77939745624321));
#78514=CARTESIAN_POINT('Ctrl Pts',(1.81367499704902,-0.2795513108415,2.8905092209491));
#78515=CARTESIAN_POINT('Ctrl Pts',(1.21882489335781,1.3718716445872,3.00162098565498));
#78516=CARTESIAN_POINT('Ctrl Pts',(-0.491149225678246,1.76814546025939,
3.11273275036087));
#78517=CARTESIAN_POINT('Ctrl Pts',(-1.75176240726965,0.546712354675795,
3.22384451506675));
#78518=CARTESIAN_POINT('Ctrl Pts',(-1.40965780689392,-1.17491735781956,
3.33495627977263));
#78519=CARTESIAN_POINT('Ctrl Pts',(0.22216714834923,-1.821594820075,3.44606804447851));
#78520=CARTESIAN_POINT('Ctrl Pts',(1.65072752973505,-0.801663615779567,
3.55717980918439));
#78521=CARTESIAN_POINT('Ctrl Pts',(1.56900868941844,0.951723522257404,3.66829157389028));
#78522=CARTESIAN_POINT('Ctrl Pts',(0.0517766104803488,1.83436231778444,
3.77940333859616));
#78523=CARTESIAN_POINT('Ctrl Pts',(-1.5128267866016,1.03871124189289,3.89051510330204));
#78524=CARTESIAN_POINT('Ctrl Pts',(-1.69331874149904,-0.707274748582536,
4.00162686800792));
#78525=CARTESIAN_POINT('Ctrl Pts',(-0.324564037009825,-1.80616281552239,
4.11273863271381));
#78526=CARTESIAN_POINT('Ctrl Pts',(1.34113992916987,-1.25256122432444,4.22385039741969));
#78527=CARTESIAN_POINT('Ctrl Pts',(1.77981173411717,0.447030336100252,4.33496216212557));
#78528=CARTESIAN_POINT('Ctrl Pts',(0.590102941931552,1.73762609563133,4.44607392683145));
#78529=CARTESIAN_POINT('Ctrl Pts',(-1.13950125746637,1.43843762969677,4.55718569153734));
#78530=CARTESIAN_POINT('Ctrl Pts',(-1.82655601048297,-0.176802349711979,
4.66829745624321));
#78531=CARTESIAN_POINT('Ctrl Pts',(-0.842463017908167,-1.63028279563768,
4.7794092209491));
#78532=CARTESIAN_POINT('Ctrl Pts',(0.912413988428717,-1.59218926136772,
4.89052098565498));
#78533=CARTESIAN_POINT('Ctrl Pts',(1.83250762592413,-0.0973741815121382,
5.00163275036086));
#78534=CARTESIAN_POINT('Ctrl Pts',(1.07600828172795,1.48653022436408,5.11274451506675));
#78535=CARTESIAN_POINT('Ctrl Pts',(-0.664949685103911,1.71038236852908,
5.22385627977262));
#78536=CARTESIAN_POINT('Ctrl Pts',(-1.79753366240856,0.369376045249255,
5.33496804447852));
#78537=CARTESIAN_POINT('Ctrl Pts',(-1.28552294329012,-1.30957882258728,
5.44607980918439));
#78538=CARTESIAN_POINT('Ctrl Pts',(0.402634992915184,-1.7903773325124,5.55719157389028));
#78539=CARTESIAN_POINT('Ctrl Pts',(1.722415197017,-0.633128596246625,5.66830333859616));
#78540=CARTESIAN_POINT('Ctrl Pts',(1.46632789037372,1.10338046393831,5.77941510330204));
#78541=CARTESIAN_POINT('Ctrl Pts',(-0.131328212526088,1.83038761766044,
5.89052686800793));
#78542=CARTESIAN_POINT('Ctrl Pts',(-1.60882985807365,0.88274142199196,6.0016386327138));
#78543=CARTESIAN_POINT('Ctrl Pts',(-1.61438518771777,-0.872540197309049,
6.11275039741969));
#78544=CARTESIAN_POINT('Ctrl Pts',(-0.142911534199397,-1.82951967020612,
6.22386216212556));
#78545=CARTESIAN_POINT('Ctrl Pts',(1.459314358533,-1.11263989390083,6.33497392683146));
#78546=CARTESIAN_POINT('Ctrl Pts',(1.72638825658138,0.622213401839696,6.44608569153733));
#78547=CARTESIAN_POINT('Ctrl Pts',(0.413959623291646,1.78779287407635,6.55719745624322));
#78548=CARTESIAN_POINT('Ctrl Pts',(-1.27720784352249,1.31768966610738,6.66830922094909));
#78549=CARTESIAN_POINT('Ctrl Pts',(-1.79983572050121,-0.357990651396945,
6.77942098565499));
#78550=CARTESIAN_POINT('Ctrl Pts',(-0.67576271128941,-1.70613911782843,
6.89053275036086));
#78551=CARTESIAN_POINT('Ctrl Pts',(1.06657731833143,-1.49331134163745,7.00164451506675));
#78552=CARTESIAN_POINT('Ctrl Pts',(1.8330872660132,0.085772860301527,7.11275627977262));
#78553=CARTESIAN_POINT('Ctrl Pts',(0.922473930454079,1.58638198158088,7.22386804447851));
#78554=CARTESIAN_POINT('Ctrl Pts',(-0.832126829622823,1.635582746655,7.33497980918439));
#78555=CARTESIAN_POINT('Ctrl Pts',(-1.82540025679483,0.188360498375512,
7.44609157389027));
#78556=CARTESIAN_POINT('Ctrl Pts',(-1.14858350391709,-1.43119600316746,
7.55720333859616));
#78557=CARTESIAN_POINT('Ctrl Pts',(0.579092478901528,-1.7413265393284,7.66831510330204));
#78558=CARTESIAN_POINT('Ctrl Pts',(1.77694618684701,-0.458287138578105,
7.77942686800792));
#78559=CARTESIAN_POINT('Ctrl Pts',(1.34904204780445,1.24404689461921,7.8905386327138));
#78560=CARTESIAN_POINT('Ctrl Pts',(-0.313125963451037,1.80818127025666,
8.00165039741968));
#78561=CARTESIAN_POINT('Ctrl Pts',(-1.68880593776952,0.71797849947452,8.11276216212556));
#78562=CARTESIAN_POINT('Ctrl Pts',(-1.51937507767073,-1.02911377754868,
8.22387392683146));
#78563=CARTESIAN_POINT('Ctrl Pts',(0.0401716659768548,-1.83465481507531,
8.33498569153734));
#78564=CARTESIAN_POINT('Ctrl Pts',(1.56293933720236,-0.961633060174499,
8.4460974562432));
#78565=CARTESIAN_POINT('Ctrl Pts',(1.65579493820754,0.791193333507556,8.5572092209491));
#78566=CARTESIAN_POINT('Ctrl Pts',(0.233643249871581,1.82016249107638,8.66832098565497));
#78567=CARTESIAN_POINT('Ctrl Pts',(-1.40209787131535,1.1837967776706,8.77943275036085));
#78568=CARTESIAN_POINT('Ctrl Pts',(-1.75536829165764,-0.535575285262948,
8.89054451506673));
#78569=CARTESIAN_POINT('Ctrl Pts',(-0.501987561899616,-1.76507334327297,
9.00165627977261));
#78570=CARTESIAN_POINT('Ctrl Pts',(1.20945989382363,-1.37942069609719,9.11276804447851));
#78571=CARTESIAN_POINT('Ctrl Pts',(1.81667878003692,0.267794033953083,9.22387980918439));
#78572=CARTESIAN_POINT('Ctrl Pts',(0.75704826665839,1.67116851298627,9.33500348225587));
#78573=CARTESIAN_POINT('Ctrl Pts',(-0.404446667459514,1.58557382935436,
9.40908990042542));
#78574=CARTESIAN_POINT('Ctrl Pts',(-0.838944599040669,1.30656819819523,
9.44613906369298));
#78575=CARTESIAN_POINT('Ctrl Pts',(0.863568020353677,1.75641452067799,3.4477629085039E-17));
#78576=CARTESIAN_POINT('Ctrl Pts',(0.902604744553564,1.73244180767701,-5.99597736019976E-15));
#78577=CARTESIAN_POINT('Ctrl Pts',(0.940679665251258,1.70703474391515,-4.40943913592352E-15));
#78578=CARTESIAN_POINT('Ctrl Pts',(0.977702286264216,1.68018861076749,-4.36976843598558E-15));
#78579=CARTESIAN_POINT('Ctrl Pts',(1.03605877752412,1.63787269440259,-4.43296922755967E-15));
#78580=CARTESIAN_POINT('Ctrl Pts',(1.09180306576185,1.59198254673329,-2.65889931022495E-15));
#78581=CARTESIAN_POINT('Ctrl Pts',(1.14477205735549,1.54286237604396,-3.09821612809458E-15));
#78582=CARTESIAN_POINT('Ctrl Pts',(1.16982237017091,1.5196322634008,-3.30597963994575E-15));
#78583=CARTESIAN_POINT('Ctrl Pts',(1.19425134178148,1.49567928312504,-2.72106579808279E-15));
#78584=CARTESIAN_POINT('Ctrl Pts',(1.21803815377256,1.47103794919798,-4.64212002171394E-15));
#78585=CARTESIAN_POINT('Ctrl Pts',(1.23019217561359,1.45844730397601,-5.76026679289046E-15));
#78586=CARTESIAN_POINT('Ctrl Pts',(1.24217850624866,1.44567693083781,-3.72464628310254E-15));
#78587=CARTESIAN_POINT('Ctrl Pts',(1.25399412029808,1.43273135759888,-2.41820452551167E-15));
#78588=CARTESIAN_POINT('Ctrl Pts',(1.26387705342325,1.42190329279817,-1.3484661602068E-15));
#78589=CARTESIAN_POINT('Ctrl Pts',(1.2736338482894,1.41095997328553,-6.32726586808925E-15));
#78590=CARTESIAN_POINT('Ctrl Pts',(1.28326192166555,1.39990597410979,-5.98132654516803E-15));
#78591=CARTESIAN_POINT('Ctrl Pts',(1.33009865628678,1.34613267952935,-3.80188911589394E-15));
#78592=CARTESIAN_POINT('Ctrl Pts',(1.37390394515539,1.28973012991194,-4.25185171829959E-15));
#78593=CARTESIAN_POINT('Ctrl Pts',(1.41451494832603,1.23103154357669,-3.94129173741931E-15));
#78594=CARTESIAN_POINT('Ctrl Pts',(1.45486584844222,1.17270890662475,-3.63272081352632E-15));
#78595=CARTESIAN_POINT('Ctrl Pts',(1.49206356397675,1.11211847710431,-7.13207777158734E-16));
#78596=CARTESIAN_POINT('Ctrl Pts',(1.52589939946977,1.04957342610525,-2.692290834716E-15));
#78597=CARTESIAN_POINT('Ctrl Pts',(1.53053080128998,1.04101234703564,-2.96318495456163E-15));
#78598=CARTESIAN_POINT('Ctrl Pts',(1.53509913603607,1.03241463996483,-2.92290991889344E-15));
#78599=CARTESIAN_POINT('Ctrl Pts',(1.53960379146143,1.02378110502453,-2.83800760669806E-15));
#78600=CARTESIAN_POINT('Ctrl Pts',(1.54537176342799,1.01272632218197,-2.70321459129075E-15));
#78601=CARTESIAN_POINT('Ctrl Pts',(1.55103093390346,1.00162120437101,-4.3669508804682E-15));
#78602=CARTESIAN_POINT('Ctrl Pts',(1.5565797653852,0.990469147617545,-4.08006961549745E-15));
#78603=CARTESIAN_POINT('Ctrl Pts',(1.58754040005414,0.928244379017568,-2.50540767500275E-15));
#78604=CARTESIAN_POINT('Ctrl Pts',(1.61507828167858,0.864543360735049,-2.82488097698718E-15));
#78605=CARTESIAN_POINT('Ctrl Pts',(1.63904016583111,0.799672791855858,-2.70616862252382E-15));
#78606=CARTESIAN_POINT('Ctrl Pts',(1.66267588766689,0.735685222614781,-2.58907214669142E-15));
#78607=CARTESIAN_POINT('Ctrl Pts',(1.68283248873858,0.670558732897526,7.68102358593484E-16));
#78608=CARTESIAN_POINT('Ctrl Pts',(1.69931294953593,0.604582527528084,-9.85322934354826E-16));
#78609=CARTESIAN_POINT('Ctrl Pts',(1.71527503781385,0.540681522131514,-2.68359640249016E-15));
#78610=CARTESIAN_POINT('Ctrl Pts',(1.72778860472168,0.47598262367475,1.07798551632638E-15));
#78611=CARTESIAN_POINT('Ctrl Pts',(1.73662635850792,0.410756644998871,3.05311331771918E-16));
#78612=CARTESIAN_POINT('Ctrl Pts',(1.73865577550429,0.395778776987271,1.27881844515988E-16));
#78613=CARTESIAN_POINT('Ctrl Pts',(1.74049115966569,0.380773177713919,-4.3644896247511E-16));
#78614=CARTESIAN_POINT('Ctrl Pts',(1.74212938372161,0.365743253928758,-1.38777878078145E-17));
#78615=CARTESIAN_POINT('Ctrl Pts',(1.74338441815136,0.3542289120664,3.87855657381648E-16));
#78616=CARTESIAN_POINT('Ctrl Pts',(1.74452367514155,0.342699905808244,-1.50379722807899E-15));
#78617=CARTESIAN_POINT('Ctrl Pts',(1.74554463432397,0.331172964306999,-1.51267887105178E-15));
#78618=CARTESIAN_POINT('Ctrl Pts',(1.75129363197339,0.266265022112653,-1.3177032770474E-15));
#78619=CARTESIAN_POINT('Ctrl Pts',(1.75330947147495,0.201304509751003,1.38313017624184E-15));
#78620=CARTESIAN_POINT('Ctrl Pts',(1.75142501653378,0.136551819838442,1.4432899320127E-15));
#78621=CARTESIAN_POINT('Ctrl Pts',(1.75088238549665,0.117906205917835,1.35711357567772E-15));
#78622=CARTESIAN_POINT('Ctrl Pts',(1.75001603328345,0.0992778655205721,
3.28733412684628E-15));
#78623=CARTESIAN_POINT('Ctrl Pts',(1.74882116957219,0.0806731627252346,
2.63677968348475E-15));
#78624=CARTESIAN_POINT('Ctrl Pts',(1.74456363386159,0.0143809272263788,
6.91801324858725E-16));
#78625=CARTESIAN_POINT('Ctrl Pts',(1.73613879272151,-0.0516130402840126,
4.04016429869329E-16));
#78626=CARTESIAN_POINT('Ctrl Pts',(1.72372214259613,-0.11700388521066,9.71445146547012E-16));
#78627=CARTESIAN_POINT('Ctrl Pts',(1.71175302959027,-0.180037827906305,
1.51842185637614E-15));
#78628=CARTESIAN_POINT('Ctrl Pts',(1.69607381160222,-0.242511988113435,
2.89105311828119E-15));
#78629=CARTESIAN_POINT('Ctrl Pts',(1.67680526621061,-0.304125446889571,
1.19348975147204E-15));
#78630=CARTESIAN_POINT('Ctrl Pts',(1.67349606673433,-0.314707004623689,
9.48250798678759E-16));
#78631=CARTESIAN_POINT('Ctrl Pts',(1.67008251071857,-0.325257870756689,
2.04358541335377E-15));
#78632=CARTESIAN_POINT('Ctrl Pts',(1.66656792507904,-0.335769504324591,
1.99840144432528E-15));
#78633=CARTESIAN_POINT('Ctrl Pts',(1.64602352982566,-0.397214914090365,
1.51477858788014E-15));
#78634=CARTESIAN_POINT('Ctrl Pts',(1.62200717575525,-0.457397724739045,
1.74320425236897E-15));
#78635=CARTESIAN_POINT('Ctrl Pts',(1.59470526868992,-0.516044303385602,
2.16493489801906E-15));
#78636=CARTESIAN_POINT('Ctrl Pts',(1.56766219269019,-0.574134893162653,
2.58266739833275E-15));
#78637=CARTESIAN_POINT('Ctrl Pts',(1.53739478791158,-0.630719029504753,
8.07801581179909E-18));
#78638=CARTESIAN_POINT('Ctrl Pts',(1.50404540903,-0.685498994844113,7.21644966006352E-16));
#78639=CARTESIAN_POINT('Ctrl Pts',(1.47097211704488,-0.739825457565848,
1.4293045652605E-15));
#78640=CARTESIAN_POINT('Ctrl Pts',(1.43486696802975,-0.792378215342184,
-2.4045611359052E-16));
#78641=CARTESIAN_POINT('Ctrl Pts',(1.39584139349689,-0.842824299455657,
2.22044604925031E-15));
#78642=CARTESIAN_POINT('Ctrl Pts',(1.38890909242928,-0.851785280733763,
2.64967646930877E-15));
#78643=CARTESIAN_POINT('Ctrl Pts',(1.38188458496569,-0.860679662653789,
2.3719929389117E-16));
#78644=CARTESIAN_POINT('Ctrl Pts',(1.37476842993966,-0.869505410466458,
-2.22044604925031E-16));
#78645=CARTESIAN_POINT('Ctrl Pts',(1.36798353599758,-0.877920314673784,
-4.05596237883174E-16));
#78646=CARTESIAN_POINT('Ctrl Pts',(1.36111848029899,-0.886268835999708,
1.31266055721992E-15));
#78647=CARTESIAN_POINT('Ctrl Pts',(1.35417907408573,-0.894543489490856,
1.4432899320127E-15));
#78648=CARTESIAN_POINT('Ctrl Pts',(1.31426263110496,-0.942140463081207,
2.31521532630317E-15));
#78649=CARTESIAN_POINT('Ctrl Pts',(1.27183845241668,-0.987359134401659,
5.67715419627107E-16));
#78650=CARTESIAN_POINT('Ctrl Pts',(1.22704572742311,-1.02993139787447,3.05311331771918E-16));
#78651=CARTESIAN_POINT('Ctrl Pts',(1.18365605299434,-1.07117016269724,5.11265742594509E-17));
#78652=CARTESIAN_POINT('Ctrl Pts',(1.13804315862614,-1.10992612710962,-1.65473560180465E-15));
#78653=CARTESIAN_POINT('Ctrl Pts',(1.09031115841745,-1.14591358180653,-8.88178419700125E-16));
#78654=CARTESIAN_POINT('Ctrl Pts',(1.04296628811536,-1.18160916061483,-1.278383918949E-16));
#78655=CARTESIAN_POINT('Ctrl Pts',(0.993535978873267,-1.21458145867935,
2.50738491799621E-16));
#78656=CARTESIAN_POINT('Ctrl Pts',(0.942108816666581,-1.24450267784172,
-4.44089209850063E-16));
#78657=CARTESIAN_POINT('Ctrl Pts',(0.929396434173388,-1.25189896350738,
-6.16937577112259E-16));
#78658=CARTESIAN_POINT('Ctrl Pts',(0.916561996392962,-1.25910856034592,
8.48047714131713E-16));
#78659=CARTESIAN_POINT('Ctrl Pts',(0.903606778650234,-1.26612599672282,
1.38777878078145E-16));
#78660=CARTESIAN_POINT('Ctrl Pts',(-0.68439852523474,1.39375347375506,-0.231693356019416));
#78661=CARTESIAN_POINT('Ctrl Pts',(-1.14819351642417,1.16601490671122,-0.194620613066161));
#78662=CARTESIAN_POINT('Ctrl Pts',(-1.82243947067649,0.215139425440093,
-0.120480536464354));
#78663=CARTESIAN_POINT('Ctrl Pts',(-1.16700196451825,-1.41845288290798,
-0.00927312621399557));
#78664=CARTESIAN_POINT('Ctrl Pts',(0.559230889619531,-1.74776969680176,
0.10192887473166));
#78665=CARTESIAN_POINT('Ctrl Pts',(1.77226725459718,-0.47789618903822,0.213130875677316));
#78666=CARTESIAN_POINT('Ctrl Pts',(1.36182366705032,1.23103394611838,0.324332876622972));
#78667=CARTESIAN_POINT('Ctrl Pts',(-0.296644861836514,1.8113809601377,0.435534877568628));
#78668=CARTESIAN_POINT('Ctrl Pts',(-1.68319109737169,0.732320442306668,
0.546736878514283));
#78669=CARTESIAN_POINT('Ctrl Pts',(-1.52752491192947,-1.01791849072323,
0.65793887945994));
#78670=CARTESIAN_POINT('Ctrl Pts',(0.0278106025051759,-1.8353719156861,
0.769140880405594));
#78671=CARTESIAN_POINT('Ctrl Pts',(1.55764750349177,-0.97116016910973,0.880342881351252));
#78672=CARTESIAN_POINT('Ctrl Pts',(1.6602541346855,0.782929184096576,0.991544882296906));
#78673=CARTESIAN_POINT('Ctrl Pts',(0.241601151042511,1.81962454490285,1.10274688324257));
#78674=CARTESIAN_POINT('Ctrl Pts',(-1.39842339561947,1.18904387044759,1.21394888418822));
#78675=CARTESIAN_POINT('Ctrl Pts',(-1.75710394763706,-0.531035633958278,
1.32515088513388));
#78676=CARTESIAN_POINT('Ctrl Pts',(-0.505787344160485,-1.76453676504907,
1.43635288607953));
#78677=CARTESIAN_POINT('Ctrl Pts',(1.20897096626336,-1.38123183937464,1.54755488702519));
#78678=CARTESIAN_POINT('Ctrl Pts',(1.81597539920978,0.267666584309658,1.65875688797085));
#78679=CARTESIAN_POINT('Ctrl Pts',(0.759040591941426,1.67130761262598,1.7699588889165));
#78680=CARTESIAN_POINT('Ctrl Pts',(-0.993386711824161,1.5435656135746,1.88116088986216));
#78681=CARTESIAN_POINT('Ctrl Pts',(-1.83559519323598,0.00148761400844592,
1.99236289080781));
#78682=CARTESIAN_POINT('Ctrl Pts',(-0.995887320575892,-1.54195341526314,
2.10356489175347));
#78683=CARTESIAN_POINT('Ctrl Pts',(0.756330647254053,-1.67253576128902,
2.21476689269912));
#78684=CARTESIAN_POINT('Ctrl Pts',(1.81553913667872,-0.270609601690128,
2.32596889364478));
#78685=CARTESIAN_POINT('Ctrl Pts',(1.21120821638892,1.37927030188772,2.43717089459044));
#78686=CARTESIAN_POINT('Ctrl Pts',(-0.502926704453015,1.76535453762567,
2.54837289553609));
#78687=CARTESIAN_POINT('Ctrl Pts',(-1.75624071862036,0.533882431307681,
2.65957489648175));
#78688=CARTESIAN_POINT('Ctrl Pts',(-1.40034918806097,-1.1867746472047,2.7707768974274));
#78689=CARTESIAN_POINT('Ctrl Pts',(0.23865214255216,-1.82001567774525,2.88197889837307));
#78690=CARTESIAN_POINT('Ctrl Pts',(1.65898165512988,-0.785615542163932,
2.99318089931871));
#78691=CARTESIAN_POINT('Ctrl Pts',(1.55922200833015,0.968627193943045,3.10438290026438));
#78692=CARTESIAN_POINT('Ctrl Pts',(0.0307808179488378,1.8353376946604,3.21558490121002));
#78693=CARTESIAN_POINT('Ctrl Pts',(-1.5258641729711,1.02036779535577,3.32678690215569));
#78694=CARTESIAN_POINT('Ctrl Pts',(-1.68439268635781,-0.729543138065348,
3.43798890310133));
#78695=CARTESIAN_POINT('Ctrl Pts',(-0.299548459802115,-1.81098940703584,
3.549190904047));
#78696=CARTESIAN_POINT('Ctrl Pts',(1.35976556877685,-1.23306508754754,3.66039290499265));
#78697=CARTESIAN_POINT('Ctrl Pts',(1.77315569340789,0.474690213818483,3.77159490593831));
#78698=CARTESIAN_POINT('Ctrl Pts',(0.561841446517521,1.74749709617399,3.88279690688396));
#78699=CARTESIAN_POINT('Ctrl Pts',(-1.16427601683786,1.41911002701576,3.99399890782962));
#78700=CARTESIAN_POINT('Ctrl Pts',(-1.82359244222051,-0.209576995008506,
4.10520090877527));
#78701=CARTESIAN_POINT('Ctrl Pts',(-0.811990389454478,-1.64623313039021,
4.21640290972094));
#78702=CARTESIAN_POINT('Ctrl Pts',(0.943620968464573,-1.57448130507625,
4.32760491066658));
#78703=CARTESIAN_POINT('Ctrl Pts',(1.83461275675203,-0.0600661712062762,
4.43880691161225));
#78704=CARTESIAN_POINT('Ctrl Pts',(1.04458839004179,1.50938630163076,4.5500089125579));
#78705=CARTESIAN_POINT('Ctrl Pts',(-0.702569820048048,1.69582061554822,
4.66121091350355));
#78706=CARTESIAN_POINT('Ctrl Pts',(-1.80597843602436,0.328411024138448,
4.77241291444921));
#78707=CARTESIAN_POINT('Ctrl Pts',(-1.2546079083578,-1.33991451535041,4.88361491539487));
#78708=CARTESIAN_POINT('Ctrl Pts',(0.446332823906676,-1.78050524359359,
4.99481691634052));
#78709=CARTESIAN_POINT('Ctrl Pts',(1.73830840277212,-0.589657365774751,
5.10601891728618));
#78710=CARTESIAN_POINT('Ctrl Pts',(1.43750943198197,1.14148085622289,5.21722091823183));
#78711=CARTESIAN_POINT('Ctrl Pts',(-0.180448470157521,1.8267047549561,5.32842291917749));
#78712=CARTESIAN_POINT('Ctrl Pts',(-1.63306532560299,0.838158430413411,
5.43962492012315));
#78713=CARTESIAN_POINT('Ctrl Pts',(-1.58933959627052,-0.918374411602515,
5.55082692106879));
#78714=CARTESIAN_POINT('Ctrl Pts',(-0.0893362261792351,-1.83342056028012,
5.66202892201447));
#78715=CARTESIAN_POINT('Ctrl Pts',(1.49252400382976,-1.06854293790466,5.77323092296011));
#78716=CARTESIAN_POINT('Ctrl Pts',(1.7068166352141,0.675417564113012,5.88443292390577));
#78717=CARTESIAN_POINT('Ctrl Pts',(0.357189945282142,1.8005074993413,5.99563492485143));
#78718=CARTESIAN_POINT('Ctrl Pts',(-1.31972219832623,1.27583119234171,6.10683692579707));
#78719=CARTESIAN_POINT('Ctrl Pts',(-1.78740131588285,-0.417861757196418,
6.21803892674275));
#78720=CARTESIAN_POINT('Ctrl Pts',(-0.617323104851327,-1.72867697867472,
6.32924092768838));
#78721=CARTESIAN_POINT('Ctrl Pts',(1.11839497117872,-1.45554271671877,6.44044292863406));
#78722=CARTESIAN_POINT('Ctrl Pts',(1.82935182324127,0.15127398653771,6.5516449295797));
#78723=CARTESIAN_POINT('Ctrl Pts',(0.864113000263691,1.61948159493796,6.66284693052535));
#78724=CARTESIAN_POINT('Ctrl Pts',(-0.892893953325356,1.60379309676545,
6.77404893147102));
#78725=CARTESIAN_POINT('Ctrl Pts',(-1.83176140908467,0.118583529746572,
6.88525093241666));
#78726=CARTESIAN_POINT('Ctrl Pts',(-1.09222533755543,-1.47528157745168,
6.99645293336233));
#78727=CARTESIAN_POINT('Ctrl Pts',(0.648093284931744,-1.71737793864714,
7.10765493430798));
#78728=CARTESIAN_POINT('Ctrl Pts',(1.79457799181862,-0.385877905180821,
7.21885693525364));
#78729=CARTESIAN_POINT('Ctrl Pts',(1.29672953139232,1.29919378271827,7.3300589361993));
#78730=CARTESIAN_POINT('Ctrl Pts',(-0.389284259787326,1.79384211159125,
7.44126093714495));
#78731=CARTESIAN_POINT('Ctrl Pts',(-1.71860528684267,0.644831698141129,
7.55246293809061));
#78732=CARTESIAN_POINT('Ctrl Pts',(-1.4732052694108,-1.09502439495669,7.66366493903626));
#78733=CARTESIAN_POINT('Ctrl Pts',(0.122060938605742,-1.83153268056824,
7.77486693998192));
#78734=CARTESIAN_POINT('Ctrl Pts',(1.60548546662183,-0.889848045343311,
7.88606894092758));
#78735=CARTESIAN_POINT('Ctrl Pts',(1.61783799478507,0.86718714352479,7.99727094187323));
#78736=CARTESIAN_POINT('Ctrl Pts',(0.147800881629908,1.82963370650723,8.10847294281889));
#78737=CARTESIAN_POINT('Ctrl Pts',(-1.45766388768593,1.11563340286439,8.21967494376454));
#78738=CARTESIAN_POINT('Ctrl Pts',(-1.72750093382561,-0.620611265472203,
8.3308769447102));
#78739=CARTESIAN_POINT('Ctrl Pts',(-0.414469315409945,-1.78817747583527,
8.44207894565586));
#78740=CARTESIAN_POINT('Ctrl Pts',(1.27833776903631,-1.31732416609453,8.5532809466015));
#78741=CARTESIAN_POINT('Ctrl Pts',(1.79981975869741,0.360658199260608,8.66448294754718));
#78742=CARTESIAN_POINT('Ctrl Pts',(0.672188007145546,1.70799954328245,8.77568494849281));
#78743=CARTESIAN_POINT('Ctrl Pts',(-1.07139767954464,1.49067611804192,8.88688694943849));
#78744=CARTESIAN_POINT('Ctrl Pts',(-1.83320374739229,-0.0931665699783311,
8.99808895038412));
#78745=CARTESIAN_POINT('Ctrl Pts',(-0.915438807724953,-1.59041186183777,
9.1092909513298));
#78746=CARTESIAN_POINT('Ctrl Pts',(0.841415087544887,-1.63276538935367,
9.22049295227544));
#78747=CARTESIAN_POINT('Ctrl Pts',(1.82685908457424,-0.174175557263367,
9.3317068594123));
#78748=CARTESIAN_POINT('Ctrl Pts',(1.36830267541603,0.897665970907806,9.40585343290059));
#78749=CARTESIAN_POINT('Ctrl Pts',(0.962873456568253,1.21812346587503,9.44293267274032));
#78750=CARTESIAN_POINT('Ctrl Pts',(-0.743729541425814,1.51457899699737,
-0.153978113886642));
#78751=CARTESIAN_POINT('Ctrl Pts',(-1.24773126468288,1.267097604523,-0.116905370933388));
#78752=CARTESIAN_POINT('Ctrl Pts',(-1.98042810121144,0.233790021932478,
-0.0427652943315806));
#78753=CARTESIAN_POINT('Ctrl Pts',(-1.26817023110404,-1.54141961626444,
0.068442115918778));
#78754=CARTESIAN_POINT('Ctrl Pts',(0.607711030565455,-1.89928514921112,
0.179644116864434));
#78755=CARTESIAN_POINT('Ctrl Pts',(1.9259064184767,-0.519325364414904,0.29084611781009));
#78756=CARTESIAN_POINT('Ctrl Pts',(1.47988117164744,1.33775319272089,0.402048118755746));
#78757=CARTESIAN_POINT('Ctrl Pts',(-0.322361225112689,1.96841092018517,
0.513250119701402));
#78758=CARTESIAN_POINT('Ctrl Pts',(-1.82910818305885,0.795805845061834,
0.624452120647057));
#78759=CARTESIAN_POINT('Ctrl Pts',(-1.65994718044751,-1.10616260029898,
0.735654121592714));
#78760=CARTESIAN_POINT('Ctrl Pts',(0.0302215242805287,-1.99448166947888,
0.846856122538369));
#78761=CARTESIAN_POINT('Ctrl Pts',(1.69268112183274,-1.05535076507549,0.958058123484026));
#78762=CARTESIAN_POINT('Ctrl Pts',(1.80418279805099,0.850801896245051,1.06926012442968));
#78763=CARTESIAN_POINT('Ctrl Pts',(0.262545734170277,1.97736914743293,1.18046212537534));
#78764=CARTESIAN_POINT('Ctrl Pts',(-1.51965375785472,1.29212296622041,1.291664126321));
#78765=CARTESIAN_POINT('Ctrl Pts',(-1.90942859318027,-0.5770715072612,1.40286612726665));
#78766=CARTESIAN_POINT('Ctrl Pts',(-0.54963442447871,-1.91750576705121,
1.51406812821231));
#78767=CARTESIAN_POINT('Ctrl Pts',(1.31377755676458,-1.50097185283753,1.62527012915796));
#78768=CARTESIAN_POINT('Ctrl Pts',(1.97340365459093,0.290870799196052,1.73647213010362));
#78769=CARTESIAN_POINT('Ctrl Pts',(0.824842384303165,1.81619451019926,1.84767413104928));
#78770=CARTESIAN_POINT('Ctrl Pts',(-1.07950414327688,1.67737846242548,1.95887613199493));
#78771=CARTESIAN_POINT('Ctrl Pts',(-1.9947243031253,0.0016165763711305,
2.07007813294059));
#78772=CARTESIAN_POINT('Ctrl Pts',(-1.08222153165756,-1.67562650144563,
2.18128013388624));
#78773=CARTESIAN_POINT('Ctrl Pts',(0.821897512499189,-1.81752912798159,
2.2924821348319));
#78774=CARTESIAN_POINT('Ctrl Pts',(1.97292957213719,-0.294068948937909,
2.40368413577756));
#78775=CARTESIAN_POINT('Ctrl Pts',(1.31620875576429,1.49884026820977,2.51488613672321));
#78776=CARTESIAN_POINT('Ctrl Pts',(-0.546525793791478,1.91839443293952,
2.62608813766886));
#78777=CARTESIAN_POINT('Ctrl Pts',(-1.90849053019933,0.580165095586069,
2.73729013861453));
#78778=CARTESIAN_POINT('Ctrl Pts',(-1.52174649867255,-1.2896570223301,2.84849213956018));
#78779=CARTESIAN_POINT('Ctrl Pts',(0.259341073944776,-1.97779418787179,
2.95969414050583));
#78780=CARTESIAN_POINT('Ctrl Pts',(1.8028000062981,-0.853721136687417,3.07089614145149));
#78781=CARTESIAN_POINT('Ctrl Pts',(1.69439212166436,1.05259820441132,3.18209814239715));
#78782=CARTESIAN_POINT('Ctrl Pts',(0.0334492299058641,1.99444448180705,
3.2933001433428));
#78783=CARTESIAN_POINT('Ctrl Pts',(-1.65814247079603,1.10882423696829,3.40450214428846));
#78784=CARTESIAN_POINT('Ctrl Pts',(-1.83041393868615,-0.792787774254176,
3.51570414523411));
#78785=CARTESIAN_POINT('Ctrl Pts',(-0.325516538141336,-1.96798542305425,
3.62690614617977));
#78786=CARTESIAN_POINT('Ctrl Pts',(1.47764465530687,-1.3399604153083,3.73810814712542));
#78787=CARTESIAN_POINT('Ctrl Pts',(1.92687187670742,0.5158414608235,3.84931014807109));
#78788=CARTESIAN_POINT('Ctrl Pts',(0.610547898578811,1.89898891663257,3.96051214901674));
#78789=CARTESIAN_POINT('Ctrl Pts',(-1.2652079689957,1.54213372868275,4.0717141499624));
#78790=CARTESIAN_POINT('Ctrl Pts',(-1.9816810247145,-0.227745380277678,
4.18291615090805));
#78791=CARTESIAN_POINT('Ctrl Pts',(-0.882382439067989,-1.78894630248535,
4.2941181518537));
#78792=CARTESIAN_POINT('Ctrl Pts',(1.02542417068364,-1.71097425817256,4.40532015279937));
#78793=CARTESIAN_POINT('Ctrl Pts',(1.99365669849328,-0.0652733521761122,
4.51652215374502));
#78794=CARTESIAN_POINT('Ctrl Pts',(1.13514453298693,1.64023612055744,4.62772415469067));
#78795=CARTESIAN_POINT('Ctrl Pts',(-0.763476119275289,1.84283256354119,
4.73892615563633));
#78796=CARTESIAN_POINT('Ctrl Pts',(-1.96254004724607,0.356881219605069,
4.85012815658198));
#78797=CARTESIAN_POINT('Ctrl Pts',(-1.36337079924614,-1.4560726993232,4.96133015752764));
#78798=CARTESIAN_POINT('Ctrl Pts',(0.485025747730156,-1.93485856485438,
5.0725321584733));
#78799=CARTESIAN_POINT('Ctrl Pts',(1.88900364857879,-0.640775200524594,
5.18373415941895));
#78800=CARTESIAN_POINT('Ctrl Pts',(1.56212819172362,1.24043667898587,5.29493616036461));
#78801=CARTESIAN_POINT('Ctrl Pts',(-0.196091681984855,1.98506314615144,
5.40613816131026));
#78802=CARTESIAN_POINT('Ctrl Pts',(-1.77463697092647,0.910819006922554,
5.51734016225592));
#78803=CARTESIAN_POINT('Ctrl Pts',(-1.72712062565998,-0.997988971066346,
5.62854216320158));
#78804=CARTESIAN_POINT('Ctrl Pts',(-0.0970808499422429,-1.99236114962424,
5.73974416414723));
#78805=CARTESIAN_POINT('Ctrl Pts',(1.62191201764294,-1.16117571838582,5.85094616509288));
#78806=CARTESIAN_POINT('Ctrl Pts',(1.8547818363144,0.73397001411775,5.96214816603855));
#78807=CARTESIAN_POINT('Ctrl Pts',(0.3881550067857,1.9565948310008,6.07335016698419));
#78808=CARTESIAN_POINT('Ctrl Pts',(-1.43412989534715,1.38643394547295,6.18455216792986));
#78809=CARTESIAN_POINT('Ctrl Pts',(-1.94235246276944,-0.45408650311232,
6.29575416887551));
#78810=CARTESIAN_POINT('Ctrl Pts',(-0.670839303058379,-1.87853726917684,
6.40695616982117));
#78811=CARTESIAN_POINT('Ctrl Pts',(1.21534946143024,-1.58172479530061,6.51815817076683));
#78812=CARTESIAN_POINT('Ctrl Pts',(1.9879396907512,0.164388040723421,6.62936017171248));
#78813=CARTESIAN_POINT('Ctrl Pts',(0.93902359769959,1.7598756565667,6.74056217265814));
#78814=CARTESIAN_POINT('Ctrl Pts',(-0.970299592946644,1.74282711084183,
6.85176417360379));
#78815=CARTESIAN_POINT('Ctrl Pts',(-1.99055816538004,0.128863623966512,
6.96296617454945));
#78816=CARTESIAN_POINT('Ctrl Pts',(-1.18691116284208,-1.60317483252287,
7.07416817549511));
#78817=CARTESIAN_POINT('Ctrl Pts',(0.704276972891066,-1.86625870698184,
7.18537017644076));
#78818=CARTESIAN_POINT('Ctrl Pts',(1.95015129006943,-0.419329947223466,
7.29657217738642));
#78819=CARTESIAN_POINT('Ctrl Pts',(1.40914397704898,1.41182185615162,7.40777417833207));
#78820=CARTESIAN_POINT('Ctrl Pts',(-0.423031601239362,1.9493516158389,7.51897617927772));
#78821=CARTESIAN_POINT('Ctrl Pts',(-1.86759245490351,0.700732636720482,
7.63017818022339));
#78822=CARTESIAN_POINT('Ctrl Pts',(-1.60091852779667,-1.18995287260722,
7.74138018116903));
#78823=CARTESIAN_POINT('Ctrl Pts',(0.13264249198098,-1.99030960821872,7.85258218211471));
#78824=CARTESIAN_POINT('Ctrl Pts',(1.74466619349733,-0.966989632940643,
7.96378418306033));
#78825=CARTESIAN_POINT('Ctrl Pts',(1.75808957149651,0.942364240721947,8.07498618400602));
#78826=CARTESIAN_POINT('Ctrl Pts',(0.16061384977306,1.98824601068674,8.18618818495165));
#78827=CARTESIAN_POINT('Ctrl Pts',(-1.58402985215346,1.21234849070882,8.29739018589733));
#78828=CARTESIAN_POINT('Ctrl Pts',(-1.87725927212678,-0.674412516764297,
8.40859218684298));
#78829=CARTESIAN_POINT('Ctrl Pts',(-0.45039996802915,-1.94319590860429,
8.51979418778862));
#78830=CARTESIAN_POINT('Ctrl Pts',(1.38915781916185,-1.43152397592121,8.63099618873429));
#78831=CARTESIAN_POINT('Ctrl Pts',(1.95584746960999,0.391923926276063,8.74219818967994));
#78832=CARTESIAN_POINT('Ctrl Pts',(0.730460484459456,1.85606729156128,8.8534001906256));
#78833=CARTESIAN_POINT('Ctrl Pts',(-1.16427793969766,1.61990393726448,8.96460219157125));
#78834=CARTESIAN_POINT('Ctrl Pts',(-1.99212554106622,-0.101243249088571,
9.07580419251692));
#78835=CARTESIAN_POINT('Ctrl Pts',(-0.994798877509525,-1.72828584672519,
9.18700619346256));
#78836=CARTESIAN_POINT('Ctrl Pts',(0.914357986078193,-1.77431103298107,
9.29820819440823));
#78837=CARTESIAN_POINT('Ctrl Pts',(1.98523085471874,-0.189274965615466,
9.40942210154506));
#78838=CARTESIAN_POINT('Ctrl Pts',(1.48692185005784,0.975485300275654,9.48356867503336));
#78839=CARTESIAN_POINT('Ctrl Pts',(1.04634567127244,1.32372349336162,9.5206479148731));
#78840=CARTESIAN_POINT('Ctrl Pts',(-0.80306055761689,1.63540452023967,-0.0762628717538682));
#78841=CARTESIAN_POINT('Ctrl Pts',(-1.34726901294161,1.36818030233479,-0.0391901288006135));
#78842=CARTESIAN_POINT('Ctrl Pts',(-2.1384167317464,0.252440618424864,0.0349499478011931));
#78843=CARTESIAN_POINT('Ctrl Pts',(-1.36933849768983,-1.66438634962091,
0.146157358051552));
#78844=CARTESIAN_POINT('Ctrl Pts',(0.656191171511376,-2.05080060162047,
0.257359358997207));
#78845=CARTESIAN_POINT('Ctrl Pts',(2.0795455823562,-0.56075453979159,0.368561359942864));
#78846=CARTESIAN_POINT('Ctrl Pts',(1.59793867624458,1.4444724393234,0.479763360888519));
#78847=CARTESIAN_POINT('Ctrl Pts',(-0.348077588388865,2.12544088023263,
0.590965361834176));
#78848=CARTESIAN_POINT('Ctrl Pts',(-1.97502526874602,0.859291247817001,
0.702167362779829));
#78849=CARTESIAN_POINT('Ctrl Pts',(-1.79236944896554,-1.19440670987473,
0.813369363725489));
#78850=CARTESIAN_POINT('Ctrl Pts',(0.0326324460558829,-2.15359142327166,
0.924571364671141));
#78851=CARTESIAN_POINT('Ctrl Pts',(1.8277147401737,-1.13954136104124,1.03577336561681));
#78852=CARTESIAN_POINT('Ctrl Pts',(1.94811146141648,0.918674608393528,1.14697536656246));
#78853=CARTESIAN_POINT('Ctrl Pts',(0.283490317298041,2.13511374996301,1.25817736750812));
#78854=CARTESIAN_POINT('Ctrl Pts',(-1.64088412008999,1.39520206199323,1.36937936845377));
#78855=CARTESIAN_POINT('Ctrl Pts',(-2.06175323872349,-0.62310738056412,
1.48058136939943));
#78856=CARTESIAN_POINT('Ctrl Pts',(-0.593481504796934,-2.07047476905335,
1.59178337034508));
#78857=CARTESIAN_POINT('Ctrl Pts',(1.4185841472658,-1.62071186630041,1.70298537129074));
#78858=CARTESIAN_POINT('Ctrl Pts',(2.13083190997207,0.314075014082447,1.81418737223639));
#78859=CARTESIAN_POINT('Ctrl Pts',(0.890644176664907,1.96108140777255,1.92538937318205));
#78860=CARTESIAN_POINT('Ctrl Pts',(-1.16562157472959,1.81119131127637,2.03659137412771));
#78861=CARTESIAN_POINT('Ctrl Pts',(-2.15385341301462,0.0017455387338156,
2.14779337507336));
#78862=CARTESIAN_POINT('Ctrl Pts',(-1.16855574273922,-1.80929958762813,
2.25899537601902));
#78863=CARTESIAN_POINT('Ctrl Pts',(0.887464377744325,-1.96252249467416,
2.37019737696467));
#78864=CARTESIAN_POINT('Ctrl Pts',(2.13032000759568,-0.31752829618569,2.48139937791033));
#78865=CARTESIAN_POINT('Ctrl Pts',(1.42120929513966,1.61841023453182,2.59260137885599));
#78866=CARTESIAN_POINT('Ctrl Pts',(-0.590124883129942,2.07143432825337,
2.70380337980164));
#78867=CARTESIAN_POINT('Ctrl Pts',(-2.06074034177829,0.626447759864455,
2.8150053807473));
#78868=CARTESIAN_POINT('Ctrl Pts',(-1.64314380928414,-1.39253939745549,
2.92620738169295));
#78869=CARTESIAN_POINT('Ctrl Pts',(0.280030005337393,-2.13557269799833,
3.03740938263861));
#78870=CARTESIAN_POINT('Ctrl Pts',(1.94661835746632,-0.921826731210898,
3.14861138358427));
#78871=CARTESIAN_POINT('Ctrl Pts',(1.82956223499856,1.13656921487958,3.25981338452992));
#78872=CARTESIAN_POINT('Ctrl Pts',(0.0361176418628893,2.1535512689537,3.37101538547558));
#78873=CARTESIAN_POINT('Ctrl Pts',(-1.79042076862095,1.19728067858081,3.48221738642123));
#78874=CARTESIAN_POINT('Ctrl Pts',(-1.97643519101449,-0.856032410443005,
3.59341938736689));
#78875=CARTESIAN_POINT('Ctrl Pts',(-0.351484616480558,-2.12498143907265,
3.70462138831255));
#78876=CARTESIAN_POINT('Ctrl Pts',(1.59552374183691,-1.44685574306907,3.8158233892582));
#78877=CARTESIAN_POINT('Ctrl Pts',(2.08058806000694,0.556992707828519,3.92702539020386));
#78878=CARTESIAN_POINT('Ctrl Pts',(0.659254350640102,2.05048073709114,4.03822739114951));
#78879=CARTESIAN_POINT('Ctrl Pts',(-1.36613992115355,1.66515743034975,4.14942939209517));
#78880=CARTESIAN_POINT('Ctrl Pts',(-2.13976960720848,-0.245913765546851,
4.26063139304082));
#78881=CARTESIAN_POINT('Ctrl Pts',(-0.952774488681501,-1.93165947458048,
4.37183339398649));
#78882=CARTESIAN_POINT('Ctrl Pts',(1.10722737290271,-1.84746721126887,4.48303539493214));
#78883=CARTESIAN_POINT('Ctrl Pts',(2.15270064023453,-0.0704805331459489,
4.59423739587779));
#78884=CARTESIAN_POINT('Ctrl Pts',(1.22570067593207,1.77108593948412,4.70543939682345));
#78885=CARTESIAN_POINT('Ctrl Pts',(-0.824382418502531,1.98984451153416,
4.8166413977691));
#78886=CARTESIAN_POINT('Ctrl Pts',(-2.11910165846778,0.385351415071689,
4.92784339871477));
#78887=CARTESIAN_POINT('Ctrl Pts',(-1.47213369013448,-1.57223088329599,
5.0390453996604));
#78888=CARTESIAN_POINT('Ctrl Pts',(0.523718671553637,-2.08921188611517,
5.15024740060608));
#78889=CARTESIAN_POINT('Ctrl Pts',(2.03969889438546,-0.691893035274437,
5.26144940155171));
#78890=CARTESIAN_POINT('Ctrl Pts',(1.68674695146527,1.33939250174884,5.37265140249739));
#78891=CARTESIAN_POINT('Ctrl Pts',(-0.21173489381219,2.14342153734678,5.48385340344304));
#78892=CARTESIAN_POINT('Ctrl Pts',(-1.91620861624996,0.983479583431696,
5.5950554043887));
#78893=CARTESIAN_POINT('Ctrl Pts',(-1.86490165504943,-1.07760353053018,
5.70625740533434));
#78894=CARTESIAN_POINT('Ctrl Pts',(-0.104825473705251,-2.15130173896834,
5.81745940628001));
#78895=CARTESIAN_POINT('Ctrl Pts',(1.75130003145614,-1.25380849886698,5.92866140722567));
#78896=CARTESIAN_POINT('Ctrl Pts',(2.0027470374147,0.792522464122489,6.03986340817132));
#78897=CARTESIAN_POINT('Ctrl Pts',(0.419120068289257,2.11268216266031,6.15106540911698));
#78898=CARTESIAN_POINT('Ctrl Pts',(-1.54853759236808,1.4970366986042,6.26226741006263));
#78899=CARTESIAN_POINT('Ctrl Pts',(-2.09730360965604,-0.490311249028223,
6.37346941100829));
#78900=CARTESIAN_POINT('Ctrl Pts',(-0.724355501265427,-2.02839755967897,
6.48467141195395));
#78901=CARTESIAN_POINT('Ctrl Pts',(1.31230395168176,-1.70790687388245,6.59587341289959));
#78902=CARTESIAN_POINT('Ctrl Pts',(2.14652755826115,0.177502094909133,6.70707541384526));
#78903=CARTESIAN_POINT('Ctrl Pts',(1.01393419513548,1.90026971819544,6.81827741479091));
#78904=CARTESIAN_POINT('Ctrl Pts',(-1.04770523256793,1.88186112491823,6.92947941573657));
#78905=CARTESIAN_POINT('Ctrl Pts',(-2.14935492167541,0.139143718186449,
7.04068141668223));
#78906=CARTESIAN_POINT('Ctrl Pts',(-1.28159698812875,-1.73106808759405,
7.15188341762787));
#78907=CARTESIAN_POINT('Ctrl Pts',(0.76046066085039,-2.01513947531656,7.26308541857355));
#78908=CARTESIAN_POINT('Ctrl Pts',(2.10572458832024,-0.452781989266107,
7.37428741951918));
#78909=CARTESIAN_POINT('Ctrl Pts',(1.52155842270565,1.52444992958496,7.48548942046485));
#78910=CARTESIAN_POINT('Ctrl Pts',(-0.456778942691401,2.10486112008655,
7.59669142141051));
#78911=CARTESIAN_POINT('Ctrl Pts',(-2.01657962296436,0.756633575299834,
7.70789342235615));
#78912=CARTESIAN_POINT('Ctrl Pts',(-1.72863178618255,-1.28488135025776,
7.81909542330182));
#78913=CARTESIAN_POINT('Ctrl Pts',(0.14322404535622,-2.14908653586922,7.93029742424747));
#78914=CARTESIAN_POINT('Ctrl Pts',(1.88384692037282,-1.04413122053797,8.04149942519313));
#78915=CARTESIAN_POINT('Ctrl Pts',(1.89834114820795,1.0175413379191,8.15270142613878));
#78916=CARTESIAN_POINT('Ctrl Pts',(0.173426817916207,2.14685831486625,8.26390342708444));
#78917=CARTESIAN_POINT('Ctrl Pts',(-1.710395816621,1.30906357855325,8.3751054280301));
#78918=CARTESIAN_POINT('Ctrl Pts',(-2.02701761042795,-0.728213768056391,
8.48630742897575));
#78919=CARTESIAN_POINT('Ctrl Pts',(-0.486330620648357,-2.0982143413733,
8.59750942992142));
#78920=CARTESIAN_POINT('Ctrl Pts',(1.4999778692874,-1.54572378574789,8.70871143086706));
#78921=CARTESIAN_POINT('Ctrl Pts',(2.11187518052256,0.423189653291518,8.81991343181272));
#78922=CARTESIAN_POINT('Ctrl Pts',(0.788732961773369,2.00413503984011,8.93111543275837));
#78923=CARTESIAN_POINT('Ctrl Pts',(-1.25715819985068,1.74913175648703,9.04231743370403));
#78924=CARTESIAN_POINT('Ctrl Pts',(-2.15104733474015,-0.109319928198811,
9.15351943464968));
#78925=CARTESIAN_POINT('Ctrl Pts',(-1.0741589472941,-1.86615983161261,9.26472143559535));
#78926=CARTESIAN_POINT('Ctrl Pts',(0.987300884611498,-1.91585667660846,
9.37592343654099));
#78927=CARTESIAN_POINT('Ctrl Pts',(2.14360262486323,-0.204374373967568,
9.48713734367785));
#78928=CARTESIAN_POINT('Ctrl Pts',(1.60554102469966,1.0533046296435,9.56128391716614));
#78929=CARTESIAN_POINT('Ctrl Pts',(1.12981788597663,1.42932352084821,9.59836315700588));
#78930=CARTESIAN_POINT('Ctrl Pts',(-0.862391573807965,1.75623004348198,
0.00145237037890559));
#78931=CARTESIAN_POINT('Ctrl Pts',(-1.44680676120033,1.46926300014658,0.0385251133321603));
#78932=CARTESIAN_POINT('Ctrl Pts',(-2.29640536228136,0.271091214917251,
0.112665189933967));
#78933=CARTESIAN_POINT('Ctrl Pts',(-1.47050676427563,-1.78735308297738,
0.223872600184326));
#78934=CARTESIAN_POINT('Ctrl Pts',(0.704671312457304,-2.20231605402983,
0.335074601129981));
#78935=CARTESIAN_POINT('Ctrl Pts',(2.23318474623571,-0.602183715168276,
0.446276602075638));
#78936=CARTESIAN_POINT('Ctrl Pts',(1.71599618084173,1.55119168592591,0.557478603021293));
#78937=CARTESIAN_POINT('Ctrl Pts',(-0.373793951665039,2.2824708402801,0.66868060396695));
#78938=CARTESIAN_POINT('Ctrl Pts',(-2.12094235443319,0.922776650572171,
0.779882604912605));
#78939=CARTESIAN_POINT('Ctrl Pts',(-1.92479171748357,-1.28265081945048,
0.891084605858262));
#78940=CARTESIAN_POINT('Ctrl Pts',(0.0350433678312346,-2.31270117706443,
1.00228660680391));
#78941=CARTESIAN_POINT('Ctrl Pts',(1.96274835851467,-1.22373195700699,1.11348860774957));
#78942=CARTESIAN_POINT('Ctrl Pts',(2.09204012478197,0.986547320542003,1.22469060869523));
#78943=CARTESIAN_POINT('Ctrl Pts',(0.304434900425805,2.29285835249309,1.33589260964088));
#78944=CARTESIAN_POINT('Ctrl Pts',(-1.76211448232525,1.49828115776604,1.44709461058654));
#78945=CARTESIAN_POINT('Ctrl Pts',(-2.2140778842667,-0.669143253867042,
1.55829661153219));
#78946=CARTESIAN_POINT('Ctrl Pts',(-0.637328585115159,-2.22344377105548,
1.66949861247785));
#78947=CARTESIAN_POINT('Ctrl Pts',(1.52339073776703,-1.7404518797633,1.7807006134235));
#78948=CARTESIAN_POINT('Ctrl Pts',(2.28826016535321,0.337279228968842,1.89190261436916));
#78949=CARTESIAN_POINT('Ctrl Pts',(0.956445969026647,2.10596830534583,2.00310461531481));
#78950=CARTESIAN_POINT('Ctrl Pts',(-1.2517390061823,1.94500416012725,2.11430661626047));
#78951=CARTESIAN_POINT('Ctrl Pts',(-2.31298252290394,0.00187450109649862,
2.22550861720613));
#78952=CARTESIAN_POINT('Ctrl Pts',(-1.25488995382088,-1.94297267381061,
2.33671061815178));
#78953=CARTESIAN_POINT('Ctrl Pts',(0.95303124298946,-2.10751586136672,2.44791261909744));
#78954=CARTESIAN_POINT('Ctrl Pts',(2.28771044305415,-0.340987643433472,
2.55911462004309));
#78955=CARTESIAN_POINT('Ctrl Pts',(1.52620983451504,1.73798020085387,2.67031662098875));
#78956=CARTESIAN_POINT('Ctrl Pts',(-0.633723972468404,2.22447422356722,
2.78151862193441));
#78957=CARTESIAN_POINT('Ctrl Pts',(-2.21299015335724,0.672730424142846,
2.89272062288006));
#78958=CARTESIAN_POINT('Ctrl Pts',(-1.76454111989571,-1.49542177258089,
3.00392262382573));
#78959=CARTESIAN_POINT('Ctrl Pts',(0.300718936730009,-2.29335120812486,
3.11512462477137));
#78960=CARTESIAN_POINT('Ctrl Pts',(2.09043670863454,-0.989932325734382,
3.22632662571703));
#78961=CARTESIAN_POINT('Ctrl Pts',(1.96473234833276,1.22054022534784,3.33752862666269));
#78962=CARTESIAN_POINT('Ctrl Pts',(0.0387860538199159,2.31265805610036,
3.44873062760834));
#78963=CARTESIAN_POINT('Ctrl Pts',(-1.92269906644588,1.28573712019333,3.559932628554));
#78964=CARTESIAN_POINT('Ctrl Pts',(-2.12245644334284,-0.919277046631835,
3.67113462949965));
#78965=CARTESIAN_POINT('Ctrl Pts',(-0.377452694819782,-2.28197745509106,
3.78233663044531));
#78966=CARTESIAN_POINT('Ctrl Pts',(1.71340282836695,-1.55375107082984,3.89353863139097));
#78967=CARTESIAN_POINT('Ctrl Pts',(2.23430424330645,0.598143954833538,4.00474063233662));
#78968=CARTESIAN_POINT('Ctrl Pts',(0.707960802701394,2.20197255754971,4.11594263328228));
#78969=CARTESIAN_POINT('Ctrl Pts',(-1.46707187331139,1.78818113201674,4.22714463422794));
#78970=CARTESIAN_POINT('Ctrl Pts',(-2.29785818970246,-0.264082150816026,
4.33834663517359));
#78971=CARTESIAN_POINT('Ctrl Pts',(-1.02316653829502,-2.07437264667561,
4.44954863611926));
#78972=CARTESIAN_POINT('Ctrl Pts',(1.18903057512178,-1.98396016436518,4.5607506370649));
#78973=CARTESIAN_POINT('Ctrl Pts',(2.31174458197577,-0.0756877141157843,
4.67195263801057));
#78974=CARTESIAN_POINT('Ctrl Pts',(1.3162568188772,1.90193575841081,4.78315463895623));
#78975=CARTESIAN_POINT('Ctrl Pts',(-0.885288717729772,2.13685645952712,
4.89435663990187));
#78976=CARTESIAN_POINT('Ctrl Pts',(-2.2756632696895,0.413821610538309,5.00555864084753));
#78977=CARTESIAN_POINT('Ctrl Pts',(-1.58089658102282,-1.68838906726877,
5.1167606417932));
#78978=CARTESIAN_POINT('Ctrl Pts',(0.562411595377116,-2.24356520737596,
5.22796264273883));
#78979=CARTESIAN_POINT('Ctrl Pts',(2.19039414019213,-0.743010870024276,
5.3391646436845));
#78980=CARTESIAN_POINT('Ctrl Pts',(1.81136571120691,1.43834832451181,5.45036664463017));
#78981=CARTESIAN_POINT('Ctrl Pts',(-0.227378105639523,2.30177992854213,
5.56156864557579));
#78982=CARTESIAN_POINT('Ctrl Pts',(-2.05778026157344,1.05614015994084,5.67277064652148));
#78983=CARTESIAN_POINT('Ctrl Pts',(-2.00268268443888,-1.15721808999401,
5.78397264746711));
#78984=CARTESIAN_POINT('Ctrl Pts',(-0.11257009746826,-2.31024232831246,
5.89517464841279));
#78985=CARTESIAN_POINT('Ctrl Pts',(1.88068804526933,-1.34644127934815,6.00637664935843));
#78986=CARTESIAN_POINT('Ctrl Pts',(2.15071223851501,0.851074914127227,6.11757865030409));
#78987=CARTESIAN_POINT('Ctrl Pts',(0.450085129792815,2.26876949431981,6.22878065124975));
#78988=CARTESIAN_POINT('Ctrl Pts',(-1.662945289389,1.60763945173544,6.33998265219541));
#78989=CARTESIAN_POINT('Ctrl Pts',(-2.25225475654263,-0.526535994944125,
6.45118465314106));
#78990=CARTESIAN_POINT('Ctrl Pts',(-0.777871699472479,-2.1782578501811,
6.56238665408672));
#78991=CARTESIAN_POINT('Ctrl Pts',(1.40925844193328,-1.83408895246428,6.67358865503238));
#78992=CARTESIAN_POINT('Ctrl Pts',(2.30511542577108,0.190616149094843,6.78479065597802));
#78993=CARTESIAN_POINT('Ctrl Pts',(1.08884479257138,2.04066377982418,6.89599265692368));
#78994=CARTESIAN_POINT('Ctrl Pts',(-1.12511087218922,2.02089513899462,7.00719465786934));
#78995=CARTESIAN_POINT('Ctrl Pts',(-2.30815167797076,0.149423812406389,
7.118396658815));
#78996=CARTESIAN_POINT('Ctrl Pts',(-1.37628281341541,-1.85896134266524,
7.22959865976065));
#78997=CARTESIAN_POINT('Ctrl Pts',(0.816644348809715,-2.16402024365127,
7.34080066070631));
#78998=CARTESIAN_POINT('Ctrl Pts',(2.26129788657104,-0.486234031308752,
7.45200266165195));
#78999=CARTESIAN_POINT('Ctrl Pts',(1.63397286836232,1.63707800301831,7.56320466259762));
#79000=CARTESIAN_POINT('Ctrl Pts',(-0.490526284143436,2.2603706243342,7.67440666354327));
#79001=CARTESIAN_POINT('Ctrl Pts',(-2.16556679102521,0.812534513879188,
7.78560866448893));
#79002=CARTESIAN_POINT('Ctrl Pts',(-1.85634504456841,-1.37980982790828,
7.8968106654346));
#79003=CARTESIAN_POINT('Ctrl Pts',(0.153805598731459,-2.3078634635197,8.00801266638024));
#79004=CARTESIAN_POINT('Ctrl Pts',(2.02302764724831,-1.1212728081353,8.11921466732591));
#79005=CARTESIAN_POINT('Ctrl Pts',(2.03859272491938,1.09271843511626,8.23041666827155));
#79006=CARTESIAN_POINT('Ctrl Pts',(0.186239786059356,2.30547061904575,8.34161866921722));
#79007=CARTESIAN_POINT('Ctrl Pts',(-1.83676178108854,1.40577866639767,8.45282067016287));
#79008=CARTESIAN_POINT('Ctrl Pts',(-2.17677594872913,-0.782015019348484,
8.56402267110853));
#79009=CARTESIAN_POINT('Ctrl Pts',(-0.522261273267561,-2.25323277414232,
8.67522467205418));
#79010=CARTESIAN_POINT('Ctrl Pts',(1.61079791941295,-1.65992359557459,8.78642667299984));
#79011=CARTESIAN_POINT('Ctrl Pts',(2.26790289143513,0.454455380306972,8.8976286739455));
#79012=CARTESIAN_POINT('Ctrl Pts',(0.847005439087281,2.15220278811892,9.00883067489114));
#79013=CARTESIAN_POINT('Ctrl Pts',(-1.3500384600037,1.87835957570958,9.12003267583681));
#79014=CARTESIAN_POINT('Ctrl Pts',(-2.30996912841407,-0.117396607309049,
9.23123467678246));
#79015=CARTESIAN_POINT('Ctrl Pts',(-1.15351901707866,-2.00403381650003,
9.34243667772811));
#79016=CARTESIAN_POINT('Ctrl Pts',(1.0602437831448,-2.05740232023586,9.45363867867378));
#79017=CARTESIAN_POINT('Ctrl Pts',(2.30197439500773,-0.219473782319668,
9.56485258581061));
#79018=CARTESIAN_POINT('Ctrl Pts',(1.72416019934148,1.13112395901135,9.63899915929891));
#79019=CARTESIAN_POINT('Ctrl Pts',(1.21329010068083,1.53492354833479,9.67607839913864));
#79020=CARTESIAN_POINT('',(-0.904509582502828,-1.26706033424728,-0.000727943534944579));
#79021=CARTESIAN_POINT('Ctrl Pts',(-0.905550660636154,-1.26792405592273,
3.33717428691038E-16));
#79022=CARTESIAN_POINT('Ctrl Pts',(-0.937331646933895,-1.25093119319315,
-1.91748806585551E-15));
#79023=CARTESIAN_POINT('Ctrl Pts',(-0.968423391396879,-1.23278887404085,
-3.93171517975868E-15));
#79024=CARTESIAN_POINT('Ctrl Pts',(-0.998756220109606,-1.21351103938414,
-3.10862446895044E-15));
#79025=CARTESIAN_POINT('Ctrl Pts',(-1.0491021278163,-1.18151402078745,-1.75196333938182E-15));
#79026=CARTESIAN_POINT('Ctrl Pts',(-1.09735862263973,-1.14639180321778,
-1.66246197192591E-15));
#79027=CARTESIAN_POINT('Ctrl Pts',(-1.14344573691603,-1.10847083762139,
-1.88390969491081E-15));
#79028=CARTESIAN_POINT('Ctrl Pts',(-1.16929613914609,-1.08720085296273,
-2.0081203946255E-15));
#79029=CARTESIAN_POINT('Ctrl Pts',(-1.19446376238245,-1.06504939091104,
-9.9374122142534E-16));
#79030=CARTESIAN_POINT('Ctrl Pts',(-1.21893184621839,-1.04206746474762,
-1.99493199737333E-15));
#79031=CARTESIAN_POINT('Ctrl Pts',(-1.23255995383574,-1.02926710959479,
-2.49718249979953E-15));
#79032=CARTESIAN_POINT('Ctrl Pts',(-1.24597488110422,-1.01620487704946,
4.81999660303363E-16));
#79033=CARTESIAN_POINT('Ctrl Pts',(-1.25915060380592,-1.0029128321029,5.62050406216485E-16));
#79034=CARTESIAN_POINT('Ctrl Pts',(-1.30279148681256,-0.958886664311984,
4.90052638460193E-16));
#79035=CARTESIAN_POINT('Ctrl Pts',(-1.34385262686326,-0.912305708298536,
-1.22866962404621E-15));
#79036=CARTESIAN_POINT('Ctrl Pts',(-1.3822468326494,-0.863513449211606,
6.59194920871187E-16));
#79037=CARTESIAN_POINT('Ctrl Pts',(-1.40779034735979,-0.831052150371822,
1.91518380739542E-15));
#79038=CARTESIAN_POINT('Ctrl Pts',(-1.4321530736785,-0.797610973924513,
1.23008985062119E-15));
#79039=CARTESIAN_POINT('Ctrl Pts',(-1.45530339706809,-0.763280061968941,
7.14706072102445E-16));
#79040=CARTESIAN_POINT('Ctrl Pts',(-1.46804523103353,-0.74438448229783,
4.31041156332024E-16));
#79041=CARTESIAN_POINT('Ctrl Pts',(-1.48041969259617,-0.725219227959009,
1.33627721405136E-16));
#79042=CARTESIAN_POINT('Ctrl Pts',(-1.49242075014977,-0.705798385792698,
6.73072708679001E-16));
#79043=CARTESIAN_POINT('Ctrl Pts',(-1.50150857656975,-0.691091911654995,
1.08156857544523E-15));
#79044=CARTESIAN_POINT('Ctrl Pts',(-1.51038448432321,-0.676234681791649,
1.10657574010046E-15));
#79045=CARTESIAN_POINT('Ctrl Pts',(-1.51903027706774,-0.661260208511432,
1.11022302462516E-15));
#79046=CARTESIAN_POINT('Ctrl Pts',(-1.55206526232624,-0.60404376593845,
1.12415905039712E-15));
#79047=CARTESIAN_POINT('Ctrl Pts',(-1.58178299126492,-0.545059351017348,
2.78962851734901E-16));
#79048=CARTESIAN_POINT('Ctrl Pts',(-1.60808638764007,-0.484680550384653,
1.16573417585641E-15));
#79049=CARTESIAN_POINT('Ctrl Pts',(-1.63436099254972,-0.424367839854187,
2.05153484791377E-15));
#79050=CARTESIAN_POINT('Ctrl Pts',(-1.65722893541898,-0.362663618825764,
1.62943944703187E-15));
#79051=CARTESIAN_POINT('Ctrl Pts',(-1.67655774217872,-0.29990105864075,
2.37310171513627E-15));
#79052=CARTESIAN_POINT('Ctrl Pts',(-1.68825939151139,-0.261904638083861,
2.82331445674351E-15));
#79053=CARTESIAN_POINT('Ctrl Pts',(-1.6986632113407,-0.22351958384957,1.0977060151425E-15));
#79054=CARTESIAN_POINT('Ctrl Pts',(-1.70773212765127,-0.184814675751519,
1.67921232474555E-15));
#79055=CARTESIAN_POINT('Ctrl Pts',(-1.71421027330989,-0.157166826353006,
2.09459630735212E-15));
#79056=CARTESIAN_POINT('Ctrl Pts',(-1.72000709785751,-0.129355980394314,
2.03148131458715E-15));
#79057=CARTESIAN_POINT('Ctrl Pts',(-1.72510714810462,-0.10140553099961,
1.41553435639707E-15));
#79058=CARTESIAN_POINT('Ctrl Pts',(-1.72714678432153,-0.0902274550783656,
1.16920193558766E-15));
#79059=CARTESIAN_POINT('Ctrl Pts',(-1.72907514617003,-0.0790258298363134,
8.63363090934406E-16));
#79060=CARTESIAN_POINT('Ctrl Pts',(-1.73089043201219,-0.0678066984905213,
9.99200722162641E-16));
#79061=CARTESIAN_POINT('Ctrl Pts',(-1.74172160283504,-0.000866095931864194,
1.93493306363864E-15));
#79062=CARTESIAN_POINT('Ctrl Pts',(-1.748486900033,0.0664195158076903,2.98350052951504E-15));
#79063=CARTESIAN_POINT('Ctrl Pts',(-1.75106690168969,0.1336922072272,1.33226762955019E-15));
#79064=CARTESIAN_POINT('Ctrl Pts',(-1.75197579459359,0.157391289628444,
9.56040573665211E-16));
#79065=CARTESIAN_POINT('Ctrl Pts',(-1.7523649021625,0.181089059905602,2.7599826661696E-15));
#79066=CARTESIAN_POINT('Ctrl Pts',(-1.75222770108741,0.204770690960272,
2.17881268582687E-15));
#79067=CARTESIAN_POINT('Ctrl Pts',(-1.75184793058349,0.270321088092813,
4.77379898077456E-16));
#79068=CARTESIAN_POINT('Ctrl Pts',(-1.74743979276228,0.335747132875219,
1.54789476185541E-15));
#79069=CARTESIAN_POINT('Ctrl Pts',(-1.73922727433975,0.400805521086702,
1.60982338570648E-15));
#79070=CARTESIAN_POINT('Ctrl Pts',(-1.73101475591721,0.465863909298186,
1.67175200955754E-15));
#79071=CARTESIAN_POINT('Ctrl Pts',(-1.71899757684948,0.530555453607267,
3.18517571214417E-15));
#79072=CARTESIAN_POINT('Ctrl Pts',(-1.70334767938921,0.594640505552196,
9.15933995315754E-16));
#79073=CARTESIAN_POINT('Ctrl Pts',(-1.70064831213801,0.605694193983742,
3.51217563452488E-16));
#79074=CARTESIAN_POINT('Ctrl Pts',(-1.69784071539616,0.616729589129694,
2.72828645400985E-15));
#79075=CARTESIAN_POINT('Ctrl Pts',(-1.69492950185833,0.627731892802464,
2.38697950294409E-15));
#79076=CARTESIAN_POINT('Ctrl Pts',(-1.67764017062698,0.693073191211115,
2.64844180626529E-16));
#79077=CARTESIAN_POINT('Ctrl Pts',(-1.65667167698021,0.757368056664447,
3.89680800276467E-16));
#79078=CARTESIAN_POINT('Ctrl Pts',(-1.632278840768,0.820363247272086,-1.11022302462516E-16));
#79079=CARTESIAN_POINT('Ctrl Pts',(-1.60714941139895,0.885260710576183,
-6.26845191842105E-16));
#79080=CARTESIAN_POINT('Ctrl Pts',(-1.578385616419,0.948779708185034,2.13504031261271E-15));
#79081=CARTESIAN_POINT('Ctrl Pts',(-1.54620991004292,1.01064658923624,1.85962356624714E-15));
#79082=CARTESIAN_POINT('Ctrl Pts',(-1.51403420366684,1.07251347028744,1.58420681988156E-15));
#79083=CARTESIAN_POINT('Ctrl Pts',(-1.47844619815798,1.13272920500638,2.35794009978941E-15));
#79084=CARTESIAN_POINT('Ctrl Pts',(-1.43961707028964,1.19100921034501,2.41473507855972E-15));
#79085=CARTESIAN_POINT('Ctrl Pts',(-1.42987064738873,1.20563795968555,2.47976585367877E-15));
#79086=CARTESIAN_POINT('Ctrl Pts',(-1.41991978147756,1.22014465371079,1.22964269444539E-15));
#79087=CARTESIAN_POINT('Ctrl Pts',(-1.40976671738967,1.23452457045435,1.22124532708767E-15));
#79088=CARTESIAN_POINT('Ctrl Pts',(-1.40016197586479,1.24812789081909,1.2626273074017E-15));
#79089=CARTESIAN_POINT('Ctrl Pts',(-1.39037610631028,1.2616175763207,1.15601544640403E-15));
#79090=CARTESIAN_POINT('Ctrl Pts',(-1.38042895433654,1.27496651867268,7.49400541621981E-16));
#79091=CARTESIAN_POINT('Ctrl Pts',(-1.33728364574509,1.33286693465769,-1.01427267771033E-15));
#79092=CARTESIAN_POINT('Ctrl Pts',(-1.29103059232721,1.38823206717148,-5.46656303023409E-16));
#79093=CARTESIAN_POINT('Ctrl Pts',(-1.24190881939456,1.44078043502317,-4.44089209850063E-16));
#79094=CARTESIAN_POINT('Ctrl Pts',(-1.19270542345375,1.49341611967151,-3.41351686454363E-16));
#79095=CARTESIAN_POINT('Ctrl Pts',(-1.14062332922914,1.54322667971843,1.00148334219595E-15));
#79096=CARTESIAN_POINT('Ctrl Pts',(-1.08585348598407,1.58991235213884,8.32667268468867E-17));
#79097=CARTESIAN_POINT('Ctrl Pts',(-1.03227982431091,1.63557840248782,-8.14895900226442E-16));
#79098=CARTESIAN_POINT('Ctrl Pts',(-0.97613396306252,1.67825542174933,-1.71497774819462E-15));
#79099=CARTESIAN_POINT('Ctrl Pts',(-0.917555232362004,1.7176331456658,-1.99840144432528E-15));
#79100=CARTESIAN_POINT('Ctrl Pts',(-0.899118809741871,1.73002645551156,
-2.08760308765107E-15));
#79101=CARTESIAN_POINT('Ctrl Pts',(-0.880441136441611,1.74209268004149,
-1.43728562686843E-15));
#79102=CARTESIAN_POINT('Ctrl Pts',(-0.861525859670561,1.75382131162753,
1.94289029309402E-16));
#79103=CARTESIAN_POINT('Ctrl Pts',(-0.903762994389396,-1.26601449437687,
-0.000727943534944708));
#79104=CARTESIAN_POINT('Ctrl Pts',(-0.898466996491729,-1.26979512006444,
-0.000485295689962951));
#79105=CARTESIAN_POINT('Ctrl Pts',(-0.893147275587681,-1.27354251394864,
-0.000242647844981202));
#79106=CARTESIAN_POINT('Ctrl Pts',(-0.887804250576279,-1.27725638094264,
5.55111512312578E-16));
#79107=CARTESIAN_POINT('Origin',(-0.866025403784439,-1.5,-4.));
#79108=CARTESIAN_POINT('',(-0.866025403784439,-1.5,-4.));
#79109=CARTESIAN_POINT('',(0.866025403784439,-1.5,-4.));
#79110=CARTESIAN_POINT('',(-0.43301270189222,-1.5,-4.));
#79111=CARTESIAN_POINT('',(-0.866025403784439,-1.5,-2.));
#79112=CARTESIAN_POINT('',(-0.866025403784439,-1.5,-4.));
#79113=CARTESIAN_POINT('',(0.866025403784439,-1.5,-2.));
#79114=CARTESIAN_POINT('',(-0.866025403784439,-1.5,-2.));
#79115=CARTESIAN_POINT('',(0.866025403784439,-1.5,-4.));
#79116=CARTESIAN_POINT('Origin',(-1.73205080756888,2.12115047744981E-16,
-4.));
#79117=CARTESIAN_POINT('',(-1.73205080756888,2.12115047744981E-16,-4.));
#79118=CARTESIAN_POINT('',(-1.51554445662277,-0.375,-4.));
#79119=CARTESIAN_POINT('',(-1.73205080756888,2.77555756156289E-16,-2.));
#79120=CARTESIAN_POINT('',(-1.73205080756888,2.12115047744981E-16,-4.));
#79121=CARTESIAN_POINT('',(-1.73205080756888,2.12115047744981E-16,-2.));
#79122=CARTESIAN_POINT('Origin',(-0.866025403784438,1.5,-4.));
#79123=CARTESIAN_POINT('',(-0.866025403784438,1.5,-4.));
#79124=CARTESIAN_POINT('',(-1.08253175473055,1.125,-4.));
#79125=CARTESIAN_POINT('',(-0.866025403784438,1.5,-2.));
#79126=CARTESIAN_POINT('',(-0.866025403784438,1.5,-4.));
#79127=CARTESIAN_POINT('',(-0.866025403784438,1.5,-2.));
#79128=CARTESIAN_POINT('Origin',(0.866025403784439,1.5,-4.));
#79129=CARTESIAN_POINT('',(0.866025403784439,1.5,-4.));
#79130=CARTESIAN_POINT('',(0.43301270189222,1.5,-4.));
#79131=CARTESIAN_POINT('',(0.866025403784439,1.5,-2.));
#79132=CARTESIAN_POINT('',(0.866025403784439,1.5,-4.));
#79133=CARTESIAN_POINT('',(0.866025403784439,1.5,-2.));
#79134=CARTESIAN_POINT('Origin',(1.73205080756888,0.,-4.));
#79135=CARTESIAN_POINT('',(1.73205080756888,0.,-4.));
#79136=CARTESIAN_POINT('',(1.51554445662277,0.375,-4.));
#79137=CARTESIAN_POINT('',(1.73205080756888,0.,-2.));
#79138=CARTESIAN_POINT('',(1.73205080756888,0.,-4.));
#79139=CARTESIAN_POINT('',(1.73205080756888,0.,-2.));
#79140=CARTESIAN_POINT('Origin',(0.866025403784439,-1.5,-4.));
#79141=CARTESIAN_POINT('',(1.08253175473055,-1.125,-4.));
#79142=CARTESIAN_POINT('',(0.866025403784439,-1.5,-2.));
#79143=CARTESIAN_POINT('Origin',(0.,2.77555756156289E-16,-2.));
#79144=CARTESIAN_POINT('Origin',(0.,0.,0.));
#79145=CARTESIAN_POINT('',(-3.5,-4.28626379701574E-16,0.));
#79146=CARTESIAN_POINT('Origin',(0.,0.,0.));
#79147=CARTESIAN_POINT('Origin',(0.,0.,-4.));
#79148=CARTESIAN_POINT('',(-3.5,-4.28626379701574E-16,-4.));
#79149=CARTESIAN_POINT('',(-3.5,-4.28626379701574E-16,-4.));
#79150=CARTESIAN_POINT('Origin',(0.,0.,-4.));
#79151=CARTESIAN_POINT('Origin',(0.,0.,-4.));
#79152=CARTESIAN_POINT('Origin',(0.,0.,10.));
#94390=UNCERTAINTY_MEASURE_WITH_UNIT(LENGTH_MEASURE(0.01),#94413,
'DISTANCE_ACCURACY_VALUE',
'Maximum model space distance between geometric entities at asserted c
onnectivities');
#94394=UNCERTAINTY_MEASURE_WITH_UNIT(LENGTH_MEASURE(0.01),#94413,
'DISTANCE_ACCURACY_VALUE',
'Maximum model space distance between geometric entities at asserted c
onnectivities');
#94408=(
GEOMETRIC_REPRESENTATION_CONTEXT(3)
GLOBAL_UNCERTAINTY_ASSIGNED_CONTEXT((#94390))
GLOBAL_UNIT_ASSIGNED_CONTEXT((#94413,#94415,#94416))
REPRESENTATION_CONTEXT('','3D')
);
#94412=(
GEOMETRIC_REPRESENTATION_CONTEXT(3)
GLOBAL_UNCERTAINTY_ASSIGNED_CONTEXT((#94394))
GLOBAL_UNIT_ASSIGNED_CONTEXT((#94413,#94415,#94416))
REPRESENTATION_CONTEXT('','3D')
);
#94413=(
LENGTH_UNIT()
NAMED_UNIT(*)
SI_UNIT(.MILLI.,.METRE.)
);
#94415=(
NAMED_UNIT(*)
PLANE_ANGLE_UNIT()
SI_UNIT($,.RADIAN.)
);
#94416=(
NAMED_UNIT(*)
SI_UNIT($,.STERADIAN.)
SOLID_ANGLE_UNIT()
);
#94430=SHAPE_DEFINITION_REPRESENTATION(#94464,#94499);
#94464=PRODUCT_DEFINITION_SHAPE('',$,#94517);
#94499=SHAPE_REPRESENTATION('',(#8810),#94408);
#94503=PRODUCT_DEFINITION_CONTEXT('part definition',#94556,'design');
#94517=PRODUCT_DEFINITION('Socket head cap screw M4x10',
'Socket head cap screw M4x10',#94534,#94503);
#94534=PRODUCT_DEFINITION_FORMATION('',$,#94571);
#94556=APPLICATION_CONTEXT(
'Core Data for Automotive Mechanical Design Process');
#94557=PRODUCT_CONTEXT('part definition',#94556,'mechanical');
#94571=PRODUCT('Socket head cap screw M4x10',
'Socket head cap screw M4x10',$,(#94557));
#94578=PRESENTATION_STYLE_ASSIGNMENT((#94585));
#94585=SURFACE_STYLE_USAGE(.BOTH.,#94592);
#94592=SURFACE_SIDE_STYLE('',(#94599));
#94599=SURFACE_STYLE_FILL_AREA(#94606);
#94606=FILL_AREA_STYLE('Opaque(64,72,82)',(#94613));
#94613=FILL_AREA_STYLE_COLOUR('Opaque(64,72,82)',#94620);
#94620=COLOUR_RGB('Opaque(64,72,82)',0.250980392156863,0.282352941176471,
0.32156862745098);
ENDSEC;
END-ISO-10303-21;
